ISO-10303-21;
HEADER;
FILE_DESCRIPTION (('STEP AP203'),
    '1' );
FILE_NAME ('PruningShears_Predeterminado.step',
    '2026-10-08T11:28:20',
    ( '' ),
    ( '' ),
    'SwSTEP 2.0',
    'SolidWorks 2024',
    '' );
FILE_SCHEMA (( 'AUTOMOTIVE_DESIGN' ));
ENDSEC;

DATA;
#6=CARTESIAN_POINT ( 'NONE',  ( 8.895558325401111688, 6.000000000000000000, -141.4560052469132643 ) ) ;
#10=( BOUNDED_SURFACE ( )  B_SPLINE_SURFACE ( 3, 2, ( 
 ( #2250, #5719, #10439 ),
 ( #12764, #3401, #13776 ),
 ( #9122, #8110, #5419 ),
 ( #12528, #2173, #793 ),
 ( #9278, #3171, #9054 ),
 ( #6877, #11445, #7884 ),
 ( #5641, #7962, #13852 ),
 ( #1011, #6953, #14952 ),
 ( #3250, #868, #2099 ),
 ( #10357, #4569, #1944 ),
 ( #15098, #11671, #12608 ),
 ( #4272, #6806, #14003 ),
 ( #12683, #8975, #11522 ),
 ( #3329, #938, #6657 ),
 ( #8038, #13706, #12837 ),
 ( #11370, #3105, #7816 ),
 ( #5571, #9201, #4347 ),
 ( #2023, #6733, #10286 ) ),
 .UNSPECIFIED., .F., .F., .F. ) 
 B_SPLINE_SURFACE_WITH_KNOTS ( ( 4, 2, 2, 2, 2, 2, 2, 2, 4 ),
 ( 3, 3 ),
 ( 0.06508395618386217385, 0.06791873945841907234, 0.07075352273297597083, 0.07217091437025441314, 0.07358830600753285545, 0.07642308928208975394, 0.07925787255664665243, 0.08209265583120353704, 0.08776222238031733403 ),
 ( 0.000000000000000000, 1.000000000000000000 ),
 .UNSPECIFIED. ) 
 GEOMETRIC_REPRESENTATION_ITEM ( )  RATIONAL_B_SPLINE_SURFACE ( (
 ( 1.000000000000000000, 0.7071067811865475727, 1.000000000000000000),
 ( 1.000000000000000000, 0.7071067811865475727, 1.000000000000000000),
 ( 1.000000000000000000, 0.7071067811865475727, 1.000000000000000000),
 ( 1.000000000000000000, 0.7071067811865475727, 1.000000000000000000),
 ( 1.000000000000000000, 0.7071067811865471286, 1.000000000000000000),
 ( 1.000000000000000000, 0.7071067811865471286, 1.000000000000000000),
 ( 1.000000000000000000, 0.7071067811865475727, 1.000000000000000000),
 ( 1.000000000000000000, 0.7071067811865475727, 1.000000000000000000),
 ( 1.000000000000000000, 0.7071067811865475727, 1.000000000000000000),
 ( 1.000000000000000000, 0.7071067811865475727, 1.000000000000000000),
 ( 1.000000000000000000, 0.7071067811865475727, 1.000000000000000000),
 ( 1.000000000000000000, 0.7071067811865475727, 1.000000000000000000),
 ( 1.000000000000000000, 0.7071067811865475727, 1.000000000000000000),
 ( 1.000000000000000000, 0.7071067811865475727, 1.000000000000000000),
 ( 1.000000000000000000, 0.7071067811865475727, 1.000000000000000000),
 ( 1.000000000000000000, 0.7071067811865475727, 1.000000000000000000),
 ( 1.000000000000000000, 0.7071067811865474617, 1.000000000000000000),
 ( 1.000000000000000000, 0.7071067811865474617, 1.000000000000000000) ) ) 
 REPRESENTATION_ITEM ( '' )  SURFACE ( )  );
#14=CIRCLE ( 'NONE', #8648, 3.500000000000003109 ) ;
#16=VERTEX_POINT ( 'NONE', #5138 ) ;
#18=CARTESIAN_POINT ( 'NONE',  ( 11.02991327057161008, 4.000000000000000000, -167.7534593579462125 ) ) ;
#21=CARTESIAN_POINT ( 'NONE',  ( 1.114947364559086829, 5.000000000000000888, -139.4079432275550232 ) ) ;
#22=ORIENTED_EDGE ( 'NONE', *, *, #13407, .T. ) ;
#23=CARTESIAN_POINT ( 'NONE',  ( -6.510167201457561781, 0.4374612817596250647, -117.0692195733290504 ) ) ;
#25=AXIS2_PLACEMENT_3D ( 'NONE', #11533, #14885, #11235 ) ;
#29=CARTESIAN_POINT ( 'NONE',  ( 14.17870013830592235, 8.673617379884035472E-16, -133.6038822290509813 ) ) ;
#33=CARTESIAN_POINT ( 'NONE',  ( 17.45707370880436216, 8.749999999999998224, -89.70141063960701899 ) ) ;
#34=CARTESIAN_POINT ( 'NONE',  ( 12.21230042249527514, -8.519112334771948619E-13, -124.0782217032746217 ) ) ;
#40=VERTEX_POINT ( 'NONE', #4981 ) ;
#46=CARTESIAN_POINT ( 'NONE',  ( 4.515869450399739193, 15.00000000000000000, -104.3391973869742060 ) ) ;
#48=VECTOR ( 'NONE', #1448, 1000.000000000000114 ) ;
#54=ORIENTED_EDGE ( 'NONE', *, *, #7438, .F. ) ;
#64=CARTESIAN_POINT ( 'NONE',  ( 9.455311519598982528, 14.93740492236557138, -106.0041704794325454 ) ) ;
#68=ORIENTED_EDGE ( 'NONE', *, *, #7323, .F. ) ;
#69=CARTESIAN_POINT ( 'NONE',  ( 5.522929128040925839, 0.1436561706274334937, 1.641076506811401270 ) ) ;
#77=CARTESIAN_POINT ( 'NONE',  ( 21.59580923397518859, 6.000000000000000000, -133.6052420832058374 ) ) ;
#78=CARTESIAN_POINT ( 'NONE',  ( 9.096999351293019842, 14.99999999999896438, -106.0212576677412812 ) ) ;
#83=CARTESIAN_POINT ( 'NONE',  ( -0.2962205294200081496, 8.673617379884033500E-16, -113.2751335308100096 ) ) ;
#91=CARTESIAN_POINT ( 'NONE',  ( 8.807773658247754156, 15.00000000000000000, -105.8689255569352667 ) ) ;
#93=ORIENTED_EDGE ( 'NONE', *, *, #14365, .F. ) ;
#96=CARTESIAN_POINT ( 'NONE',  ( 10.93680211553660619, 8.749999999999998224, -88.84347220940026091 ) ) ;
#98=AXIS2_PLACEMENT_3D ( 'NONE', #12343, #1762, #3856 ) ;
#101=DIRECTION ( 'NONE',  ( -0.02181900108494732801, 0.000000000000000000, 0.9997619372588931741 ) ) ;
#105=DIRECTION ( 'NONE',  ( 0.000000000000000000, 1.000000000000000000, 0.000000000000000000 ) ) ;
#107=AXIS2_PLACEMENT_3D ( 'NONE', #15128, #4596, #14185 ) ;
#109=CARTESIAN_POINT ( 'NONE',  ( 10.14688567188825274, 12.49999999999999822, -108.1982192590441088 ) ) ;
#110=CARTESIAN_POINT ( 'NONE',  ( 16.81337476685454391, 5.000000000000000888, -129.2521154345601246 ) ) ;
#116=DIRECTION ( 'NONE',  ( -0.000000000000000000, -1.000000000000000000, -0.000000000000000000 ) ) ;
#120=CARTESIAN_POINT ( 'NONE',  ( -1.334601435215557519, 9.999999999999998224, -105.6792246796216403 ) ) ;
#128=ORIENTED_EDGE ( 'NONE', *, *, #6104, .F. ) ;
#130=CARTESIAN_POINT ( 'NONE',  ( -4.234402844927150689, 15.00000000000000000, -117.4888040839639558 ) ) ;
#133=B_SPLINE_CURVE_WITH_KNOTS ( 'NONE', 3,
 ( #5793, #4490, #6875, #8036, #2247, #9119, #866, #3327, #10513, #12761, #13773, #3478, #11520, #10215, #15248, #4639, #8187, #5717, #11590, #14950, #12912, #2325, #9052, #7024 ),
 .UNSPECIFIED., .F., .F.,
 ( 4, 2, 2, 2, 2, 2, 2, 2, 2, 2, 2, 4 ),
 ( 0.001027084968682773474, 0.001754664737541044694, 0.002482244506399315480, 0.003937404044115912563, 0.004664983812974211538, 0.005392563581832510514, 0.006847723119549108464, 0.009758042194982304365, 0.01121320173269890232, 0.01194078150155724292, 0.01230457138598641496, 0.01266836127041558527 ),
 .UNSPECIFIED. ) ;
#137=ADVANCED_FACE ( 'NONE', ( #11160 ), #2010, .F. ) ;
#138=CARTESIAN_POINT ( 'NONE',  ( 9.910078351765200466, 14.75237657882121667, -106.1010689402279468 ) ) ;
#140=EDGE_CURVE ( 'NONE', #13676, #587, #14399, .T. ) ;
#144=CARTESIAN_POINT ( 'NONE',  ( 5.475582110871519248, 2.099780042704602945, 4.221432182364227792 ) ) ;
#157=CARTESIAN_POINT ( 'NONE',  ( -5.309262520577839872, 13.36526483154179523, -125.0911079416483176 ) ) ;
#160=DIRECTION ( 'NONE',  ( 0.000000000000000000, -0.000000000000000000, 1.000000000000000000 ) ) ;
#162=EDGE_CURVE ( 'NONE', #10108, #12142, #11036, .T. ) ;
#163=DIRECTION ( 'NONE',  ( -0.000000000000000000, 1.000000000000000000, -0.000000000000000000 ) ) ;
#165=FACE_OUTER_BOUND ( 'NONE', #967, .T. ) ;
#167=CARTESIAN_POINT ( 'NONE',  ( 8.617011912565523346, 3.196949058014985745, 2.666643044219553893 ) ) ;
#169=ORIENTED_EDGE ( 'NONE', *, *, #3673, .F. ) ;
#176=DIRECTION ( 'NONE',  ( -0.9997619372588932851, -0.000000000000000000, -0.02181900108494707474 ) ) ;
#180=CARTESIAN_POINT ( 'NONE',  ( 19.46764420669212470, 5.416677968589100837E-32, -137.9817351395554681 ) ) ;
#182=CARTESIAN_POINT ( 'NONE',  ( -1.794496370643203553, 15.00000000000000711, -123.9659188807642920 ) ) ;
#184=CARTESIAN_POINT ( 'NONE',  ( -4.891470111510197505, 6.071532165918824830E-15, -115.0631877436127581 ) ) ;
#185=CARTESIAN_POINT ( 'NONE',  ( 20.93263444585494781, -4.267469463954428261E-13, -132.7914611339567159 ) ) ;
#187=ORIENTED_EDGE ( 'NONE', *, *, #1290, .T. ) ;
#191=VERTEX_POINT ( 'NONE', #10233 ) ;
#192=CARTESIAN_POINT ( 'NONE',  ( 22.32840821305085655, 0.1344125794277489794, -138.8040290914306922 ) ) ;
#196=CARTESIAN_POINT ( 'NONE',  ( 6.130233522805849766, 11.30590447954031497, 5.118507051967887911 ) ) ;
#205=CARTESIAN_POINT ( 'NONE',  ( -0.9850606648477213678, 15.00000000000000000, -125.5681744140592144 ) ) ;
#208=DIRECTION ( 'NONE',  ( -0.9997619372588932851, -0.000000000000000000, -0.02181900108494707821 ) ) ;
#210=CARTESIAN_POINT ( 'NONE',  ( 9.985685122837379524, 1.585996910455645059, -106.2985558885148833 ) ) ;
#212=CARTESIAN_POINT ( 'NONE',  ( -2.555845825458327170, 14.83119756125146438, -125.3948779398220381 ) ) ;
#215=CARTESIAN_POINT ( 'NONE',  ( 5.309569511722092905, 0.1704923354856621165, -0.3824473862144103231 ) ) ;
#235=DIRECTION ( 'NONE',  ( 0.9997619372588932851, -0.000000000000000000, 0.02181900108494707474 ) ) ;
#236=LINE ( 'NONE', #6346, #3220 ) ;
#237=CARTESIAN_POINT ( 'NONE',  ( -19.59630400042128784, 8.673617379884035472E-16, -169.8472985358678216 ) ) ;
#255=B_SPLINE_CURVE_WITH_KNOTS ( 'NONE', 3,
 ( #476, #7341, #3878, #8660, #12368, #14639, #2797, #7574, #10984, #1631 ),
 .UNSPECIFIED., .F., .F.,
 ( 4, 2, 2, 2, 4 ),
 ( 2.327414349645749169E-05, 0.0008162123097076399297, 0.001609150475918822527, 0.002402088642130005124, 0.003195026808341187505 ),
 .UNSPECIFIED. ) ;
#257=CARTESIAN_POINT ( 'NONE',  ( -8.749806588114534378, 5.000000000000000888, -116.1271478199639944 ) ) ;
#262=CARTESIAN_POINT ( 'NONE',  ( -3.149239014774738887, 4.336808689942018525E-15, -131.9551168574780320 ) ) ;
#263=CARTESIAN_POINT ( 'NONE',  ( 21.65409573403057664, 5.000000000000000888, -133.3516700273328581 ) ) ;
#264=ORIENTED_EDGE ( 'NONE', *, *, #11581, .T. ) ;
#265=CARTESIAN_POINT ( 'NONE',  ( 10.97171279554003043, 8.773889247172311556, -44.61149169061435060 ) ) ;
#268=ORIENTED_EDGE ( 'NONE', *, *, #15190, .T. ) ;
#269=CARTESIAN_POINT ( 'NONE',  ( 26.64344053652503774, 3.212383873964119285, -138.2698333691874382 ) ) ;
#273=VERTEX_POINT ( 'NONE', #7283 ) ;
#275=CARTESIAN_POINT ( 'NONE',  ( -11.39745071144076860, 8.673617379884034486E-16, -180.6895918776547774 ) ) ;
#279=ADVANCED_FACE ( 'NONE', ( #4972 ), #9605, .T. ) ;
#284=AXIS2_PLACEMENT_3D ( 'NONE', #14005, #3560, #9280 ) ;
#285=CARTESIAN_POINT ( 'NONE',  ( -24.73595349569526292, 2.956764506585224606, -208.3499888930396651 ) ) ;
#286=ORIENTED_EDGE ( 'NONE', *, *, #1844, .F. ) ;
#295=CARTESIAN_POINT ( 'NONE',  ( 6.904992501205359900, 0.03088707369837453628, -105.2571219807955600 ) ) ;
#302=CARTESIAN_POINT ( 'NONE',  ( 7.612871144712937799, 1.444594270924061563, 4.322043199100508382 ) ) ;
#309=CARTESIAN_POINT ( 'NONE',  ( 9.781835551935063933, 14.76107634091859211, -106.3941254748761764 ) ) ;
#316=CARTESIAN_POINT ( 'NONE',  ( 10.81319851844414792, 0.4839222075730109651, -164.6269009810859814 ) ) ;
#317=EDGE_CURVE ( 'NONE', #11237, #8015, #6605, .T. ) ;
#321=CARTESIAN_POINT ( 'NONE',  ( -7.527385229589118154, 8.673617379884035472E-16, -152.8686794106570801 ) ) ;
#322=CARTESIAN_POINT ( 'NONE',  ( 9.068716941525991615, 0.000000000000000000, -163.1923081219560174 ) ) ;
#327=ORIENTED_EDGE ( 'NONE', *, *, #13407, .F. ) ;
#332=CYLINDRICAL_SURFACE ( 'NONE', #1318, 3.000000000000011990 ) ;
#334=AXIS2_PLACEMENT_3D ( 'NONE', #907, #6844, #6699 ) ;
#342=ADVANCED_FACE ( 'NONE', ( #8359 ), #7831, .T. ) ;
#343=CARTESIAN_POINT ( 'NONE',  ( -3.608581043498830354, 8.673617379884035472E-16, -119.4283565286392559 ) ) ;
#344=CARTESIAN_POINT ( 'NONE',  ( 3.623039170307543078, 8.673617379884035472E-16, -110.8080360795144372 ) ) ;
#345=ORIENTED_EDGE ( 'NONE', *, *, #4027, .T. ) ;
#348=VECTOR ( 'NONE', #4531, 1000.000000000000114 ) ;
#349=DIRECTION ( 'NONE',  ( 0.000000000000000000, 1.000000000000000000, 0.000000000000000000 ) ) ;
#351=ORIENTED_EDGE ( 'NONE', *, *, #9219, .T. ) ;
#356=ORIENTED_EDGE ( 'NONE', *, *, #13763, .F. ) ;
#357=LINE ( 'NONE', #12527, #6752 ) ;
#361=CARTESIAN_POINT ( 'NONE',  ( -25.42287067452675586, 4.143790226087491035, -209.0992770757332835 ) ) ;
#362=CARTESIAN_POINT ( 'NONE',  ( 4.031205673867843231, 0.1109222935295775953, -0.8398591784643215652 ) ) ;
#366=CARTESIAN_POINT ( 'NONE',  ( -24.98815304704661600, 1.710977557088027678, -206.9418329696514718 ) ) ;
#379=CARTESIAN_POINT ( 'NONE',  ( 8.429434715646030085, 0.4626179564848506565, -105.7324733393003413 ) ) ;
#383=ORIENTED_EDGE ( 'NONE', *, *, #11565, .F. ) ;
#384=CARTESIAN_POINT ( 'NONE',  ( 5.231840533899993595, 1.637990804157756664, 3.762912466793266297 ) ) ;
#391=CARTESIAN_POINT ( 'NONE',  ( 11.24760135325740507, 13.22314450393356822, -106.7872448694843399 ) ) ;
#400=CARTESIAN_POINT ( 'NONE',  ( -1.694477158799985395, 4.000000000000112799, -141.3413698475477815 ) ) ;
#402=DIRECTION ( 'NONE',  ( -0.000000000000000000, 1.000000000000000000, -0.000000000000000000 ) ) ;
#405=ORIENTED_EDGE ( 'NONE', *, *, #6941, .F. ) ;
#412=EDGE_CURVE ( 'NONE', #5516, #2826, #7749, .T. ) ;
#419=CARTESIAN_POINT ( 'NONE',  ( -8.589347325610479089, 9.999999999999184652, -120.3237211899656955 ) ) ;
#421=CARTESIAN_POINT ( 'NONE',  ( -9.247150027884355694, 4.999999999998421707, -118.2023151954170288 ) ) ;
#422=CARTESIAN_POINT ( 'NONE',  ( 3.734989709506049138, 8.673617379884035472E-16, -110.3183269162431230 ) ) ;
#425=CARTESIAN_POINT ( 'NONE',  ( 10.96506291612846162, 11.77387593150068668, -44.79863320250961323 ) ) ;
#426=ORIENTED_EDGE ( 'NONE', *, *, #15123, .F. ) ;
#427=ORIENTED_EDGE ( 'NONE', *, *, #7782, .T. ) ;
#434=EDGE_LOOP ( 'NONE', ( #13261, #4707, #9189, #5976 ) ) ;
#436=( BOUNDED_CURVE ( )  B_SPLINE_CURVE ( 3, ( #14135, #7607, #10719, #6304 ),
 .UNSPECIFIED., .F., .F. ) 
 B_SPLINE_CURVE_WITH_KNOTS ( ( 4, 4 ),
 ( 1.570796326794899667, 1.765402715644074361 ),
 .UNSPECIFIED. ) 
 CURVE ( )  GEOMETRIC_REPRESENTATION_ITEM ( )  RATIONAL_B_SPLINE_CURVE ( ( 1.000000000000000000, 0.9968465187034001307, 0.9968465187034001307, 1.000000000000000000 ) ) 
 REPRESENTATION_ITEM ( '' )  );
#439=CARTESIAN_POINT ( 'NONE',  ( 1.078198036487820088, 5.000000000000000888, -139.4303465535634245 ) ) ;
#452=CARTESIAN_POINT ( 'NONE',  ( 6.436143463598923198, 9.999999999999998224, 2.800833825385760090 ) ) ;
#454=CARTESIAN_POINT ( 'NONE',  ( 11.01414178047344095, 4.315957715773897974, -107.1012222462659196 ) ) ;
#458=ORIENTED_EDGE ( 'NONE', *, *, #10462, .T. ) ;
#465=CARTESIAN_POINT ( 'NONE',  ( 10.67045167996756128, 14.18553633651329804, -106.2656505685997104 ) ) ;
#473=CARTESIAN_POINT ( 'NONE',  ( 12.49422757225345570, 2.167092202804963730, -165.7027478962374971 ) ) ;
#475=CARTESIAN_POINT ( 'NONE',  ( -8.055328022171806879, 8.673617379884035472E-16, -153.4262481318472737 ) ) ;
#476=CARTESIAN_POINT ( 'NONE',  ( 6.577825583858426306, 0.000000000000000000, -139.0000488628143103 ) ) ;
#477=CARTESIAN_POINT ( 'NONE',  ( -25.40168623993593400, 8.673617379884045333E-16, -197.6107370494183044 ) ) ;
#478=EDGE_LOOP ( 'NONE', ( #9570, #4632, #3133, #10760 ) ) ;
#480=ORIENTED_EDGE ( 'NONE', *, *, #12357, .T. ) ;
#481=DIRECTION ( 'NONE',  ( 0.000000000000000000, -0.9434476287765544145, 0.3315216007380165641 ) ) ;
#482=CARTESIAN_POINT ( 'NONE',  ( -19.28976728528864371, 4.000000000000588862, -198.7222929113018779 ) ) ;
#495=CARTESIAN_POINT ( 'NONE',  ( 3.361270396691331541, 8.673617379884035472E-16, -115.2606357392248242 ) ) ;
#498=CARTESIAN_POINT ( 'NONE',  ( 10.95172361697086139, 11.63674386448545128, -43.69557350477573010 ) ) ;
#500=CARTESIAN_POINT ( 'NONE',  ( 10.00087860767147241, 5.000000000000001776, -45.95880046359210525 ) ) ;
#509=AXIS2_PLACEMENT_3D ( 'NONE', #9059, #10445, #12537 ) ;
#510=CARTESIAN_POINT ( 'NONE',  ( 9.958926971456385502, 12.69564389515387326, -44.38794094253861999 ) ) ;
#512=DIRECTION ( 'NONE',  ( 0.000000000000000000, 1.000000000000000000, 0.000000000000000000 ) ) ;
#517=EDGE_CURVE ( 'NONE', #14224, #673, #14001, .T. ) ;
#520=AXIS2_PLACEMENT_3D ( 'NONE', #7871, #1136, #702 ) ;
#526=CARTESIAN_POINT ( 'NONE',  ( -5.309262520577839872, 6.000000000000000000, -125.0911079416483176 ) ) ;
#530=CARTESIAN_POINT ( 'NONE',  ( 3.902875325215932723, 12.49999999999999822, -114.6800873586639824 ) ) ;
#534=EDGE_CURVE ( 'NONE', #8407, #5461, #13303, .T. ) ;
#544=DIRECTION ( 'NONE',  ( -0.000000000000000000, -1.000000000000000000, -0.000000000000000000 ) ) ;
#550=CARTESIAN_POINT ( 'NONE',  ( 12.35274956116099254, 1.933739209396013514, -165.5990192671287105 ) ) ;
#552=EDGE_CURVE ( 'NONE', #6914, #4341, #15183, .T. ) ;
#553=CARTESIAN_POINT ( 'NONE',  ( -17.27880384526778101, 1.734723475976807094E-15, -165.6175314860322771 ) ) ;
#560=CARTESIAN_POINT ( 'NONE',  ( 13.47730208875211844, 6.000000000000000000, -127.1728814958210876 ) ) ;
#561=CARTESIAN_POINT ( 'NONE',  ( 6.941279403247599511, 5.883355326356809467E-13, -105.1775688070215438 ) ) ;
#566=CARTESIAN_POINT ( 'NONE',  ( -9.385448346790807861, 4.636404319127126250, -115.3551636526218687 ) ) ;
#576=CARTESIAN_POINT ( 'NONE',  ( 11.18419171849477323, 5.000000000000000888, -106.9754176129513752 ) ) ;
#577=CARTESIAN_POINT ( 'NONE',  ( -6.790153584124027475, 6.000000000000000000, -124.9643354754709748 ) ) ;
#579=ORIENTED_EDGE ( 'NONE', *, *, #14346, .F. ) ;
#580=CARTESIAN_POINT ( 'NONE',  ( 10.98638911170980670, 5.830450750434273743, -45.28397108166865337 ) ) ;
#581=CARTESIAN_POINT ( 'NONE',  ( 11.97422441543835525, 12.49999999999999289, -123.6845202709325520 ) ) ;
#583=CIRCLE ( 'NONE', #13426, 2.499999999999999556 ) ;
#587=VERTEX_POINT ( 'NONE', #5869 ) ;
#592=CARTESIAN_POINT ( 'NONE',  ( 4.804596213718521192, 0.9953211363309286686, 2.828019302905943722 ) ) ;
#593=CARTESIAN_POINT ( 'NONE',  ( 26.88777289245741642, 6.000000000000000000, -138.4814624290441429 ) ) ;
#604=AXIS2_PLACEMENT_3D ( 'NONE', #5543, #14991, #4390 ) ;
#606=ADVANCED_FACE ( 'NONE', ( #6812 ), #11530, .F. ) ;
#610=CARTESIAN_POINT ( 'NONE',  ( -5.794432043291358525, 6.000000000000000000, -125.0404107129116085 ) ) ;
#621=CARTESIAN_POINT ( 'NONE',  ( 11.24846813935491596, 13.18102764301277219, -106.3932454387446285 ) ) ;
#627=CARTESIAN_POINT ( 'NONE',  ( -7.472766077161563381, 0.9471434298996047607, -116.8715385114339966 ) ) ;
#631=DIRECTION ( 'NONE',  ( 0.7260798585963988971, 0.000000000000000000, 0.6876103830954222174 ) ) ;
#632=CARTESIAN_POINT ( 'NONE',  ( -21.40529191659825159, 8.673617379884035472E-16, -173.7943469130565290 ) ) ;
#633=CARTESIAN_POINT ( 'NONE',  ( 12.76858567064540217, 3.999999999993260502, -166.6103056774037441 ) ) ;
#641=FACE_OUTER_BOUND ( 'NONE', #434, .T. ) ;
#648=EDGE_CURVE ( 'NONE', #13215, #10636, #6120, .T. ) ;
#654=CARTESIAN_POINT ( 'NONE',  ( 8.322646197901347520, 2.167618682171565639E-13, -114.4990917221396103 ) ) ;
#656=ORIENTED_EDGE ( 'NONE', *, *, #3653, .T. ) ;
#657=CARTESIAN_POINT ( 'NONE',  ( 10.01221399140626644, 5.773894451085546997, -44.97775305520311662 ) ) ;
#658=CARTESIAN_POINT ( 'NONE',  ( 4.999999999999998224, 15.00000000000000178, -101.4583377608209389 ) ) ;
#664=CARTESIAN_POINT ( 'NONE',  ( 10.99551757066059032, 11.56847231179307656, -45.70224318734323532 ) ) ;
#665=EDGE_CURVE ( 'NONE', #7526, #1605, #6267, .T. ) ;
#667=CARTESIAN_POINT ( 'NONE',  ( 4.736400576334578005, 0.9069609750089387967, 2.656850315087319281 ) ) ;
#669=CARTESIAN_POINT ( 'NONE',  ( 27.03835354040190708, 6.000000000000000000, -138.2189567750509696 ) ) ;
#671=CARTESIAN_POINT ( 'NONE',  ( 13.66360635606377905, 12.49999999999999822, -125.8738101254713513 ) ) ;
#672=CARTESIAN_POINT ( 'NONE',  ( 26.71007981189074343, 4.606906972201797679, -136.8791680518442320 ) ) ;
#673=VERTEX_POINT ( 'NONE', #14309 ) ;
#677=AXIS2_PLACEMENT_3D ( 'NONE', #6, #9437, #944 ) ;
#679=CARTESIAN_POINT ( 'NONE',  ( -8.817544209126937815, 12.32420660420548764, -115.6114935513795103 ) ) ;
#686=CARTESIAN_POINT ( 'NONE',  ( 8.855022830454526428, 5.000000000000000888, -117.5519203246167876 ) ) ;
#693=CARTESIAN_POINT ( 'NONE',  ( 10.80856694317891176, 13.64261357360079074, -106.9774774610350789 ) ) ;
#702=DIRECTION ( 'NONE',  ( 0.000000000000000000, 0.000000000000000000, 1.000000000000000000 ) ) ;
#704=ORIENTED_EDGE ( 'NONE', *, *, #7602, .F. ) ;
#705=CARTESIAN_POINT ( 'NONE',  ( -26.83547194577748130, 4.000000000000714984, -174.1755862676965023 ) ) ;
#706=CARTESIAN_POINT ( 'NONE',  ( 10.73855780921090641, 0.4779626745339241589, -164.7294754465163180 ) ) ;
#710=ORIENTED_EDGE ( 'NONE', *, *, #5262, .F. ) ;
#714=CARTESIAN_POINT ( 'NONE',  ( -20.63752471692298229, 8.673617379884034486E-16, -191.9478744570439233 ) ) ;
#719=VECTOR ( 'NONE', #9665, 1000.000000000000000 ) ;
#725=CARTESIAN_POINT ( 'NONE',  ( 26.73765619226448464, 5.000000000000000888, -138.7442522361673127 ) ) ;
#728=EDGE_CURVE ( 'NONE', #8528, #2185, #3376, .T. ) ;
#729=CARTESIAN_POINT ( 'NONE',  ( 10.97489471145172324, 5.773894329885068899, -44.95261283940258323 ) ) ;
#730=CARTESIAN_POINT ( 'NONE',  ( -11.98491608995024649, 4.000000000000000888, -188.7215518410329196 ) ) ;
#733=EDGE_CURVE ( 'NONE', #7347, #6645, #12998, .T. ) ;
#737=CARTESIAN_POINT ( 'NONE',  ( 10.00369055844187827, 12.49999999999999822, -46.08764602067113714 ) ) ;
#739=CARTESIAN_POINT ( 'NONE',  ( 4.275750346740477603, 0.3778493581961822056, 1.174871939900954620 ) ) ;
#740=CARTESIAN_POINT ( 'NONE',  ( -9.513824166154529749, 11.41184093592985072, -116.4115394435323907 ) ) ;
#742=CARTESIAN_POINT ( 'NONE',  ( 8.317394296536116727, 12.49999999999999822, -114.4625571486762254 ) ) ;
#744=CARTESIAN_POINT ( 'NONE',  ( 23.26395690036145680, 0.3310048020727625606, -138.4206416885019735 ) ) ;
#747=CARTESIAN_POINT ( 'NONE',  ( -29.69146998481285138, 4.000000000000000000, -183.7653926644912303 ) ) ;
#754=AXIS2_PLACEMENT_3D ( 'NONE', #5135, #7448, #1582 ) ;
#756=DIRECTION ( 'NONE',  ( -0.02181900108494696719, 0.000000000000000000, 0.9997619372588931741 ) ) ;
#764=AXIS2_PLACEMENT_3D ( 'NONE', #12903, #2315, #4335 ) ;
#768=CARTESIAN_POINT ( 'NONE',  ( 30.96695154071790412, 8.773889247172311556, -44.17511166891541308 ) ) ;
#771=CIRCLE ( 'NONE', #11377, 6.000000000000005329 ) ;
#775=CARTESIAN_POINT ( 'NONE',  ( 10.95001698349728336, 5.943472311793079221, -43.61737436169475046 ) ) ;
#779=FACE_OUTER_BOUND ( 'NONE', #3430, .T. ) ;
#780=DIRECTION ( 'NONE',  ( 0.02181900108494707127, 0.000000000000000000, -0.9997619372588931741 ) ) ;
#781=CARTESIAN_POINT ( 'NONE',  ( 9.049521024876144182, 0.9101575677978732681, -106.1719994250351533 ) ) ;
#782=AXIS2_PLACEMENT_3D ( 'NONE', #7076, #13916, #9800 ) ;
#784=CARTESIAN_POINT ( 'NONE',  ( -27.95915014381559871, 4.000000000000232703, -177.3149405089903325 ) ) ;
#788=VERTEX_POINT ( 'NONE', #3566 ) ;
#789=DIRECTION ( 'NONE',  ( -0.000000000000000000, -1.000000000000000000, -0.000000000000000000 ) ) ;
#793=CARTESIAN_POINT ( 'NONE',  ( 4.515869450397831386, 0.000000000000000000, -104.3391973869891416 ) ) ;
#796=CARTESIAN_POINT ( 'NONE',  ( 1.123679064339592859, 4.590773665857039276, -139.4222662838609210 ) ) ;
#797=EDGE_CURVE ( 'NONE', #6985, #13403, #11978, .T. ) ;
#810=CARTESIAN_POINT ( 'NONE',  ( -16.36917573835871309, 4.000000000000001776, -194.3843815398161894 ) ) ;
#819=CARTESIAN_POINT ( 'NONE',  ( -25.30358147364459143, 4.000000000000000000, -209.1611233605720201 ) ) ;
#821=CARTESIAN_POINT ( 'NONE',  ( 9.146012981469503700, 15.00000000000000000, -118.4481327387345857 ) ) ;
#822=CYLINDRICAL_SURFACE ( 'NONE', #9374, 2.000000000000001776 ) ;
#823=CARTESIAN_POINT ( 'NONE',  ( 1.243260443319662123, 4.179859613694246079, -139.4020581015306846 ) ) ;
#826=CARTESIAN_POINT ( 'NONE',  ( -30.52456163227999753, 4.000000000000000000, -196.5486136056819362 ) ) ;
#828=ORIENTED_EDGE ( 'NONE', *, *, #9715, .F. ) ;
#832=CIRCLE ( 'NONE', #8231, 4.999999999999992895 ) ;
#833=CARTESIAN_POINT ( 'NONE',  ( -25.67290302457112006, 1.351337947638526771, -206.3516727230842491 ) ) ;
#837=EDGE_CURVE ( 'NONE', #10045, #8227, #6025, .T. ) ;
#839=EDGE_CURVE ( 'NONE', #4330, #9805, #4660, .T. ) ;
#842=CIRCLE ( 'NONE', #12440, 3.000000000000005329 ) ;
#844=VECTOR ( 'NONE', #5757, 1000.000000000000000 ) ;
#846=CARTESIAN_POINT ( 'NONE',  ( 8.673617379884035472E-16, 15.00000000000000000, -1.663700395152567513 ) ) ;
#849=CARTESIAN_POINT ( 'NONE',  ( -8.817544209126905841, 2.675793395794448859, -115.6114935513795672 ) ) ;
#850=CARTESIAN_POINT ( 'NONE',  ( -4.234402844927150689, 0.000000000000000000, -117.4888040839639558 ) ) ;
#853=CIRCLE ( 'NONE', #107, 1.000000000000000888 ) ;
#859=CARTESIAN_POINT ( 'NONE',  ( -28.35615173165206215, 0.000000000000000000, -181.5209395138616912 ) ) ;
#865=DIRECTION ( 'NONE',  ( 1.000000000000000000, 0.000000000000000000, 0.000000000000000000 ) ) ;
#866=CARTESIAN_POINT ( 'NONE',  ( -25.59205555683100641, 2.114949368667459417, -207.6177744677006274 ) ) ;
#867=CARTESIAN_POINT ( 'NONE',  ( 6.124315080327858318, 10.65467060482632178, 5.249130883299187644 ) ) ;
#868=CARTESIAN_POINT ( 'NONE',  ( -1.499260709884682408, -1.623598343467119499E-12, -106.0110764664930940 ) ) ;
#870=CARTESIAN_POINT ( 'NONE',  ( 22.05157068914783380, 5.000000000000000888, -147.3126055969165407 ) ) ;
#881=VERTEX_POINT ( 'NONE', #4261 ) ;
#890=CARTESIAN_POINT ( 'NONE',  ( 10.99170198404801724, 11.63674357114055624, -45.52741062780659576 ) ) ;
#893=CARTESIAN_POINT ( 'NONE',  ( -9.817351912530863700, 10.77704051039747490, -115.7707972434356520 ) ) ;
#895=CARTESIAN_POINT ( 'NONE',  ( 7.666318370587849707, 15.00000000000000000, -107.4043470738708237 ) ) ;
#896=CARTESIAN_POINT ( 'NONE',  ( -8.926802767664696603, 12.61830395633300661, -116.5496838980187988 ) ) ;
#898=CARTESIAN_POINT ( 'NONE',  ( 26.52981115270372925, 2.371853495815368973, -137.6347934788561247 ) ) ;
#905=EDGE_LOOP ( 'NONE', ( #12470, #7304, #11009, #7164 ) ) ;
#907=CARTESIAN_POINT ( 'NONE',  ( 0.5944212552585367293, 5.000000000000000888, -138.5540974747773930 ) ) ;
#912=CARTESIAN_POINT ( 'NONE',  ( 10.23520164300409441, 4.999999999999998224, -120.8438954876117180 ) ) ;
#913=DIRECTION ( 'NONE',  ( 0.9997619372588932851, 0.000000000000000000, 0.02181900108494707821 ) ) ;
#917=DIRECTION ( 'NONE',  ( 0.9997619372588932851, 0.000000000000000000, 0.02181900108494707821 ) ) ;
#926=CARTESIAN_POINT ( 'NONE',  ( 11.05907272987663070, 13.62184257006102150, -106.3512328423712177 ) ) ;
#928=ORIENTED_EDGE ( 'NONE', *, *, #5981, .F. ) ;
#929=CARTESIAN_POINT ( 'NONE',  ( -24.61704333935664124, 8.673617379884035472E-16, -200.7969854990674605 ) ) ;
#933=VERTEX_POINT ( 'NONE', #6415 ) ;
#937=CARTESIAN_POINT ( 'NONE',  ( 8.954400122595130185, 11.89263850632991293, 1.991577900038186799 ) ) ;
#938=CARTESIAN_POINT ( 'NONE',  ( -4.781971238309704830, 1.734723475976807094E-15, -110.8602639898849418 ) ) ;
#944=DIRECTION ( 'NONE',  ( 0.000000000000000000, 0.000000000000000000, 1.000000000000000000 ) ) ;
#949=ORIENTED_EDGE ( 'NONE', *, *, #8090, .T. ) ;
#951=CARTESIAN_POINT ( 'NONE',  ( 0.1414445318493903758, 0.000000000000000000, -169.8395012284044867 ) ) ;
#954=CARTESIAN_POINT ( 'NONE',  ( 26.64925767285982161, 4.000000000000000000, -138.6957041034480653 ) ) ;
#955=EDGE_LOOP ( 'NONE', ( #6140, #13422, #2165, #11339 ) ) ;
#957=CARTESIAN_POINT ( 'NONE',  ( 0.000000000000000000, 5.000000000000000888, -100.6237003951525679 ) ) ;
#961=CARTESIAN_POINT ( 'NONE',  ( 9.667889503803975160, 12.49999999999999822, -108.9228968456644537 ) ) ;
#964=B_SPLINE_CURVE_WITH_KNOTS ( 'NONE', 3,
 ( #5074, #8538, #4909, #11858, #14518, #2441, #7135, #1283, #10709, #9624, #4837, #14357, #9549, #14275, #7376, #3756 ),
 .UNSPECIFIED., .F., .F.,
 ( 4, 2, 2, 2, 2, 2, 2, 4 ),
 ( -1.886156721772299085E-05, 0.0008578064990923553543, 0.001734474565402433811, 0.003487810698022590292, 0.004364478764332667231, 0.005241146830642744170, 0.006117814896952821109, 0.006994482963262898048 ),
 .UNSPECIFIED. ) ;
#965=CARTESIAN_POINT ( 'NONE',  ( 26.98129511509239720, 4.223198481478519284, -138.2263353510321053 ) ) ;
#967=EDGE_LOOP ( 'NONE', ( #8072, #15134, #4528, #327 ) ) ;
#970=CARTESIAN_POINT ( 'NONE',  ( -20.64382723625413263, 3.999999999999999112, -161.8400422034196424 ) ) ;
#977=CARTESIAN_POINT ( 'NONE',  ( -25.49856690235932177, 3.011500147457180976, -208.5102016022315752 ) ) ;
#981=EDGE_CURVE ( 'NONE', #10451, #3740, #9627, .T. ) ;
#982=CARTESIAN_POINT ( 'NONE',  ( 14.55113584266641169, 5.000000000000001776, -126.9185724433401248 ) ) ;
#987=CARTESIAN_POINT ( 'NONE',  ( -3.664341105599659976, 9.999999999999994671, -109.4598404583043987 ) ) ;
#992=CARTESIAN_POINT ( 'NONE',  ( 4.999999999999998224, 0.000000000000000000, -45.97309604003007877 ) ) ;
#995=CIRCLE ( 'NONE', #12103, 5.000000000000000000 ) ;
#1003=TOROIDAL_SURFACE ( 'NONE', #9148, 2.000000000000000000, 5.000000000000000000 ) ;
#1007=( BOUNDED_CURVE ( )  B_SPLINE_CURVE ( 3, ( #8686, #2825, #4208, #6294 ),
 .UNSPECIFIED., .F., .T. ) 
 B_SPLINE_CURVE_WITH_KNOTS ( ( 4, 4 ),
 ( 4.517782591535512537, 4.712388980384686121 ),
 .UNSPECIFIED. ) 
 CURVE ( )  GEOMETRIC_REPRESENTATION_ITEM ( )  RATIONAL_B_SPLINE_CURVE ( ( 1.000000000000000000, 0.9968465187034001307, 0.9968465187034001307, 1.000000000000000000 ) ) 
 REPRESENTATION_ITEM ( '' )  );
#1008=CARTESIAN_POINT ( 'NONE',  ( 6.288457687488933523, 0.000000000000000000, -105.0111312234435985 ) ) ;
#1011=CARTESIAN_POINT ( 'NONE',  ( -1.334601435215332810, 5.000000000000000888, -105.6792246796211572 ) ) ;
#1014=CARTESIAN_POINT ( 'NONE',  ( 13.15367060044211733, 5.000000000000000888, -166.3809663071982641 ) ) ;
#1019=EDGE_CURVE ( 'NONE', #8185, #8798, #11512, .T. ) ;
#1029=CARTESIAN_POINT ( 'NONE',  ( -15.99371261050736059, 8.673617379884035472E-16, -185.9135522072651270 ) ) ;
#1033=ORIENTED_EDGE ( 'NONE', *, *, #162, .F. ) ;
#1041=CARTESIAN_POINT ( 'NONE',  ( 8.122171302341582688, 15.00000000000000000, -106.7308232591198447 ) ) ;
#1047=ORIENTED_EDGE ( 'NONE', *, *, #3849, .F. ) ;
#1050=CARTESIAN_POINT ( 'NONE',  ( 8.990525241558630754, 12.49999999999999822, 0.3362996048474836686 ) ) ;
#1054=CARTESIAN_POINT ( 'NONE',  ( 2.958795351717913302, 15.00000000000000000, -108.2770199283341270 ) ) ;
#1058=CARTESIAN_POINT ( 'NONE',  ( -25.69488127297490010, 1.053316850392583603, -205.6773358527060509 ) ) ;
#1063=VERTEX_POINT ( 'NONE', #10505 ) ;
#1069=CARTESIAN_POINT ( 'NONE',  ( 10.94790802041947941, 11.56847231179307656, -43.52074019388548010 ) ) ;
#1076=CIRCLE ( 'NONE', #9720, 3.000000000000005329 ) ;
#1077=CARTESIAN_POINT ( 'NONE',  ( 9.978237861888676008, 4.811578193488561084, -45.08415836920456599 ) ) ;
#1080=CARTESIAN_POINT ( 'NONE',  ( -30.01749617214946042, 3.999999999999751754, -199.5820917270032453 ) ) ;
#1087=CARTESIAN_POINT ( 'NONE',  ( 8.938384216414224426, 10.81018948157493220, 2.725437957519308618 ) ) ;
#1088=EDGE_CURVE ( 'NONE', #1352, #13049, #14712, .T. ) ;
#1091=AXIS2_PLACEMENT_3D ( 'NONE', #4040, #8970, #8745 ) ;
#1092=CARTESIAN_POINT ( 'NONE',  ( 4.999999999999999112, 0.000000000000000000, -100.6237003951525679 ) ) ;
#1099=AXIS2_PLACEMENT_3D ( 'NONE', #8541, #6456, #8617 ) ;
#1101=CARTESIAN_POINT ( 'NONE',  ( 27.03835354040193195, 5.000000000000000888, -138.2189567750509980 ) ) ;
#1102=ORIENTED_EDGE ( 'NONE', *, *, #11420, .T. ) ;
#1118=CYLINDRICAL_SURFACE ( 'NONE', #9743, 1.000000000000000888 ) ;
#1119=CARTESIAN_POINT ( 'NONE',  ( 18.61385351463323090, 8.673617379884035472E-16, -137.3217374087719520 ) ) ;
#1120=VERTEX_POINT ( 'NONE', #13992 ) ;
#1125=CARTESIAN_POINT ( 'NONE',  ( -9.721966606378851239, 10.00000000000000000, -116.3614657639809309 ) ) ;
#1129=CARTESIAN_POINT ( 'NONE',  ( 0.2132689653709242128, 15.00000000000000000, -112.6263465441548561 ) ) ;
#1133=B_SPLINE_CURVE_WITH_KNOTS ( 'NONE', 3,
 ( #10230, #10373, #725, #4427 ),
 .UNSPECIFIED., .F., .F.,
 ( 4, 4 ),
 ( 0.000000000000000000, 0.0009078663748908937306 ),
 .UNSPECIFIED. ) ;
#1134=CARTESIAN_POINT ( 'NONE',  ( -24.64352728812290039, 3.658198090794281931, -208.7829853464023984 ) ) ;
#1136=DIRECTION ( 'NONE',  ( 0.000000000000000000, 1.000000000000000000, 0.000000000000000000 ) ) ;
#1138=DIRECTION ( 'NONE',  ( 0.000000000000000000, -1.000000000000000000, 0.000000000000000000 ) ) ;
#1152=CARTESIAN_POINT ( 'NONE',  ( -22.03984370847868490, 0.000000000000000000, -205.5299584989701600 ) ) ;
#1159=CARTESIAN_POINT ( 'NONE',  ( 9.068716941525991615, 0.000000000000000000, -163.1923081219560174 ) ) ;
#1165=DIRECTION ( 'NONE',  ( 0.000000000000000000, 0.000000000000000000, -1.000000000000000000 ) ) ;
#1166=EDGE_CURVE ( 'NONE', #4807, #3224, #3390, .T. ) ;
#1168=EDGE_CURVE ( 'NONE', #11237, #4454, #4051, .T. ) ;
#1173=ORIENTED_EDGE ( 'NONE', *, *, #9323, .F. ) ;
#1176=CARTESIAN_POINT ( 'NONE',  ( 8.424062888332693788, 12.50000000000000178, -112.3245025925639169 ) ) ;
#1182=CARTESIAN_POINT ( 'NONE',  ( -1.653263949012559797, 5.000000000000000888, -106.3284344075506311 ) ) ;
#1183=FACE_OUTER_BOUND ( 'NONE', #6773, .T. ) ;
#1186=CARTESIAN_POINT ( 'NONE',  ( 10.32040002734018991, 12.49999999999999822, -106.4311084481271479 ) ) ;
#1187=CARTESIAN_POINT ( 'NONE',  ( 4.114500516011223574, 1.734723475976807094E-15, -119.1606835011388767 ) ) ;
#1188=ORIENTED_EDGE ( 'NONE', *, *, #9195, .T. ) ;
#1192=VERTEX_POINT ( 'NONE', #6942 ) ;
#1193=EDGE_LOOP ( 'NONE', ( #9420, #5533, #9942, #4731, #12082, #12795, #2752, #1848 ) ) ;
#1198=CARTESIAN_POINT ( 'NONE',  ( 6.172117187913792158, 13.05783589229790564, 4.248210876070234399 ) ) ;
#1201=FACE_OUTER_BOUND ( 'NONE', #14682, .T. ) ;
#1204=CARTESIAN_POINT ( 'NONE',  ( 31.03240854397274617, 8.773889247172311556, -47.17439748069210026 ) ) ;
#1206=ORIENTED_EDGE ( 'NONE', *, *, #7217, .T. ) ;
#1212=CARTESIAN_POINT ( 'NONE',  ( 9.548749501005779905, 1.188659780561164281, -105.8881707746913037 ) ) ;
#1218=ORIENTED_EDGE ( 'NONE', *, *, #14526, .T. ) ;
#1219=CARTESIAN_POINT ( 'NONE',  ( 6.010779701672017694, 3.744510043399113641, 5.110648605019955326 ) ) ;
#1221=( BOUNDED_SURFACE ( )  B_SPLINE_SURFACE ( 3, 2, ( 
 ( #5378, #4446, #3060 ),
 ( #12719, #13804, #13887 ),
 ( #7772, #12562, #13733 ),
 ( #14827, #744, #9007 ),
 ( #3204, #5452, #10092 ),
 ( #7921, #12485, #10313 ),
 ( #4226, #14979, #1975 ),
 ( #9159, #7998, #6690 ),
 ( #12641, #9083, #3132 ),
 ( #4526, #7846, #3358 ),
 ( #6767, #5528, #10247 ),
 ( #2130, #11480, #9235 ),
 ( #14906, #898, #5599 ),
 ( #15052, #6833, #3283 ),
 ( #11549, #8932, #8069 ),
 ( #965, #5672, #1615 ),
 ( #6327, #11251, #672 ),
 ( #13660, #1903, #4303 ) ),
 .UNSPECIFIED., .F., .F., .T. ) 
 B_SPLINE_SURFACE_WITH_KNOTS ( ( 4, 2, 2, 2, 2, 2, 2, 2, 4 ),
 ( 3, 3 ),
 ( -1.268724681189376368E-05, 0.001841763813947226193, 0.002768989344326786180, 0.003696214874706346167, 0.004623440405085906153, 0.005087053170275686147, 0.005550665935465466140, 0.006477891465845026127, 0.007405116996224586114 ),
 ( 0.000000000000000000, 1.000000000000000000 ),
 .UNSPECIFIED. ) 
 GEOMETRIC_REPRESENTATION_ITEM ( )  RATIONAL_B_SPLINE_SURFACE ( (
 ( 1.000000000000000000, 1.000000000000000000, 1.000000000000000000),
 ( 1.000000000000000000, 0.9999613041041146566, 1.000000000000000000),
 ( 1.000000000000000000, 0.9910800145946376816, 1.000000000000000000),
 ( 1.000000000000000000, 0.9642327837277934188, 1.000000000000000000),
 ( 1.000000000000000000, 0.9530488795586037343, 1.000000000000000000),
 ( 1.000000000000000000, 0.9269314470905131165, 1.000000000000000000),
 ( 1.000000000000000000, 0.9119402567601512244, 1.000000000000000000),
 ( 1.000000000000000000, 0.8786186012477549268, 1.000000000000000000),
 ( 1.000000000000000000, 0.8602835836478229803, 1.000000000000000000),
 ( 1.000000000000000000, 0.8324170639630756874, 1.000000000000000000),
 ( 1.000000000000000000, 0.8230360448555069652, 1.000000000000000000),
 ( 1.000000000000000000, 0.8044254825442935797, 1.000000000000000000),
 ( 1.000000000000000000, 0.7951379861664216175, 1.000000000000000000),
 ( 1.000000000000000000, 0.7688101143225162248, 1.000000000000000000),
 ( 1.000000000000000000, 0.7531508686541504849, 1.000000000000000000),
 ( 1.000000000000000000, 0.7304464755382781282, 1.000000000000000000),
 ( 1.000000000000000000, 0.7240603277304887841, 1.000000000000000000),
 ( 1.000000000000000000, 0.7240860691865900201, 1.000000000000000000) ) ) 
 REPRESENTATION_ITEM ( '' )  SURFACE ( )  );
#1229=CARTESIAN_POINT ( 'NONE',  ( 9.112379365197755376, 14.99999999812265727, -105.9782736279704238 ) ) ;
#1231=CIRCLE ( 'NONE', #7168, 1.000000000000000222 ) ;
#1235=CARTESIAN_POINT ( 'NONE',  ( 1.171458888995337677, 8.673617379884035472E-16, -111.2928373221764531 ) ) ;
#1243=AXIS2_PLACEMENT_3D ( 'NONE', #11059, #1786, #6270 ) ;
#1248=ORIENTED_EDGE ( 'NONE', *, *, #8460, .F. ) ;
#1251=LINE ( 'NONE', #12932, #7716 ) ;
#1256=EDGE_CURVE ( 'NONE', #6645, #6005, #2991, .T. ) ;
#1257=ADVANCED_FACE ( 'NONE', ( #9040 ), #3159, .F. ) ;
#1260=AXIS2_PLACEMENT_3D ( 'NONE', #2358, #4748, #6133 ) ;
#1262=DIRECTION ( 'NONE',  ( -0.000000000000000000, -1.000000000000000000, -0.000000000000000000 ) ) ;
#1264=CARTESIAN_POINT ( 'NONE',  ( -9.739626904459422363, 10.00000000000000000, -116.2879091882953446 ) ) ;
#1265=CARTESIAN_POINT ( 'NONE',  ( 1.243260443319662123, 4.000000000000000000, -139.4020581015306846 ) ) ;
#1277=CARTESIAN_POINT ( 'NONE',  ( -1.030030362071697070, 15.00000000000000000, -105.0143096063705315 ) ) ;
#1283=CARTESIAN_POINT ( 'NONE',  ( 11.86236191862562706, 1.294159459973254878, -165.2395099304358723 ) ) ;
#1284=CARTESIAN_POINT ( 'NONE',  ( 6.803763450426751014, 15.00000000000000000, -119.3127978128359530 ) ) ;
#1286=DIRECTION ( 'NONE',  ( 0.9997619372588932851, -0.000000000000000000, 0.02181900108494707474 ) ) ;
#1289=DIRECTION ( 'NONE',  ( -0.9997619372588931741, -0.000000000000000000, -0.02181900108494707127 ) ) ;
#1290=EDGE_CURVE ( 'NONE', #13945, #6914, #8284, .T. ) ;
#1293=CARTESIAN_POINT ( 'NONE',  ( 1.086818044140344774, 4.588323854676484181, -139.4449740270702591 ) ) ;
#1296=CARTESIAN_POINT ( 'NONE',  ( 0.000000000000000000, 5.000000000000000888, -100.6237003951525537 ) ) ;
#1298=CARTESIAN_POINT ( 'NONE',  ( 6.918686878921664452, 0.02960220130170718167, -105.2168480447504493 ) ) ;
#1300=CARTESIAN_POINT ( 'NONE',  ( -5.309262520577839872, 13.36526483154179523, -125.0911079416483176 ) ) ;
#1302=ORIENTED_EDGE ( 'NONE', *, *, #11838, .T. ) ;
#1303=CARTESIAN_POINT ( 'NONE',  ( 4.165066839799179021, 0.2629148108822390584, 0.5887562915265751595 ) ) ;
#1305=VECTOR ( 'NONE', #13119, 1000.000000000000000 ) ;
#1316=CARTESIAN_POINT ( 'NONE',  ( -4.234402844927150689, 0.000000000000000000, -117.4888040839639558 ) ) ;
#1318=AXIS2_PLACEMENT_3D ( 'NONE', #5046, #176, #101 ) ;
#1322=( BOUNDED_SURFACE ( )  B_SPLINE_SURFACE ( 3, 2, ( 
 ( #7539, #12256, #8782 ),
 ( #1744, #11320, #9154 ),
 ( #14753, #8850, #13729 ),
 ( #3056, #5522, #12558 ),
 ( #7610, #7768, #10243 ),
 ( #4151, #11474, #3198 ),
 ( #5447, #1824, #12635 ),
 ( #9078, #5305, #4440 ),
 ( #3129, #14975, #13656 ),
 ( #8927, #15046, #10089 ),
 ( #13578, #11248, #12482 ),
 ( #7842, #4222, #1971 ),
 ( #740, #2907, #7690 ),
 ( #6686, #893, #1899 ),
 ( #12325, #6613, #10167 ),
 ( #14901, #13799, #4297 ) ),
 .UNSPECIFIED., .F., .F., .T. ) 
 B_SPLINE_SURFACE_WITH_KNOTS ( ( 4, 2, 2, 2, 2, 2, 2, 4 ),
 ( 3, 3 ),
 ( -1.334638064060296792E-05, 0.001685485362004357284, 0.002534901233326837446, 0.003384317104649317391, 0.004233732975971796902, 0.005083148847294277281, 0.005932564718616757660, 0.006781980589939238038 ),
 ( 0.000000000000000000, 1.000000000000000000 ),
 .UNSPECIFIED. ) 
 GEOMETRIC_REPRESENTATION_ITEM ( )  RATIONAL_B_SPLINE_SURFACE ( (
 ( 1.000000000000000000, 1.000000000000000000, 1.000000000000000000),
 ( 1.000000000000000000, 0.9999849372740239328, 1.000000000000000000),
 ( 1.000000000000000000, 0.9937682810188976923, 1.000000000000000000),
 ( 1.000000000000000000, 0.9761755817002490954, 1.000000000000000000),
 ( 1.000000000000000000, 0.9688601978537569881, 1.000000000000000000),
 ( 1.000000000000000000, 0.9524575494629958783, 1.000000000000000000),
 ( 1.000000000000000000, 0.9433181971012551958, 1.000000000000000000),
 ( 1.000000000000000000, 0.9239129119548288305, 1.000000000000000000),
 ( 1.000000000000000000, 0.9135210720624407088, 1.000000000000000000),
 ( 1.000000000000000000, 0.8936014670381493552, 1.000000000000000000),
 ( 1.000000000000000000, 0.8840084896217472732, 1.000000000000000000),
 ( 1.000000000000000000, 0.8670987394474829468, 1.000000000000000000),
 ( 1.000000000000000000, 0.8600561105956968655, 1.000000000000000000),
 ( 1.000000000000000000, 0.8503557397562589992, 1.000000000000000000),
 ( 1.000000000000000000, 0.8476417977143253513, 1.000000000000000000),
 ( 1.000000000000000000, 0.8476602389432602580, 1.000000000000000000) ) ) 
 REPRESENTATION_ITEM ( '' )  SURFACE ( )  );
#1324=DIRECTION ( 'NONE',  ( -0.02181900108494732801, 0.000000000000000000, 0.9997619372588931741 ) ) ;
#1328=EDGE_LOOP ( 'NONE', ( #1206, #5247, #11489 ) ) ;
#1345=CARTESIAN_POINT ( 'NONE',  ( -6.338840459740750610, 9.999999999966100006, -126.0591383734726350 ) ) ;
#1346=CARTESIAN_POINT ( 'NONE',  ( -2.035316908179384932, 4.336808689942018525E-15, -133.6663417170241246 ) ) ;
#1347=CARTESIAN_POINT ( 'NONE',  ( 24.24946450389425934, 8.673617379884035472E-16, -141.2402007109023145 ) ) ;
#1352=VERTEX_POINT ( 'NONE', #4706 ) ;
#1357=CARTESIAN_POINT ( 'NONE',  ( 6.122889832264990062, 9.999999999999998224, 5.281130614573720905 ) ) ;
#1360=CARTESIAN_POINT ( 'NONE',  ( -24.91286313170930100, 3.952717365971852637, -209.6104391265338904 ) ) ;
#1364=DIRECTION ( 'NONE',  ( 0.000000000000000000, 0.000000000000000000, 1.000000000000000000 ) ) ;
#1365=ORIENTED_EDGE ( 'NONE', *, *, #14365, .T. ) ;
#1369=CARTESIAN_POINT ( 'NONE',  ( 17.56616871422910009, 8.749999999999998224, -94.70022032590149763 ) ) ;
#1372=CARTESIAN_POINT ( 'NONE',  ( 1.004149434879655356, 4.793811891163896277, -139.4756852570866954 ) ) ;
#1376=CARTESIAN_POINT ( 'NONE',  ( 9.135126988672782389, 15.00000000000142819, -105.9368265145316457 ) ) ;
#1379=CARTESIAN_POINT ( 'NONE',  ( -3.490754879379053044, 14.52642831644817711, -125.2917343356935476 ) ) ;
#1381=ORIENTED_EDGE ( 'NONE', *, *, #14526, .F. ) ;
#1382=CARTESIAN_POINT ( 'NONE',  ( 5.779749278148204716, 0.3260126679219001455, 0.3456447915639645485 ) ) ;
#1391=DIRECTION ( 'NONE',  ( 0.9997619372588931741, 0.000000000000000000, 0.02181900108494707474 ) ) ;
#1401=CARTESIAN_POINT ( 'NONE',  ( 5.158994870041119007, 0.1324197759708019839, -0.7446863678409911813 ) ) ;
#1418=CARTESIAN_POINT ( 'NONE',  ( 3.528837229168438228, 8.673617379884037444E-16, -111.3086135701104098 ) ) ;
#1421=CARTESIAN_POINT ( 'NONE',  ( -9.210337242380925105, 15.00000000000325961, -118.3325445941422629 ) ) ;
#1423=CARTESIAN_POINT ( 'NONE',  ( -7.626890066890017472, 7.986110130110988110E-13, -122.9684017742491733 ) ) ;
#1424=CARTESIAN_POINT ( 'NONE',  ( 8.173762862391447115, 8.673617379884035472E-16, -127.0422273781799731 ) ) ;
#1427=CYLINDRICAL_SURFACE ( 'NONE', #1260, 2.500000000000000000 ) ;
#1435=CARTESIAN_POINT ( 'NONE',  ( -22.96679436062313329, 8.673617379884035472E-16, -195.3937102046874941 ) ) ;
#1441=CARTESIAN_POINT ( 'NONE',  ( -24.70666345413006582, 3.149294185761901677, -208.4902367515576032 ) ) ;
#1442=EDGE_LOOP ( 'NONE', ( #2948, #5754, #2966, #10415, #54, #3293 ) ) ;
#1448=DIRECTION ( 'NONE',  ( -0.9997619372588931741, -0.000000000000000000, -0.02181900108494707127 ) ) ;
#1450=DIRECTION ( 'NONE',  ( -0.02181900108494679719, 0.000000000000000000, 0.9997619372588931741 ) ) ;
#1455=CARTESIAN_POINT ( 'NONE',  ( 7.782455147742629364, 1.649526740344270381, 4.504548160689787473 ) ) ;
#1462=CARTESIAN_POINT ( 'NONE',  ( 8.807773658243950976, 15.00000000000000000, -105.8689255569521492 ) ) ;
#1469=CARTESIAN_POINT ( 'NONE',  ( 12.97570930512322285, 3.737837276592360869, -166.4113073631658324 ) ) ;
#1473=CARTESIAN_POINT ( 'NONE',  ( -4.979830621673884572, 8.673617379884032514E-16, -150.2731933682584327 ) ) ;
#1478=ORIENTED_EDGE ( 'NONE', *, *, #11230, .T. ) ;
#1491=EDGE_CURVE ( 'NONE', #8920, #14065, #8555, .T. ) ;
#1494=CARTESIAN_POINT ( 'NONE',  ( 20.87131526946579285, 0.000000000000000000, -138.9752963459259547 ) ) ;
#1498=CARTESIAN_POINT ( 'NONE',  ( -7.159798564871144855, 9.999999999993500310, -124.1957246866965932 ) ) ;
#1500=CARTESIAN_POINT ( 'NONE',  ( -0.2690694657484744012, -4.336808689942017736E-15, -126.9559471811042499 ) ) ;
#1506=ORIENTED_EDGE ( 'NONE', *, *, #10462, .F. ) ;
#1507=CARTESIAN_POINT ( 'NONE',  ( 26.04664898474823431, 2.285168050702167442, -138.3460210313947414 ) ) ;
#1511=ORIENTED_EDGE ( 'NONE', *, *, #8371, .F. ) ;
#1522=CARTESIAN_POINT ( 'NONE',  ( -25.28756687824467164, 0.04309856747023026874, -200.8615385504288042 ) ) ;
#1523=ORIENTED_EDGE ( 'NONE', *, *, #8090, .F. ) ;
#1530=CARTESIAN_POINT ( 'NONE',  ( 6.931531743086595476, 0.03088707369331828573, -105.1762940087775462 ) ) ;
#1532=PRODUCT ( 'PruningShears_Predeterminado', 'PruningShears_Predeterminado', '', ( #4224 ) ) ;
#1535=CARTESIAN_POINT ( 'NONE',  ( 4.054307694666515971, 0.1412400999502742005, -0.4194500301308927148 ) ) ;
#1537=EDGE_CURVE ( 'NONE', #13049, #10207, #3619, .T. ) ;
#1543=B_SPLINE_CURVE_WITH_KNOTS ( 'NONE', 3,
 ( #10943, #12961, #2368, #8537, #5905, #10859 ),
 .UNSPECIFIED., .F., .F.,
 ( 4, 2, 4 ),
 ( 0.000000000000000000, 0.004544361750299368875, 0.009088723500598737751 ),
 .UNSPECIFIED. ) ;
#1544=CARTESIAN_POINT ( 'NONE',  ( 10.96566884988558499, 13.79079921796280850, -106.3305639400367966 ) ) ;
#1554=CARTESIAN_POINT ( 'NONE',  ( 1.167531179896777349, 3.999999999999993783, -139.4941991647475845 ) ) ;
#1556=CARTESIAN_POINT ( 'NONE',  ( -25.62073099797099829, 8.673617379884033500E-16, -189.4007417957344046 ) ) ;
#1561=CARTESIAN_POINT ( 'NONE',  ( 26.15341798802279527, 4.000000000000000000, -138.7600702976168066 ) ) ;
#1562=CARTESIAN_POINT ( 'NONE',  ( -25.04366442233794032, -1.809973046420242971E-12, -207.8080138893894002 ) ) ;
#1567=CARTESIAN_POINT ( 'NONE',  ( -9.192419678266688265, 3.588159064098102480, -115.4428990047103838 ) ) ;
#1574=DIRECTION ( 'NONE',  ( 0.000000000000000000, 1.000000000000000000, 0.000000000000000000 ) ) ;
#1576=CARTESIAN_POINT ( 'NONE',  ( -8.651617673122958152, 5.000000000001580069, -120.1343837246376580 ) ) ;
#1577=CARTESIAN_POINT ( 'NONE',  ( 8.348030713529086100, 5.000000000000000888, -112.8139498890671746 ) ) ;
#1582=DIRECTION ( 'NONE',  ( 0.02181900108494732801, 0.000000000000000000, -0.9997619372588932851 ) ) ;
#1591=EDGE_LOOP ( 'NONE', ( #6786, #11330, #11607, #12722, #9213, #14506 ) ) ;
#1595=CARTESIAN_POINT ( 'NONE',  ( 12.80672841695803577, 14.26859485420106211, -125.9388545821283003 ) ) ;
#1600=EDGE_LOOP ( 'NONE', ( #5553, #7505, #12230, #10621, #169 ) ) ;
#1605=VERTEX_POINT ( 'NONE', #2774 ) ;
#1613=CARTESIAN_POINT ( 'NONE',  ( 9.933893833910557802, 12.49999999999999822, -126.1398084322751885 ) ) ;
#1615=CARTESIAN_POINT ( 'NONE',  ( 26.65632903789428099, 4.223198481467347776, -136.8991823062413857 ) ) ;
#1620=CARTESIAN_POINT ( 'NONE',  ( -0.4873557683217199510, 10.00000000000000000, -103.5659326153046038 ) ) ;
#1621=CYLINDRICAL_SURFACE ( 'NONE', #12187, 5.000000000000000000 ) ;
#1628=CARTESIAN_POINT ( 'NONE',  ( 4.999999999999998224, 1.301042606982605321E-15, -45.97309604003012140 ) ) ;
#1631=CARTESIAN_POINT ( 'NONE',  ( 5.570677809474934072, 7.976916236371252995E-16, -141.9062416701571863 ) ) ;
#1632=CARTESIAN_POINT ( 'NONE',  ( -25.59460798226730915, 8.673617379884035472E-16, -196.2441450656505992 ) ) ;
#1633=EDGE_LOOP ( 'NONE', ( #13335, #9291, #5814, #15267, #5455, #6069 ) ) ;
#1637=CARTESIAN_POINT ( 'NONE',  ( -23.81014751474988245, 4.000000000000494715, -207.0536590050782593 ) ) ;
#1642=CARTESIAN_POINT ( 'NONE',  ( -9.345007083233795697, 4.277268689418242786, -115.3736373665757498 ) ) ;
#1644=EDGE_CURVE ( 'NONE', #8227, #14065, #14, .T. ) ;
#1647=ADVANCED_FACE ( 'NONE', ( #13601 ), #15162, .F. ) ;
#1651=CARTESIAN_POINT ( 'NONE',  ( -9.756303285186648466, 5.000000000000004441, -116.2179163664056176 ) ) ;
#1652=CARTESIAN_POINT ( 'NONE',  ( 8.346107330820501602, 5.000000000000000888, -114.8449120967954116 ) ) ;
#1655=ORIENTED_EDGE ( 'NONE', *, *, #14828, .T. ) ;
#1656=CARTESIAN_POINT ( 'NONE',  ( 10.99340860758278460, 5.943472311793079221, -45.60560901953395785 ) ) ;
#1661=EDGE_LOOP ( 'NONE', ( #5589, #1980, #6842, #9673 ) ) ;
#1664=FACE_OUTER_BOUND ( 'NONE', #3413, .T. ) ;
#1666=CARTESIAN_POINT ( 'NONE',  ( 1.114947364559086829, 5.000000000000000888, -139.4079432275550232 ) ) ;
#1668=EDGE_CURVE ( 'NONE', #8206, #10375, #1993, .T. ) ;
#1670=CARTESIAN_POINT ( 'NONE',  ( -24.82846637880105334, 2.415521945931450976, -207.8856318682263407 ) ) ;
#1671=EDGE_LOOP ( 'NONE', ( #9331, #1047, #5629, #2198, #8005 ) ) ;
#1675=DIRECTION ( 'NONE',  ( -0.02181900108494707127, 0.000000000000000000, 0.9997619372588930631 ) ) ;
#1677=CARTESIAN_POINT ( 'NONE',  ( 11.04730217088350663, 5.000000000000000888, -107.1178495010082941 ) ) ;
#1678=EDGE_CURVE ( 'NONE', #3245, #11140, #14355, .T. ) ;
#1685=DIRECTION ( 'NONE',  ( 0.000000000000000000, 0.000000000000000000, 1.000000000000000000 ) ) ;
#1696=CARTESIAN_POINT ( 'NONE',  ( -5.836146573691881834, 0.2317559567678120491, -116.8702851668251128 ) ) ;
#1700=CARTESIAN_POINT ( 'NONE',  ( 11.76219408996538895, 1.269473348720391082, -165.4091314653759639 ) ) ;
#1701=CARTESIAN_POINT ( 'NONE',  ( 6.288457687488933523, 0.000000000000000000, -105.0111312234435985 ) ) ;
#1702=CARTESIAN_POINT ( 'NONE',  ( -22.26570164085059389, 8.673617379884035472E-16, -175.9421475886515509 ) ) ;
#1705=CARTESIAN_POINT ( 'NONE',  ( 8.125871712912910994, 2.250174624375246513, 2.357012527964847948 ) ) ;
#1712=CARTESIAN_POINT ( 'NONE',  ( 26.88777289245747326, 5.000000000000000888, -138.4814624290440577 ) ) ;
#1713=CARTESIAN_POINT ( 'NONE',  ( -8.888107754931237281, 2.324435220146938708, -116.5586263778049982 ) ) ;
#1722=LINE ( 'NONE', #7673, #7012 ) ;
#1723=CARTESIAN_POINT ( 'NONE',  ( 8.481465556250880056, -2.145889335582468041E-13, -115.9036014638424632 ) ) ;
#1726=DIRECTION ( 'NONE',  ( 0.000000000000000000, 1.000000000000000000, 0.000000000000000000 ) ) ;
#1743=CARTESIAN_POINT ( 'NONE',  ( 4.132056102115797991, 0.2279355446411715780, 0.3862057507398425349 ) ) ;
#1744=CARTESIAN_POINT ( 'NONE',  ( -4.907357056059624689, 15.00000000000000000, -117.3740583286203076 ) ) ;
#1751=VECTOR ( 'NONE', #780, 1000.000000000000114 ) ;
#1753=ORIENTED_EDGE ( 'NONE', *, *, #13116, .F. ) ;
#1758=CARTESIAN_POINT ( 'NONE',  ( 8.895558325401111688, 15.00000000000000000, -141.4560052469132643 ) ) ;
#1762=DIRECTION ( 'NONE',  ( 0.000000000000000000, 1.000000000000000000, 0.000000000000000000 ) ) ;
#1771=EDGE_CURVE ( 'NONE', #4454, #8744, #5444, .T. ) ;
#1783=CARTESIAN_POINT ( 'NONE',  ( 11.20997547022881058, 0.7546953127386059057, -164.9537947295017943 ) ) ;
#1785=CARTESIAN_POINT ( 'NONE',  ( -26.07384356158112126, 3.269528285336324855E-12, -174.4700131545309603 ) ) ;
#1786=DIRECTION ( 'NONE',  ( -0.000000000000000000, -1.000000000000000000, -0.000000000000000000 ) ) ;
#1791=CARTESIAN_POINT ( 'NONE',  ( 10.79258363242540497, 2.747348697280918461, -106.2503091257652699 ) ) ;
#1794=CARTESIAN_POINT ( 'NONE',  ( 26.13050938914192756, 6.000000000000000000, -138.2605953772281566 ) ) ;
#1797=CARTESIAN_POINT ( 'NONE',  ( -9.131312970616235702, 2.485997537948267944, -116.0049100415185137 ) ) ;
#1801=AXIS2_PLACEMENT_3D ( 'NONE', #14947, #9050, #13999 ) ;
#1812=CARTESIAN_POINT ( 'NONE',  ( 10.01029310660177529, 5.834492850526031837, -45.31678212580880682 ) ) ;
#1820=B_SPLINE_CURVE_WITH_KNOTS ( 'NONE', 3,
 ( #14626, #13609, #13380, #8804 ),
 .UNSPECIFIED., .F., .F.,
 ( 4, 4 ),
 ( 7.151554039766124246E-07, 0.0004291502618545642322 ),
 .UNSPECIFIED. ) ;
#1822=CARTESIAN_POINT ( 'NONE',  ( 11.89832029942966152, 14.70551497719767475, -125.7371425972743424 ) ) ;
#1823=DIRECTION ( 'NONE',  ( 0.000000000000000000, -0.000000000000000000, 1.000000000000000000 ) ) ;
#1824=CARTESIAN_POINT ( 'NONE',  ( -7.653276971141075080, 13.99920316164806344, -116.4876868865759150 ) ) ;
#1827=CIRCLE ( 'NONE', #8721, 3.000000000000011990 ) ;
#1828=CARTESIAN_POINT ( 'NONE',  ( 13.66360635575861515, 15.00000000000000000, -125.8738101257675766 ) ) ;
#1832=CARTESIAN_POINT ( 'NONE',  ( -28.89672605278645889, 4.000000000000001776, -180.4390744492250747 ) ) ;
#1835=CARTESIAN_POINT ( 'NONE',  ( -9.203922670347713719, 11.37012112914805506, -115.4376859600374559 ) ) ;
#1837=AXIS2_PLACEMENT_3D ( 'NONE', #5416, #5343, #865 ) ;
#1844=EDGE_CURVE ( 'NONE', #12142, #2185, #3221, .T. ) ;
#1847=DIRECTION ( 'NONE',  ( 0.000000000000000000, 0.000000000000000000, 1.000000000000000000 ) ) ;
#1848=ORIENTED_EDGE ( 'NONE', *, *, #2219, .T. ) ;
#1849=CARTESIAN_POINT ( 'NONE',  ( 5.228075279701640099, 4.000000000000000000, -165.7939279834373849 ) ) ;
#1854=CARTESIAN_POINT ( 'NONE',  ( 11.32911567345497872, 12.86975428404477029, -106.8195553291829185 ) ) ;
#1858=CARTESIAN_POINT ( 'NONE',  ( 10.95703869986693491, 5.830414896929611679, -43.93911433197450833 ) ) ;
#1859=CARTESIAN_POINT ( 'NONE',  ( -4.924212822021339697, 0.02956586206423728741, -117.3690025739556262 ) ) ;
#1867=CARTESIAN_POINT ( 'NONE',  ( -29.36516290028746212, -2.190758066230379322E-12, -186.4185780521328581 ) ) ;
#1871=EDGE_LOOP ( 'NONE', ( #286, #1033, #7734, #5875 ) ) ;
#1873=CARTESIAN_POINT ( 'NONE',  ( 11.32016196459919755, 4.662706325538023222, -106.4092894470422408 ) ) ;
#1874=FACE_OUTER_BOUND ( 'NONE', #12453, .T. ) ;
#1876=LINE ( 'NONE', #7457, #4298 ) ;
#1878=CARTESIAN_POINT ( 'NONE',  ( 20.15233411323433188, 8.673617379884035472E-16, -140.2512511322913440 ) ) ;
#1883=ADVANCED_FACE ( 'NONE', ( #4617 ), #9097, .T. ) ;
#1888=CARTESIAN_POINT ( 'NONE',  ( 10.94790802041947941, 11.56847231179307656, -43.52074019388548010 ) ) ;
#1890=CARTESIAN_POINT ( 'NONE',  ( -0.2962205294200088712, 15.00000000000000000, -113.2751335308100096 ) ) ;
#1896=CARTESIAN_POINT ( 'NONE',  ( 9.950460554352121179, 12.63099284567753777, -43.64860988872874259 ) ) ;
#1898=CARTESIAN_POINT ( 'NONE',  ( -16.51872302133460124, 15.00000000000000000, -108.9020125831789727 ) ) ;
#1899=CARTESIAN_POINT ( 'NONE',  ( -9.345007083234262879, 10.72273131058215867, -115.3736373665762471 ) ) ;
#1901=CARTESIAN_POINT ( 'NONE',  ( 5.807692710371052947, 15.00000000000000000, -113.5160805275953209 ) ) ;
#1902=CARTESIAN_POINT ( 'NONE',  ( 9.044950117654433797, 0.000000000000000000, -141.4826476090360643 ) ) ;
#1903=CARTESIAN_POINT ( 'NONE',  ( 27.51230737804261395, 5.000000000000002665, -137.3927180530722580 ) ) ;
#1906=CARTESIAN_POINT ( 'NONE',  ( -27.72689154219598962, 3.999999999999999112, -176.3502337898269445 ) ) ;
#1922=CARTESIAN_POINT ( 'NONE',  ( 7.000000000000000888, 15.00000000000000000, -1.663700395152567513 ) ) ;
#1927=CARTESIAN_POINT ( 'NONE',  ( -6.738069272572023038, 0.6073807294375053178, -116.5044176451308999 ) ) ;
#1934=VERTEX_POINT ( 'NONE', #3447 ) ;
#1935=CARTESIAN_POINT ( 'NONE',  ( -20.78833667511313976, 3.151119262966928298E-15, -163.5248793559493379 ) ) ;
#1936=CARTESIAN_POINT ( 'NONE',  ( 12.40744575253754611, 2.644372666245800918, -166.2747719090159819 ) ) ;
#1939=ORIENTED_EDGE ( 'NONE', *, *, #2781, .F. ) ;
#1941=DIRECTION ( 'NONE',  ( -0.000000000000000000, -1.000000000000000000, -0.000000000000000000 ) ) ;
#1942=CARTESIAN_POINT ( 'NONE',  ( -4.781971238371357735, 9.999999999999998224, -110.8602639898391402 ) ) ;
#1944=CARTESIAN_POINT ( 'NONE',  ( 2.299001413601184485, 8.673617379884035472E-16, -109.5170782816581010 ) ) ;
#1946=CARTESIAN_POINT ( 'NONE',  ( 21.45872126895855558, 8.673617379884035472E-16, -137.8933061875234216 ) ) ;
#1957=DIRECTION ( 'NONE',  ( 0.000000000000000000, 0.000000000000000000, 1.000000000000000000 ) ) ;
#1958=CARTESIAN_POINT ( 'NONE',  ( -20.89020113344621166, 4.000000000000000888, -201.4223823251848842 ) ) ;
#1963=EDGE_CURVE ( 'NONE', #1934, #5913, #13212, .T. ) ;
#1965=ADVANCED_FACE ( 'NONE', ( #7938 ), #12566, .T. ) ;
#1966=ADVANCED_FACE ( 'NONE', ( #4413 ), #10, .T. ) ;
#1970=PLANE ( 'NONE',  #4007 ) ;
#1971=CARTESIAN_POINT ( 'NONE',  ( -9.079473912025640914, 11.74640706415874902, -115.4940425210668593 ) ) ;
#1972=CIRCLE ( 'NONE', #14579, 4.000000000000002665 ) ;
#1973=CARTESIAN_POINT ( 'NONE',  ( 6.794935331052586847, 15.00000000000000000, -119.3072837454165978 ) ) ;
#1975=CARTESIAN_POINT ( 'NONE',  ( 24.39879083497066148, 1.007048232812085553, -137.7273893344313933 ) ) ;
#1978=CARTESIAN_POINT ( 'NONE',  ( -30.67393154469030847, 4.000000000000000000, -191.3981176163640328 ) ) ;
#1980=ORIENTED_EDGE ( 'NONE', *, *, #4223, .T. ) ;
#1982=CARTESIAN_POINT ( 'NONE',  ( 5.000000000000000000, 9.999999999999998224, -100.6237003951525679 ) ) ;
#1986=CARTESIAN_POINT ( 'NONE',  ( -25.36802828785869579, 1.152219026994713014, -206.4234313139986909 ) ) ;
#1990=CARTESIAN_POINT ( 'NONE',  ( 8.479240049521797218, 5.000000000000000000, -112.0221658571874741 ) ) ;
#1991=AXIS2_PLACEMENT_3D ( 'NONE', #7091, #1391, #5795 ) ;
#1993=CIRCLE ( 'NONE', #7913, 6.000000000000005329 ) ;
#1996=CARTESIAN_POINT ( 'NONE',  ( -9.385448347264267355, 9.999999999999998224, -115.3551636530117150 ) ) ;
#2000=( BOUNDED_SURFACE ( )  B_SPLINE_SURFACE ( 3, 2, ( 
 ( #4769, #5846, #13123 ),
 ( #11947, #11794, #1293 ),
 ( #9484, #2533, #15301 ),
 ( #7234, #1372, #2838 ) ),
 .UNSPECIFIED., .F., .F., .F. ) 
 B_SPLINE_SURFACE_WITH_KNOTS ( ( 4, 4 ),
 ( 3, 3 ),
 ( 0.09990852050945690788, 0.1000240204753783668 ),
 ( 0.000000000000000000, 0.05733937959224865571 ),
 .UNSPECIFIED. ) 
 GEOMETRIC_REPRESENTATION_ITEM ( )  RATIONAL_B_SPLINE_SURFACE ( (
 ( 1.000000000000000000, 0.9832056845464598460, 0.9683373203504848092),
 ( 1.000000000000000000, 0.9832056845464598460, 0.9683373203504848092),
 ( 1.000000000000000000, 0.9832056845464598460, 0.9683373203504848092),
 ( 1.000000000000000000, 0.9832056845464598460, 0.9683373203504848092) ) ) 
 REPRESENTATION_ITEM ( '' )  SURFACE ( )  );
#2001=AXIS2_PLACEMENT_3D ( 'NONE', #10565, #13041, #2451 ) ;
#2010=( BOUNDED_SURFACE ( )  B_SPLINE_SURFACE ( 3, 2, ( 
 ( #4359, #7679, #6599 ),
 ( #6672, #9067, #11238 ),
 ( #12313, #10005, #2897 ),
 ( #729, #657, #3045 ),
 ( #580, #1812, #8768 ),
 ( #1656, #5362, #500 ) ),
 .UNSPECIFIED., .F., .F., .F. ) 
 B_SPLINE_SURFACE_WITH_KNOTS ( ( 4, 2, 4 ),
 ( 3, 3 ),
 ( 0.000000000000000000, 0.001345013985307758498, 0.002690027970615516996 ),
 ( 0.000000000000000000, 1.000000000000000000 ),
 .UNSPECIFIED. ) 
 GEOMETRIC_REPRESENTATION_ITEM ( )  RATIONAL_B_SPLINE_SURFACE ( (
 ( 1.000000000000000000, 0.7071067811865477948, 1.000000000000000000),
 ( 1.000000000000000000, 0.7155213219688852933, 1.000000000000000000),
 ( 1.000000000000000000, 0.7203076836420526652, 1.000000000000000000),
 ( 1.000000000000000000, 0.7203068556383743770, 1.000000000000000000),
 ( 1.000000000000000000, 0.7155213468501946394, 1.000000000000000000),
 ( 1.000000000000000000, 0.7071067811865475727, 1.000000000000000000) ) ) 
 REPRESENTATION_ITEM ( '' )  SURFACE ( )  );
#2011=CARTESIAN_POINT ( 'NONE',  ( 9.044950117654433797, 6.000000000000000000, -141.4826476090360643 ) ) ;
#2012=AXIS2_PLACEMENT_3D ( 'NONE', #5865, #15179, #3481 ) ;
#2014=CARTESIAN_POINT ( 'NONE',  ( -29.80312056968273993, -8.173210768771287891E-13, -194.9698201312028232 ) ) ;
#2015=CARTESIAN_POINT ( 'NONE',  ( 12.05350762744194171, 1.921718543347064934, -165.9463472480123016 ) ) ;
#2019=CARTESIAN_POINT ( 'NONE',  ( -8.749806588114527273, 10.00000000000000000, -116.1271478199639944 ) ) ;
#2022=CARTESIAN_POINT ( 'NONE',  ( 8.990769910733003911, 12.49999999999999822, 0.3250886916252367920 ) ) ;
#2023=CARTESIAN_POINT ( 'NONE',  ( -9.476787056091271921, 5.000000000000000888, -115.4301398046334981 ) ) ;
#2025=CARTESIAN_POINT ( 'NONE',  ( 16.56640677697020436, 8.749999999999998224, -94.72203932698644735 ) ) ;
#2028=CARTESIAN_POINT ( 'NONE',  ( -6.624869655310543060, 11.24276207080473888, -124.9757423372164595 ) ) ;
#2030=CARTESIAN_POINT ( 'NONE',  ( 22.59313949056596726, 0.2140682042508952609, -138.3733707844687331 ) ) ;
#2037=ORIENTED_EDGE ( 'NONE', *, *, #13851, .F. ) ;
#2039=CARTESIAN_POINT ( 'NONE',  ( 3.872594309009198987, 15.00000000000000000, -106.2339216993545676 ) ) ;
#2050=CARTESIAN_POINT ( 'NONE',  ( 8.541738004602031253, 15.00000000000000178, -116.2437985782397476 ) ) ;
#2051=CARTESIAN_POINT ( 'NONE',  ( 5.228075279701640099, 1.000000000000000000, -165.7939279834373849 ) ) ;
#2055=CARTESIAN_POINT ( 'NONE',  ( 1.279752910752960382, 4.059554565823606076, -139.4003843612397020 ) ) ;
#2059=CARTESIAN_POINT ( 'NONE',  ( -11.98604617743635181, 4.000000000000000000, -150.3522495476669292 ) ) ;
#2068=CARTESIAN_POINT ( 'NONE',  ( -25.53589191382039658, 2.627299923236849910, -208.1764131119443846 ) ) ;
#2071=CYLINDRICAL_SURFACE ( 'NONE', #4074, 0.5000000000000004441 ) ;
#2072=ADVANCED_FACE ( 'NONE', ( #3786 ), #12860, .T. ) ;
#2083=VECTOR ( 'NONE', #10768, 999.9999999999998863 ) ;
#2084=CARTESIAN_POINT ( 'NONE',  ( 11.23659815053166611, 13.16053590981122312, -106.3906584630388039 ) ) ;
#2088=CARTESIAN_POINT ( 'NONE',  ( -27.57977843586095190, -1.786917643684941595E-12, -204.3315731964443387 ) ) ;
#2098=CARTESIAN_POINT ( 'NONE',  ( 8.941075674752649860, 14.66517635709258194, 2.602113448209936841 ) ) ;
#2099=CARTESIAN_POINT ( 'NONE',  ( 2.958795351719239797, 8.673617379884035472E-16, -108.2770199283325780 ) ) ;
#2108=CARTESIAN_POINT ( 'NONE',  ( 11.00225911879145002, 8.749999999999998224, -91.84275802117696230 ) ) ;
#2111=CARTESIAN_POINT ( 'NONE',  ( -3.545188519422978413, 5.000000000000000000, -132.7285785787237558 ) ) ;
#2114=CARTESIAN_POINT ( 'NONE',  ( 8.554370898791335165, 8.673617379884035472E-16, -168.5027005598435039 ) ) ;
#2117=CARTESIAN_POINT ( 'NONE',  ( 13.13192191588670887, 4.000000000000000000, -166.1703390355876877 ) ) ;
#2118=ORIENTED_EDGE ( 'NONE', *, *, #13876, .T. ) ;
#2122=CARTESIAN_POINT ( 'NONE',  ( -0.1117941955214328681, 5.000000000000000888, -102.1231258608400907 ) ) ;
#2124=( NAMED_UNIT ( * ) SI_UNIT ( $, .STERADIAN. ) SOLID_ANGLE_UNIT ( ) );
#2127=CARTESIAN_POINT ( 'NONE',  ( 8.459890227649916383, 12.49999999999999822, -115.7934283673321261 ) ) ;
#2128=CARTESIAN_POINT ( 'NONE',  ( -8.506498296742877940, 13.16062949075057809, -116.6455419169648593 ) ) ;
#2130=CARTESIAN_POINT ( 'NONE',  ( 26.20154845188031700, 2.488669359958907812, -138.3263134144609410 ) ) ;
#2132=EDGE_LOOP ( 'NONE', ( #13908, #15093, #3361 ) ) ;
#2133=VERTEX_POINT ( 'NONE', #5110 ) ;
#2135=CARTESIAN_POINT ( 'NONE',  ( 1.004809442601927394, 5.000000000000000888, -139.4752805618705622 ) ) ;
#2140=MANIFOLD_SOLID_BREP ( 'Redondeo5', #8564 ) ;
#2144=ADVANCED_FACE ( 'NONE', ( #8502 ), #13393, .F. ) ;
#2145=CARTESIAN_POINT ( 'NONE',  ( -25.48033468270072532, 3.216921005771350206, -208.6603374304535805 ) ) ;
#2148=CARTESIAN_POINT ( 'NONE',  ( 21.53395630484880385, 5.000000000000001776, -133.2577068754237644 ) ) ;
#2149=DIRECTION ( 'NONE',  ( 0.02181900108494663065, 0.000000000000000000, -0.9997619372588932851 ) ) ;
#2153=LINE ( 'NONE', #15073, #6492 ) ;
#2154=EDGE_CURVE ( 'NONE', #3281, #13049, #7652, .T. ) ;
#2165=ORIENTED_EDGE ( 'NONE', *, *, #13598, .T. ) ;
#2166=CARTESIAN_POINT ( 'NONE',  ( -25.22286604074212235, 8.673617379884035472E-16, -198.5635032934493154 ) ) ;
#2172=CARTESIAN_POINT ( 'NONE',  ( 8.941148554184975339, 11.11253373586288440, 2.598774061488354103 ) ) ;
#2173=CARTESIAN_POINT ( 'NONE',  ( -0.3214635615751804121, 1.215333660157913752E-12, -103.0394908280570405 ) ) ;
#2175=CARTESIAN_POINT ( 'NONE',  ( 2.469015410240005259, 8.673617379884035472E-16, -109.2094522964932963 ) ) ;
#2178=FACE_OUTER_BOUND ( 'NONE', #9307, .T. ) ;
#2179=CARTESIAN_POINT ( 'NONE',  ( 26.66216796319303484, 4.264883946051542196, -136.8970070307220794 ) ) ;
#2185=VERTEX_POINT ( 'NONE', #7418 ) ;
#2186=CARTESIAN_POINT ( 'NONE',  ( 8.305508344667165588, 12.50000000000000000, -114.1336091688761343 ) ) ;
#2190=ORIENTED_EDGE ( 'NONE', *, *, #14746, .T. ) ;
#2194=EDGE_CURVE ( 'NONE', #9763, #4330, #4228, .T. ) ;
#2198=ORIENTED_EDGE ( 'NONE', *, *, #8627, .F. ) ;
#2207=VERTEX_POINT ( 'NONE', #3953 ) ;
#2208=CARTESIAN_POINT ( 'NONE',  ( -0.5126277339387972365, 9.999999999999998224, -103.6859198938611399 ) ) ;
#2211=CARTESIAN_POINT ( 'NONE',  ( -25.31370737356648348, 0.4053893758470029085, -203.6075974930378152 ) ) ;
#2219=EDGE_CURVE ( 'NONE', #5143, #8206, #255, .T. ) ;
#2222=CARTESIAN_POINT ( 'NONE',  ( 10.16835622167071840, 14.49892404887047981, -106.6099690722883082 ) ) ;
#2236=EDGE_CURVE ( 'NONE', #12980, #11984, #236, .T. ) ;
#2237=CARTESIAN_POINT ( 'NONE',  ( -28.17198374595783861, 3.576437372583847189E-12, -202.9920081940992986 ) ) ;
#2245=CARTESIAN_POINT ( 'NONE',  ( 1.114947364559086829, 15.00000000000000000, -139.4079432275550232 ) ) ;
#2247=CARTESIAN_POINT ( 'NONE',  ( -25.50370618284765456, 2.956430103652706531, -208.4658715182746391 ) ) ;
#2248=CARTESIAN_POINT ( 'NONE',  ( -4.037064903932549242, 8.673617379884035472E-16, -173.3783848444354021 ) ) ;
#2250=CARTESIAN_POINT ( 'NONE',  ( 0.000000000000000000, 5.000000000000000888, -100.6237003951525537 ) ) ;
#2252=CARTESIAN_POINT ( 'NONE',  ( 10.58692965144313014, 0.000000000000000000, -159.5308220099450409 ) ) ;
#2257=DIRECTION ( 'NONE',  ( 0.000000000000000000, 1.000000000000000000, 0.000000000000000000 ) ) ;
#2258=CARTESIAN_POINT ( 'NONE',  ( 23.25775510017668424, 0.4289495323832013263, -138.1373351626023975 ) ) ;
#2263=FACE_OUTER_BOUND ( 'NONE', #5972, .T. ) ;
#2265=ORIENTED_EDGE ( 'NONE', *, *, #11673, .F. ) ;
#2266=CARTESIAN_POINT ( 'NONE',  ( -9.846744731551831720, 4.000000000000000888, -186.2620189933751647 ) ) ;
#2270=ORIENTED_EDGE ( 'NONE', *, *, #2909, .F. ) ;
#2278=CARTESIAN_POINT ( 'NONE',  ( 9.335939850627564596, 15.00000000000000000, -105.2901324735335891 ) ) ;
#2279=CARTESIAN_POINT ( 'NONE',  ( 13.25562203902501146, 5.000000000000000888, -125.4200107876433918 ) ) ;
#2280=ORIENTED_EDGE ( 'NONE', *, *, #5172, .F. ) ;
#2286=CARTESIAN_POINT ( 'NONE',  ( -29.74068399868164647, 4.000000000000000888, -200.7425342145079412 ) ) ;
#2291=CARTESIAN_POINT ( 'NONE',  ( 0.7716514365830442479, 14.99999999999999822, -111.8714012163870564 ) ) ;
#2294=CARTESIAN_POINT ( 'NONE',  ( -25.46814831223248277, 0.6176455659345582161, -204.7850756988478338 ) ) ;
#2295=CARTESIAN_POINT ( 'NONE',  ( 2.399330854043891126, -6.071532165918825619E-15, -131.2813267747279440 ) ) ;
#2303=AXIS2_PLACEMENT_3D ( 'NONE', #1982, #9169, #10322 ) ;
#2304=EDGE_CURVE ( 'NONE', #7276, #5674, #7459, .T. ) ;
#2315=DIRECTION ( 'NONE',  ( 0.9997619372588932851, -0.000000000000000000, 0.02181900108494707474 ) ) ;
#2316=CIRCLE ( 'NONE', #2824, 3.000000000000005329 ) ;
#2317=EDGE_LOOP ( 'NONE', ( #11165, #10698, #4534, #2746 ) ) ;
#2318=CARTESIAN_POINT ( 'NONE',  ( 8.915781819284724463, 4.487270727378674273, 2.843881670126054306 ) ) ;
#2325=CARTESIAN_POINT ( 'NONE',  ( -25.16238623267244989, 0.0006965968045201811161, -199.2040625880622997 ) ) ;
#2326=CARTESIAN_POINT ( 'NONE',  ( 8.915609759151768898, 13.95926557866610018, 3.768979567163230460 ) ) ;
#2331=CARTESIAN_POINT ( 'NONE',  ( 3.558820106718695975, 8.673617379884034486E-16, -107.0002797207564100 ) ) ;
#2342=ORIENTED_EDGE ( 'NONE', *, *, #12922, .T. ) ;
#2343=DIRECTION ( 'NONE',  ( 0.02181900108494707127, 0.000000000000000000, -0.9997619372588931741 ) ) ;
#2347=ORIENTED_EDGE ( 'NONE', *, *, #6925, .F. ) ;
#2351=CARTESIAN_POINT ( 'NONE',  ( 7.439269063064413601, 8.673617379884033500E-16, -125.9756671148725360 ) ) ;
#2354=FACE_OUTER_BOUND ( 'NONE', #9758, .T. ) ;
#2355=CARTESIAN_POINT ( 'NONE',  ( 8.895820146784114257, 5.000000000000000888, -117.6809082909101960 ) ) ;
#2356=ORIENTED_EDGE ( 'NONE', *, *, #10729, .F. ) ;
#2358=CARTESIAN_POINT ( 'NONE',  ( 6.436143463598922310, 15.00000000000000000, 2.800833825385760090 ) ) ;
#2359=EDGE_LOOP ( 'NONE', ( #2645, #13183, #3473, #5234, #9733, #15217, #4209, #1188, #4900 ) ) ;
#2365=CARTESIAN_POINT ( 'NONE',  ( -2.027137927901855097, 9.999999999999998224, -107.0032022124461122 ) ) ;
#2368=CARTESIAN_POINT ( 'NONE',  ( -8.933522129290233593, 9.999999999999998224, -119.2934400955039251 ) ) ;
#2378=CYLINDRICAL_SURFACE ( 'NONE', #782, 3.000000000000005329 ) ;
#2380=CARTESIAN_POINT ( 'NONE',  ( 9.246414981748314332, 0.9484790359934494042, -106.0253644157543249 ) ) ;
#2385=ORIENTED_EDGE ( 'NONE', *, *, #8923, .T. ) ;
#2386=CARTESIAN_POINT ( 'NONE',  ( -26.89045353704901942, -1.363139722109709093E-13, -205.6554657723100945 ) ) ;
#2394=CARTESIAN_POINT ( 'NONE',  ( 9.442321227527154193, 14.94013921602285855, -106.0014341817649495 ) ) ;
#2411=CARTESIAN_POINT ( 'NONE',  ( 8.305142154013848810, 12.50000000000000000, -113.6818879023987137 ) ) ;
#2417=CARTESIAN_POINT ( 'NONE',  ( -7.128555860240339825, 5.000000000000001776, -113.3867792963409471 ) ) ;
#2418=CARTESIAN_POINT ( 'NONE',  ( 1.004809442601927394, 6.000000000000000000, -139.4752805618705622 ) ) ;
#2423=DIRECTION ( 'NONE',  ( 0.000000000000000000, -1.000000000000000000, 0.000000000000000000 ) ) ;
#2426=FACE_OUTER_BOUND ( 'NONE', #14314, .T. ) ;
#2428=ORIENTED_EDGE ( 'NONE', *, *, #12357, .F. ) ;
#2431=CARTESIAN_POINT ( 'NONE',  ( -27.89696216417192787, 4.000000000000000888, -205.5469850651400918 ) ) ;
#2439=PRODUCT_DEFINITION ( 'UNKNOWN', '', #10116, #12530 ) ;
#2441=CARTESIAN_POINT ( 'NONE',  ( 10.89963103874143791, 0.4779808835687370805, -164.5338399313753257 ) ) ;
#2442=VECTOR ( 'NONE', #5189, 1000.000000000000000 ) ;
#2443=CARTESIAN_POINT ( 'NONE',  ( 10.22352057816269699, 15.00000000000000000, -125.5112093480189657 ) ) ;
#2449=CARTESIAN_POINT ( 'NONE',  ( 8.673617379884035472E-16, 15.00000000000000000, -1.663700395152567513 ) ) ;
#2451=DIRECTION ( 'NONE',  ( 0.000000000000000000, 0.000000000000000000, 1.000000000000000000 ) ) ;
#2453=CARTESIAN_POINT ( 'NONE',  ( -9.242581453897864563, 4.999999999999996447, -118.3503833458025127 ) ) ;
#2455=CARTESIAN_POINT ( 'NONE',  ( 7.799741786693411782, 0.2423173772441938045, -105.6274327777687745 ) ) ;
#2461=ORIENTED_EDGE ( 'NONE', *, *, #7434, .F. ) ;
#2462=CARTESIAN_POINT ( 'NONE',  ( 4.354212728048433512, 0.4612449236405465336, 1.472775563304803415 ) ) ;
#2476=CARTESIAN_POINT ( 'NONE',  ( 17.33677725112149304, 2.336213234116637878E-12, -156.7678757840980097 ) ) ;
#2482=CARTESIAN_POINT ( 'NONE',  ( -5.137055953098589534, 8.673617379884034486E-16, -145.0199091983525648 ) ) ;
#2485=CARTESIAN_POINT ( 'NONE',  ( 13.13192191588670887, 4.000000000000000000, -166.1703390355876877 ) ) ;
#2496=CARTESIAN_POINT ( 'NONE',  ( -6.385995564645482681, 0.4374612817417152244, -116.6487767744768291 ) ) ;
#2501=CARTESIAN_POINT ( 'NONE',  ( 10.57895993728494410, 8.673617379884033500E-16, -129.9860179236332840 ) ) ;
#2507=CARTESIAN_POINT ( 'NONE',  ( 20.93263444590049005, 5.000000000000000888, -132.7914611339006683 ) ) ;
#2514=LINE ( 'NONE', #15213, #844 ) ;
#2518=VERTEX_POINT ( 'NONE', #4827 ) ;
#2519=CARTESIAN_POINT ( 'NONE',  ( 6.445944033997953682, 15.00000000000000355, 0.5979964941558831848 ) ) ;
#2527=CARTESIAN_POINT ( 'NONE',  ( 30.96695154071790412, 8.773889247172311556, -44.17511166891541308 ) ) ;
#2530=DIRECTION ( 'NONE',  ( -0.000000000000000000, -1.000000000000000000, -0.000000000000000000 ) ) ;
#2532=AXIS2_PLACEMENT_3D ( 'NONE', #560, #9981, #14720 ) ;
#2533=CARTESIAN_POINT ( 'NONE',  ( 1.041036260628390275, 4.793811891163896277, -139.4530670678220474 ) ) ;
#2535=CARTESIAN_POINT ( 'NONE',  ( -3.486117781607304345, 5.000000000000000000, -110.4977313129625145 ) ) ;
#2537=CARTESIAN_POINT ( 'NONE',  ( 8.370726826406757581, 0.4830037559535477754, -105.8718434674591578 ) ) ;
#2542=ORIENTED_EDGE ( 'NONE', *, *, #9382, .F. ) ;
#2543=CARTESIAN_POINT ( 'NONE',  ( 6.189785629711340498, 0.5131405437846897621, 0.8071071970720852251 ) ) ;
#2545=CIRCLE ( 'NONE', #3282, 3.500000000000003109 ) ;
#2561=DIRECTION ( 'NONE',  ( 0.000000000000000000, 0.000000000000000000, 1.000000000000000000 ) ) ;
#2563=CARTESIAN_POINT ( 'NONE',  ( -4.512114784912129473, 6.000000000000000000, -130.1824886095253646 ) ) ;
#2565=CARTESIAN_POINT ( 'NONE',  ( 3.717577911061880958, 0.000000000000000000, -143.6771719914432879 ) ) ;
#2573=VECTOR ( 'NONE', #15019, 1000.000000000000000 ) ;
#2580=CARTESIAN_POINT ( 'NONE',  ( 4.634195662811253946, 8.673617379884033500E-16, -120.6336223843100868 ) ) ;
#2582=VECTOR ( 'NONE', #2680, 1000.000000000000000 ) ;
#2583=CARTESIAN_POINT ( 'NONE',  ( 1.320501113854922082, 4.999999999999995559, -137.8664870916820178 ) ) ;
#2584=FACE_OUTER_BOUND ( 'NONE', #478, .T. ) ;
#2589=VERTEX_POINT ( 'NONE', #10772 ) ;
#2594=VERTEX_POINT ( 'NONE', #9539 ) ;
#2603=CARTESIAN_POINT ( 'NONE',  ( -25.21953614097411034, 0.8110625423123717370, -205.0088040713835369 ) ) ;
#2604=ORIENTED_EDGE ( 'NONE', *, *, #12449, .T. ) ;
#2608=ADVANCED_FACE ( 'NONE', ( #12951 ), #1427, .T. ) ;
#2611=CARTESIAN_POINT ( 'NONE',  ( 13.78275167297412906, 13.34157715675068623, -126.2206732457524794 ) ) ;
#2613=CARTESIAN_POINT ( 'NONE',  ( 11.04510349467952146, 3.336188342164840392, -106.3259430280883322 ) ) ;
#2618=CARTESIAN_POINT ( 'NONE',  ( 8.555302993508680842, 3.062150894005132962, 2.628411868347194869 ) ) ;
#2626=CARTESIAN_POINT ( 'NONE',  ( 26.71007981443199952, 6.000000000000000000, -136.8791680534710054 ) ) ;
#2628=CARTESIAN_POINT ( 'NONE',  ( 8.990769910733003911, 15.00000000000000000, 0.3250886916252364589 ) ) ;
#2635=CARTESIAN_POINT ( 'NONE',  ( 11.39998925557648413, 0.9113012638559210288, -165.1104261359550662 ) ) ;
#2637=CARTESIAN_POINT ( 'NONE',  ( -5.917161057971962457, 8.673617379884035472E-16, -151.2264619204686937 ) ) ;
#2638=DIRECTION ( 'NONE',  ( -0.04581719776170027625, 0.000000000000000000, 0.9989498407774363153 ) ) ;
#2639=CARTESIAN_POINT ( 'NONE',  ( -23.03755312564397073, 8.673617379884035472E-16, -178.0552937557089592 ) ) ;
#2645=ORIENTED_EDGE ( 'NONE', *, *, #7438, .T. ) ;
#2652=CARTESIAN_POINT ( 'NONE',  ( -7.369174163213311424, 0.8229795343181387501, -116.5771123024643714 ) ) ;
#2658=CARTESIAN_POINT ( 'NONE',  ( 1.320501113854931408, 5.000000000000000888, -137.8664870916819893 ) ) ;
#2661=CARTESIAN_POINT ( 'NONE',  ( -1.445049718557150253, 5.000000000000792255, -134.5128495240823270 ) ) ;
#2662=CARTESIAN_POINT ( 'NONE',  ( 3.364081176287436303, 8.673617379884035472E-16, -112.2881015945827130 ) ) ;
#2663=VERTEX_POINT ( 'NONE', #8766 ) ;
#2668=CARTESIAN_POINT ( 'NONE',  ( 5.000000000000000888, 5.000000000000000888, -1.663700395152567513 ) ) ;
#2672=EDGE_LOOP ( 'NONE', ( #6989, #928, #356, #3266, #10511, #480, #13102, #13966, #3596, #9914, #5894, #9381, #9465, #2118, #3005, #7630, #5393, #2799 ) ) ;
#2677=EDGE_CURVE ( 'NONE', #9805, #5143, #771, .T. ) ;
#2680=DIRECTION ( 'NONE',  ( -0.000000000000000000, -1.000000000000000000, -0.000000000000000000 ) ) ;
#2681=ORIENTED_EDGE ( 'NONE', *, *, #2219, .F. ) ;
#2690=CARTESIAN_POINT ( 'NONE',  ( 10.05365188728890935, 14.67691136496379123, -106.1318723917360671 ) ) ;
#2696=CARTESIAN_POINT ( 'NONE',  ( 4.534579168377672609, -0.0002385848209785603532, -1.093758300940373074 ) ) ;
#2703=CARTESIAN_POINT ( 'NONE',  ( 9.127846621026490581, 15.00000000000139622, -105.9353198608211670 ) ) ;
#2713=CARTESIAN_POINT ( 'NONE',  ( 30.90149453746306207, 8.773889247172311556, -41.17582585713872589 ) ) ;
#2717=CARTESIAN_POINT ( 'NONE',  ( -20.78509463529371004, 8.673617379884033500E-16, -172.2980575345146974 ) ) ;
#2718=EDGE_LOOP ( 'NONE', ( #6691, #8467, #1302, #11751, #12754 ) ) ;
#2723=CARTESIAN_POINT ( 'NONE',  ( -27.15694708024977189, 8.673617379884035472E-16, -202.7147527119508368 ) ) ;
#2726=AXIS2_PLACEMENT_3D ( 'NONE', #15205, #3280, #7845 ) ;
#2738=CARTESIAN_POINT ( 'NONE',  ( -6.338840459429284202, 14.99999999995480060, -126.0591383733374329 ) ) ;
#2741=CARTESIAN_POINT ( 'NONE',  ( 2.616643680530136962, -8.673617379884035472E-16, -131.5934110696268249 ) ) ;
#2742=CARTESIAN_POINT ( 'NONE',  ( 8.322646197883424080, 5.000000000000000888, -114.4990917221399798 ) ) ;
#2746=ORIENTED_EDGE ( 'NONE', *, *, #4845, .F. ) ;
#2748=CARTESIAN_POINT ( 'NONE',  ( 27.03835354040193195, 5.000000000000000888, -138.2189567750509980 ) ) ;
#2752=ORIENTED_EDGE ( 'NONE', *, *, #2995, .F. ) ;
#2754=CARTESIAN_POINT ( 'NONE',  ( -6.310237929021329961, 14.99999999999999822, -119.2996315833885035 ) ) ;
#2758=CARTESIAN_POINT ( 'NONE',  ( 9.976451240238549900, 12.67941325565633548, -45.12530232831228716 ) ) ;
#2771=CARTESIAN_POINT ( 'NONE',  ( 10.88592809031993092, 3.654497976000929516, -107.0374611167700607 ) ) ;
#2774=CARTESIAN_POINT ( 'NONE',  ( 14.22910372453204353, 12.49999999999999822, -126.5134921567817941 ) ) ;
#2777=CARTESIAN_POINT ( 'NONE',  ( 5.018427371053902242, 0.04004715687429680204, 0.6822673155829361846 ) ) ;
#2781=EDGE_CURVE ( 'NONE', #933, #14561, #1007, .T. ) ;
#2784=FACE_OUTER_BOUND ( 'NONE', #4308, .T. ) ;
#2786=EDGE_CURVE ( 'NONE', #14187, #10636, #6901, .T. ) ;
#2795=CARTESIAN_POINT ( 'NONE',  ( 8.394286649619360219, 0.4947992169189873168, -105.8820645551709418 ) ) ;
#2797=CARTESIAN_POINT ( 'NONE',  ( 5.592744633116710773, 0.02476476750516211703, -140.8472914376584981 ) ) ;
#2798=CARTESIAN_POINT ( 'NONE',  ( -16.95575562637076317, 8.673617379884034486E-16, -165.1048961890580244 ) ) ;
#2799=ORIENTED_EDGE ( 'NONE', *, *, #1088, .F. ) ;
#2803=CARTESIAN_POINT ( 'NONE',  ( -20.53214307163321450, 4.000000000000000000, -200.7518619190079505 ) ) ;
#2809=CARTESIAN_POINT ( 'NONE',  ( -9.392097536374029332, 3.253592935916376216, -116.4406435548291796 ) ) ;
#2818=CARTESIAN_POINT ( 'NONE',  ( -9.492276965212552042, 15.00000000002442491, -117.3221826542650490 ) ) ;
#2819=CARTESIAN_POINT ( 'NONE',  ( -8.326762665057291457, 4.999999999999208633, -121.0857513973247279 ) ) ;
#2820=CARTESIAN_POINT ( 'NONE',  ( 8.873074003812353894, 5.000000000000000888, -110.5883967389741827 ) ) ;
#2821=ORIENTED_EDGE ( 'NONE', *, *, #3761, .T. ) ;
#2823=DIRECTION ( 'NONE',  ( 0.000000000000000000, 1.000000000000000000, 0.000000000000000000 ) ) ;
#2824=AXIS2_PLACEMENT_3D ( 'NONE', #8319, #7389, #1450 ) ;
#2825=CARTESIAN_POINT ( 'NONE',  ( 4.999922846598173543, 0.03155975272377924828, -16.26256187091226835 ) ) ;
#2826=VERTEX_POINT ( 'NONE', #6367 ) ;
#2828=CARTESIAN_POINT ( 'NONE',  ( 20.87131526946579285, 0.000000000000000000, -138.9752963459259547 ) ) ;
#2829=( BOUNDED_SURFACE ( )  B_SPLINE_SURFACE ( 3, 2, ( 
 ( #12532, #15101, #3033 ),
 ( #1946, #12460, #6659 ),
 ( #1878, #9056, #7887 ),
 ( #12610, #11450, #870 ),
 ( #4415, #5797, #11595 ),
 ( #8040, #2476, #8336 ),
 ( #2252, #6879, #11674 ),
 ( #9352, #9433, #1014 ) ),
 .UNSPECIFIED., .F., .F., .T. ) 
 B_SPLINE_SURFACE_WITH_KNOTS ( ( 4, 2, 2, 4 ),
 ( 3, 3 ),
 ( 0.06905721847989758355, 0.07704657673304832199, 0.08503593498619907431, 0.1010146514925005512 ),
 ( 0.000000000000000000, 1.000000000000000000 ),
 .UNSPECIFIED. ) 
 GEOMETRIC_REPRESENTATION_ITEM ( )  RATIONAL_B_SPLINE_SURFACE ( (
 ( 1.000000000000000000, 0.7071067811865475727, 1.000000000000000000),
 ( 1.000000000000000000, 0.7071067811865475727, 1.000000000000000000),
 ( 1.000000000000000000, 0.7071067811865475727, 1.000000000000000000),
 ( 1.000000000000000000, 0.7071067811865475727, 1.000000000000000000),
 ( 1.000000000000000000, 0.7071067811865473507, 1.000000000000000000),
 ( 1.000000000000000000, 0.7071067811865473507, 1.000000000000000000),
 ( 1.000000000000000000, 0.7071067811865475727, 1.000000000000000000),
 ( 1.000000000000000000, 0.7071067811865475727, 1.000000000000000000) ) ) 
 REPRESENTATION_ITEM ( '' )  SURFACE ( )  );
#2833=ORIENTED_EDGE ( 'NONE', *, *, #15271, .F. ) ;
#2836=EDGE_CURVE ( 'NONE', #4737, #6769, #13190, .T. ) ;
#2838=CARTESIAN_POINT ( 'NONE',  ( 1.013023623609336843, 4.588323854676484181, -139.4901577088605791 ) ) ;
#2839=CARTESIAN_POINT ( 'NONE',  ( 1.004809442601927394, 5.000000000000000888, -139.4752805618705622 ) ) ;
#2843=LINE ( 'NONE', #12327, #13451 ) ;
#2844=ORIENTED_EDGE ( 'NONE', *, *, #12794, .F. ) ;
#2846=CIRCLE ( 'NONE', #8761, 3.000000000000011990 ) ;
#2848=ORIENTED_EDGE ( 'NONE', *, *, #7527, .F. ) ;
#2852=CARTESIAN_POINT ( 'NONE',  ( 14.22910372453204353, 12.49999999999999822, -126.5134921567817941 ) ) ;
#2856=CARTESIAN_POINT ( 'NONE',  ( 11.04730217088347644, 5.000000000000000888, -107.1178495010082656 ) ) ;
#2859=DIRECTION ( 'NONE',  ( 0.000000000000000000, 1.000000000000000000, 0.000000000000000000 ) ) ;
#2872=CARTESIAN_POINT ( 'NONE',  ( 10.00185261163550976, 0.09491738922320896998, -163.8759456858575163 ) ) ;
#2874=CARTESIAN_POINT ( 'NONE',  ( -12.11204790299879086, 8.673617379884035472E-16, -158.0701594236071514 ) ) ;
#2876=CARTESIAN_POINT ( 'NONE',  ( -0.8029028047895949705, 8.673617379884034486E-16, -146.7767709142194121 ) ) ;
#2882=CARTESIAN_POINT ( 'NONE',  ( 26.88777289245747326, 6.000000000000000000, -138.4814624290440577 ) ) ;
#2892=CARTESIAN_POINT ( 'NONE',  ( -9.518035003875171540, 4.999999999998426148, -117.2217326885085669 ) ) ;
#2893=CARTESIAN_POINT ( 'NONE',  ( 10.69730027799064764, -3.493608200715386290E-11, -107.4734661196424241 ) ) ;
#2895=CARTESIAN_POINT ( 'NONE',  ( 10.97120727310200472, 11.75624639942191507, -44.98549499369563165 ) ) ;
#2897=CARTESIAN_POINT ( 'NONE',  ( 9.958478854730328678, 4.811568727942957757, -44.17880315911963862 ) ) ;
#2906=DIRECTION ( 'NONE',  ( 0.000000000000000000, 1.000000000000000000, 0.000000000000000000 ) ) ;
#2907=CARTESIAN_POINT ( 'NONE',  ( -9.625715240929997307, 11.51017254279852509, -115.8367759348243595 ) ) ;
#2909=EDGE_CURVE ( 'NONE', #2518, #11832, #8887, .T. ) ;
#2911=( BOUNDED_CURVE ( )  B_SPLINE_CURVE ( 3, ( #669, #593, #5375, #10018 ),
 .UNSPECIFIED., .F., .T. ) 
 B_SPLINE_CURVE_WITH_KNOTS ( ( 4, 4 ),
 ( 4.702026407136986386, 4.709001436419505637 ),
 .UNSPECIFIED. ) 
 CURVE ( )  GEOMETRIC_REPRESENTATION_ITEM ( )  RATIONAL_B_SPLINE_CURVE ( ( 1.000000000000000000, 0.9999959457513183381, 0.9999959457513183381, 1.000000000000000000 ) ) 
 REPRESENTATION_ITEM ( '' )  );
#2914=ORIENTED_EDGE ( 'NONE', *, *, #981, .T. ) ;
#2925=CARTESIAN_POINT ( 'NONE',  ( 26.71007981443201018, 12.49999999999999822, -136.8791680534710054 ) ) ;
#2926=ORIENTED_EDGE ( 'NONE', *, *, #13361, .T. ) ;
#2940=CARTESIAN_POINT ( 'NONE',  ( 4.351317386395303188, 0.03165940128134000359, -16.24646476423705010 ) ) ;
#2941=CARTESIAN_POINT ( 'NONE',  ( 12.85253911111128389, 2.933442265363937818, -165.9654706698083828 ) ) ;
#2943=CARTESIAN_POINT ( 'NONE',  ( -25.15812356329616151, -6.561949609624546619E-12, -172.1841440208294784 ) ) ;
#2948=ORIENTED_EDGE ( 'NONE', *, *, #12150, .F. ) ;
#2950=CARTESIAN_POINT ( 'NONE',  ( 18.69225092093103058, 2.850949024098341860E-47, -142.9045830238807184 ) ) ;
#2954=DIRECTION ( 'NONE',  ( 0.000000000000000000, 1.000000000000000000, 0.000000000000000000 ) ) ;
#2961=DIRECTION ( 'NONE',  ( -0.02181900108494679719, 0.000000000000000000, 0.9997619372588931741 ) ) ;
#2962=CARTESIAN_POINT ( 'NONE',  ( 9.247146435675446696, 0.000000000000000000, -109.6962599556842832 ) ) ;
#2966=ORIENTED_EDGE ( 'NONE', *, *, #7047, .F. ) ;
#2968=CARTESIAN_POINT ( 'NONE',  ( -4.234402844927150689, 15.00000000000000000, -117.4888040839639558 ) ) ;
#2972=ORIENTED_EDGE ( 'NONE', *, *, #7214, .F. ) ;
#2973=ADVANCED_FACE ( 'NONE', ( #2263 ), #4576, .F. ) ;
#2978=CIRCLE ( 'NONE', #3704, 1.000000000000000888 ) ;
#2980=CARTESIAN_POINT ( 'NONE',  ( 4.370967001746241642, 0.4765682694954604393, 1.559350592413775605 ) ) ;
#2981=DIRECTION ( 'NONE',  ( 0.02181900108494732801, 0.000000000000000000, -0.9997619372588932851 ) ) ;
#2983=CARTESIAN_POINT ( 'NONE',  ( 8.428994341907280585, 15.00000000000046896, -112.3028785388761861 ) ) ;
#2988=DIRECTION ( 'NONE',  ( 0.000000000000000000, 0.000000000000000000, -1.000000000000000000 ) ) ;
#2991=CIRCLE ( 'NONE', #764, 3.000000000000005329 ) ;
#2995=EDGE_CURVE ( 'NONE', #5143, #15130, #5431, .T. ) ;
#3000=( BOUNDED_SURFACE ( )  B_SPLINE_SURFACE ( 3, 2, ( 
 ( #664, #7687, #737 ),
 ( #890, #5442, #10086 ),
 ( #14820, #8924, #6608 ),
 ( #3053, #13651, #12322 ),
 ( #14973, #12479, #5372 ),
 ( #10163, #3194, #7765 ),
 ( #12633, #10241, #1896 ),
 ( #14898, #9149, #4294 ) ),
 .UNSPECIFIED., .F., .F., .F. ) 
 B_SPLINE_SURFACE_WITH_KNOTS ( ( 4, 2, 2, 4 ),
 ( 3, 3 ),
 ( 0.000000000000000000, 0.0007402894036727104788, 0.001480578807345420958, 0.002961157614690841915 ),
 ( 0.000000000000000000, 1.000000000000000000 ),
 .UNSPECIFIED. ) 
 GEOMETRIC_REPRESENTATION_ITEM ( )  RATIONAL_B_SPLINE_SURFACE ( (
 ( 1.000000000000000000, 0.7071067811865482389, 1.000000000000000000),
 ( 1.000000000000000000, 0.7156795336770270799, 1.000000000000000000),
 ( 1.000000000000000000, 0.7224940905405163871, 1.000000000000000000),
 ( 1.000000000000000000, 0.7317806849512016321, 1.000000000000000000),
 ( 1.000000000000000000, 0.7342507314798352169, 1.000000000000000000),
 ( 1.000000000000000000, 0.7342566494600053506, 1.000000000000000000),
 ( 1.000000000000000000, 0.7244594855316945914, 1.000000000000000000),
 ( 1.000000000000000000, 0.7071067811865469066, 1.000000000000000000) ) ) 
 REPRESENTATION_ITEM ( '' )  SURFACE ( )  );
#3001=CARTESIAN_POINT ( 'NONE',  ( -6.790153584124027475, 6.000000000000000000, -124.9643354754709748 ) ) ;
#3005=ORIENTED_EDGE ( 'NONE', *, *, #11838, .F. ) ;
#3010=CARTESIAN_POINT ( 'NONE',  ( -2.397620167341370845, 9.999999999999998224, -107.6176329143618204 ) ) ;
#3017=CARTESIAN_POINT ( 'NONE',  ( -7.749031843371119166, 1.142173573887167004, -116.8124745394366784 ) ) ;
#3019=DIRECTION ( 'NONE',  ( 0.000000000000000000, 1.000000000000000000, 0.000000000000000000 ) ) ;
#3022=CARTESIAN_POINT ( 'NONE',  ( 9.414574752465050267, 1.210099420865203834, -106.3373578080001209 ) ) ;
#3023=CARTESIAN_POINT ( 'NONE',  ( -29.07636141981161515, 0.000000000000000000, -184.7664156487973912 ) ) ;
#3029=CARTESIAN_POINT ( 'NONE',  ( 9.697553513687202198, 1.319436597465116101, -105.9306301742863496 ) ) ;
#3033=CARTESIAN_POINT ( 'NONE',  ( 27.13166404935670428, 5.000000000000000888, -138.0564292571840213 ) ) ;
#3035=CIRCLE ( 'NONE', #1801, 1.000000000000042633 ) ;
#3043=CARTESIAN_POINT ( 'NONE',  ( 10.95691125489327789, 11.77390254760747546, -44.42524603584411125 ) ) ;
#3044=ORIENTED_EDGE ( 'NONE', *, *, #517, .F. ) ;
#3045=CARTESIAN_POINT ( 'NONE',  ( 9.978323787696259828, 4.811580018084409716, -45.08809239636353539 ) ) ;
#3046=CARTESIAN_POINT ( 'NONE',  ( -2.200833853042387211, 4.000000000000000000, -178.3042252324553942 ) ) ;
#3053=CARTESIAN_POINT ( 'NONE',  ( 10.97120741197404570, 11.75624598098227303, -44.98549899094406612 ) ) ;
#3054=CARTESIAN_POINT ( 'NONE',  ( 10.00369055844187649, 12.49999999999999822, -46.08764602067113714 ) ) ;
#3055=CARTESIAN_POINT ( 'NONE',  ( 4.945012662353664545, 1.189081421482657053, 3.158926035384847175 ) ) ;
#3056=CARTESIAN_POINT ( 'NONE',  ( -6.510167201456665609, 14.56253871824070956, -117.0692195733290504 ) ) ;
#3058=AXIS2_PLACEMENT_3D ( 'NONE', #12363, #3019, #7645 ) ;
#3059=CARTESIAN_POINT ( 'NONE',  ( 8.541738004265454265, 12.49999999999999822, -116.2437985783182057 ) ) ;
#3060=CARTESIAN_POINT ( 'NONE',  ( 20.87131526946576443, 1.301042606982605321E-15, -138.9752963459259547 ) ) ;
#3062=EDGE_CURVE ( 'NONE', #2133, #2207, #12988, .T. ) ;
#3076=ORIENTED_EDGE ( 'NONE', *, *, #11316, .T. ) ;
#3080=DIRECTION ( 'NONE',  ( 0.02181900108494663065, 0.000000000000000000, -0.9997619372588932851 ) ) ;
#3090=CARTESIAN_POINT ( 'NONE',  ( 9.531305032586972814, 1.319851304386060020, -106.3909117981410901 ) ) ;
#3091=EDGE_LOOP ( 'NONE', ( #11307, #6248, #1248, #4284 ) ) ;
#3093=CARTESIAN_POINT ( 'NONE',  ( -29.84187669631901940, -8.150263268976921852E-13, -194.0986676374979822 ) ) ;
#3105=CARTESIAN_POINT ( 'NONE',  ( -6.992168204694889866, 8.673617379884035472E-16, -113.2636094677359893 ) ) ;
#3119=CARTESIAN_POINT ( 'NONE',  ( 9.032890029152659039, 12.50000000000000355, -118.1323615500725310 ) ) ;
#3128=CARTESIAN_POINT ( 'NONE',  ( 5.238157166760104566, 1.649858934233373597, 3.774848331988833738 ) ) ;
#3129=CARTESIAN_POINT ( 'NONE',  ( -8.455319114079282272, 13.21761715718190899, -116.6570696633502706 ) ) ;
#3130=CARTESIAN_POINT ( 'NONE',  ( 5.856043916822682327, 15.00000000000000000, -115.1238147290586653 ) ) ;
#3132=CARTESIAN_POINT ( 'NONE',  ( 25.22814042709519100, 1.659276419493565857, -137.4257722450890356 ) ) ;
#3133=ORIENTED_EDGE ( 'NONE', *, *, #981, .F. ) ;
#3135=CYLINDRICAL_SURFACE ( 'NONE', #7983, 2.500000000000000000 ) ;
#3138=DIRECTION ( 'NONE',  ( -0.9997619372588932851, 0.000000000000000000, -0.02181900108494672086 ) ) ;
#3140=CARTESIAN_POINT ( 'NONE',  ( 9.940211158120405344, 12.49999999999999822, -43.17897536272747772 ) ) ;
#3141=CARTESIAN_POINT ( 'NONE',  ( -4.234402844927150689, 0.000000000000000000, -117.4888040839639558 ) ) ;
#3144=CARTESIAN_POINT ( 'NONE',  ( 10.50985052422430321, 5.000000000000000888, -107.7177067850638679 ) ) ;
#3145=DIRECTION ( 'NONE',  ( 0.02181900108494707474, 0.000000000000000000, -0.9997619372588931741 ) ) ;
#3146=ORIENTED_EDGE ( 'NONE', *, *, #4363, .T. ) ;
#3153=DIRECTION ( 'NONE',  ( 0.000000000000000000, 0.9314983497198057183, 0.3637455490714332496 ) ) ;
#3154=CARTESIAN_POINT ( 'NONE',  ( -8.506498296742686094, 1.839370509249187213, -116.6455419169649446 ) ) ;
#3157=CARTESIAN_POINT ( 'NONE',  ( 4.999961392659725057, -8.122774307663799537E-14, -31.10603894082280263 ) ) ;
#3158=CARTESIAN_POINT ( 'NONE',  ( 5.783145697618031100, 15.00000000000000178, -114.0858433367058637 ) ) ;
#3159=CYLINDRICAL_SURFACE ( 'NONE', #8153, 0.4999999999999726885 ) ;
#3161=CARTESIAN_POINT ( 'NONE',  ( -25.32823296183972417, 0.000000000000000000, -187.0457223361869410 ) ) ;
#3162=CARTESIAN_POINT ( 'NONE',  ( 12.72476843650552425, 3.715092006986288720, -166.5695719882495496 ) ) ;
#3165=EDGE_LOOP ( 'NONE', ( #10848, #10915, #4081, #1381 ) ) ;
#3167=CARTESIAN_POINT ( 'NONE',  ( 9.186974873226770200, 0.9102337534740122527, -105.7859147073006767 ) ) ;
#3170=CARTESIAN_POINT ( 'NONE',  ( 8.875022500030622652, 10.34680280068111458, 5.628716254818995957 ) ) ;
#3171=CARTESIAN_POINT ( 'NONE',  ( -0.5126277339614576656, -3.286289637815826199E-12, -103.6859198938546882 ) ) ;
#3188=CARTESIAN_POINT ( 'NONE',  ( -10.42889815920712060, 4.000000000000000000, -186.8962127970309837 ) ) ;
#3194=CARTESIAN_POINT ( 'NONE',  ( 10.02828843047459095, 11.77391908303435208, -44.24972543469815633 ) ) ;
#3198=CARTESIAN_POINT ( 'NONE',  ( -7.230043083586023656, 14.09412780563432221, -116.2995594653081355 ) ) ;
#3201=CARTESIAN_POINT ( 'NONE',  ( 5.834340755081701246, 15.00000000000000000, -112.9803539749909902 ) ) ;
#3202=DIRECTION ( 'NONE',  ( 0.000000000000000000, 1.000000000000000000, 0.000000000000000000 ) ) ;
#3203=ORIENTED_EDGE ( 'NONE', *, *, #13851, .T. ) ;
#3204=CARTESIAN_POINT ( 'NONE',  ( 23.63626030785080090, 0.5263503646225780042, -138.6462866365781963 ) ) ;
#3210=ORIENTED_EDGE ( 'NONE', *, *, #8656, .F. ) ;
#3213=VECTOR ( 'NONE', #1262, 1000.000000000000000 ) ;
#3215=CARTESIAN_POINT ( 'NONE',  ( -24.92455668927321000, 1.982032305341395295, -207.3388352837438049 ) ) ;
#3216=CARTESIAN_POINT ( 'NONE',  ( 0.2328350733780833737, -8.673617379884037444E-16, -127.8934642279842819 ) ) ;
#3219=CARTESIAN_POINT ( 'NONE',  ( 12.10928247722332074, 5.000000000000000000, -123.8687610530459438 ) ) ;
#3220=VECTOR ( 'NONE', #5191, 1000.000000000000000 ) ;
#3221=LINE ( 'NONE', #13907, #15096 ) ;
#3224=VERTEX_POINT ( 'NONE', #1101 ) ;
#3232=ORIENTED_EDGE ( 'NONE', *, *, #140, .F. ) ;
#3238=( GEOMETRIC_REPRESENTATION_CONTEXT ( 3 ) GLOBAL_UNCERTAINTY_ASSIGNED_CONTEXT ( ( #4788 ) ) GLOBAL_UNIT_ASSIGNED_CONTEXT ( ( #12712, #9372, #2124 ) ) REPRESENTATION_CONTEXT ( 'NONE', 'WORKASPACE' ) );
#3240=CARTESIAN_POINT ( 'NONE',  ( -28.09207221025136292, 4.000000000000024869, -205.1456435447945807 ) ) ;
#3245=VERTEX_POINT ( 'NONE', #8423 ) ;
#3249=CARTESIAN_POINT ( 'NONE',  ( 8.962104331735417873, 14.96030145802490097, 1.638565632197652944 ) ) ;
#3250=CARTESIAN_POINT ( 'NONE',  ( -1.499260709785477097, 5.000000000000000888, -106.0110764665418515 ) ) ;
#3252=TOROIDAL_SURFACE ( 'NONE', #13388, 2.000000000000009326, 1.000000000000000000 ) ;
#3258=DIRECTION ( 'NONE',  ( 0.000000000000000000, 1.000000000000000000, 0.000000000000000000 ) ) ;
#3262=CARTESIAN_POINT ( 'NONE',  ( 1.320501113854931630, 10.00000000000000000, -137.8664870916819893 ) ) ;
#3264=ORIENTED_EDGE ( 'NONE', *, *, #13113, .F. ) ;
#3266=ORIENTED_EDGE ( 'NONE', *, *, #6474, .T. ) ;
#3267=CARTESIAN_POINT ( 'NONE',  ( -18.37680385559763963, 3.999999999999999112, -197.3497678893306215 ) ) ;
#3279=CARTESIAN_POINT ( 'NONE',  ( 5.818533358179984738, 15.00000000000000000, -114.5878108573819247 ) ) ;
#3280=DIRECTION ( 'NONE',  ( 0.000000000000000000, 1.000000000000000000, 0.000000000000000000 ) ) ;
#3281=VERTEX_POINT ( 'NONE', #9754 ) ;
#3282=AXIS2_PLACEMENT_3D ( 'NONE', #9719, #14452, #8546 ) ;
#3283=CARTESIAN_POINT ( 'NONE',  ( 26.30091364428284351, 3.130032034343683378, -137.0310972895143209 ) ) ;
#3287=ORIENTED_EDGE ( 'NONE', *, *, #8631, .F. ) ;
#3293=ORIENTED_EDGE ( 'NONE', *, *, #14235, .F. ) ;
#3295=B_SPLINE_CURVE_WITH_KNOTS ( 'NONE', 3,
 ( #12252, #12009, #1435, #714, #5418, #13705, #4271, #7815, #6141, #275, #4990, #3834, #2248, #5640, #11592, #1159 ),
 .UNSPECIFIED., .F., .F.,
 ( 4, 2, 2, 2, 2, 2, 2, 4 ),
 ( 3.469446951953614189E-18, 0.006235229064615841442, 0.01247045812923167941, 0.01870568719384751652, 0.02182330172615543767, 0.02494091625846335536, 0.03741137438769520651, 0.04988183251692705766 ),
 .UNSPECIFIED. ) ;
#3300=AXIS2_PLACEMENT_3D ( 'NONE', #15057, #10250, #2988 ) ;
#3301=CARTESIAN_POINT ( 'NONE',  ( -24.82503501351391151, 2.452721149805614953, -207.8977114406789326 ) ) ;
#3304=CARTESIAN_POINT ( 'NONE',  ( 10.81974369748103371, 5.000000000000000000, -121.8879343890986888 ) ) ;
#3308=CARTESIAN_POINT ( 'NONE',  ( 4.248871783098677746, 15.00000000000000000, -126.1456066832004126 ) ) ;
#3320=CARTESIAN_POINT ( 'NONE',  ( 8.875022474551933271, 4.581109498455814055, 5.628716231298513506 ) ) ;
#3327=CARTESIAN_POINT ( 'NONE',  ( -25.63598692233250986, 1.717341244404099410, -207.0184607745250105 ) ) ;
#3329=CARTESIAN_POINT ( 'NONE',  ( -4.781971238369687960, 5.000000000000000888, -110.8602639898370654 ) ) ;
#3331=CARTESIAN_POINT ( 'NONE',  ( 4.413686865555820127, 8.673617379884035472E-16, -104.6754972201258624 ) ) ;
#3334=CARTESIAN_POINT ( 'NONE',  ( 6.122889832264990062, 15.00000000000000000, 5.281130614573720905 ) ) ;
#3335=CARTESIAN_POINT ( 'NONE',  ( 5.000000000000000888, 15.00000000000000000, -100.6237003951525679 ) ) ;
#3341=ORIENTED_EDGE ( 'NONE', *, *, #13116, .T. ) ;
#3343=CARTESIAN_POINT ( 'NONE',  ( 3.254529015745487808, 4.000000000000000000, -173.6235312550020353 ) ) ;
#3347=EDGE_LOOP ( 'NONE', ( #10939, #15172, #426 ) ) ;
#3352=ADVANCED_FACE ( 'NONE', ( #5450 ), #822, .F. ) ;
#3356=PLANE ( 'NONE',  #2726 ) ;
#3358=CARTESIAN_POINT ( 'NONE',  ( 25.59005225942203055, 2.055286875414667591, -137.2931158548774988 ) ) ;
#3361=ORIENTED_EDGE ( 'NONE', *, *, #11584, .F. ) ;
#3367=FACE_OUTER_BOUND ( 'NONE', #10909, .T. ) ;
#3370=CARTESIAN_POINT ( 'NONE',  ( -25.22011045336418533, 0.8049789667763997958, -204.9699801733243874 ) ) ;
#3371=EDGE_CURVE ( 'NONE', #1192, #5516, #8622, .T. ) ;
#3372=EDGE_CURVE ( 'NONE', #6985, #13571, #4844, .T. ) ;
#3374=EDGE_CURVE ( 'NONE', #15130, #10045, #8634, .T. ) ;
#3376=CIRCLE ( 'NONE', #9101, 16.00000000006737721 ) ;
#3379=CARTESIAN_POINT ( 'NONE',  ( 20.87131526946579285, 0.000000000000000000, -138.9752963459259547 ) ) ;
#3390=LINE ( 'NONE', #8100, #15195 ) ;
#3392=CARTESIAN_POINT ( 'NONE',  ( -29.21839114985998975, -1.098965884223355800E-12, -199.4123269880084024 ) ) ;
#3394=( BOUNDED_SURFACE ( )  B_SPLINE_SURFACE ( 3, 1, ( 
 ( #13482, #6655 ),
 ( #2882, #1712 ),
 ( #11366, #10063 ),
 ( #12376, #5345 ) ),
 .UNSPECIFIED., .F., .F., .T. ) 
 B_SPLINE_SURFACE_WITH_KNOTS ( ( 4, 4 ),
 ( 2, 2 ),
 ( 0.000000000000000000, 1.000000000000000000 ),
 ( 0.000000000000000000, 1.000000000000000000 ),
 .UNSPECIFIED. ) 
 GEOMETRIC_REPRESENTATION_ITEM ( )  RATIONAL_B_SPLINE_SURFACE ( (
 ( 1.000000000000000000, 1.000000000000000000),
 ( 0.9999959457513183381, 0.9999959457513183381),
 ( 0.9999959457513183381, 0.9999959457513183381),
 ( 1.000000000000000000, 1.000000000000000000) ) ) 
 REPRESENTATION_ITEM ( '' )  SURFACE ( )  );
#3397=ORIENTED_EDGE ( 'NONE', *, *, #12408, .T. ) ;
#3400=CARTESIAN_POINT ( 'NONE',  ( 8.875781042498779527, 10.69239977982764778, 5.593959306807169796 ) ) ;
#3401=CARTESIAN_POINT ( 'NONE',  ( -3.886960648222041021E-10, 8.673617379884035472E-16, -101.1952717268999891 ) ) ;
#3413=EDGE_LOOP ( 'NONE', ( #7446, #2542, #7270 ) ) ;
#3414=CARTESIAN_POINT ( 'NONE',  ( 9.032650406499481477, 4.000000000000000000, -169.1646757747120375 ) ) ;
#3418=ORIENTED_EDGE ( 'NONE', *, *, #10609, .F. ) ;
#3422=SHAPE_REPRESENTATION_RELATIONSHIP ( 'NONE' , 'NONE' ,  #7636, #9451 ) ;
#3430=EDGE_LOOP ( 'NONE', ( #13565, #9466, #1939 ) ) ;
#3431=ADVANCED_FACE ( 'NONE', ( #5596 ), #3356, .T. ) ;
#3439=CARTESIAN_POINT ( 'NONE',  ( -1.499260709886190313, 15.00000000000162537, -106.0110764664949556 ) ) ;
#3442=FACE_OUTER_BOUND ( 'NONE', #2132, .T. ) ;
#3447=CARTESIAN_POINT ( 'NONE',  ( 30.93967778936172053, 8.773889247172311556, -42.92540924734178986 ) ) ;
#3468=CARTESIAN_POINT ( 'NONE',  ( 8.935548306746156300, 5.000000000000000888, 2.855381328098106408 ) ) ;
#3473=ORIENTED_EDGE ( 'NONE', *, *, #3761, .F. ) ;
#3478=CARTESIAN_POINT ( 'NONE',  ( -25.70034284263700286, 0.9795334954347006962, -205.5107766831865774 ) ) ;
#3481=DIRECTION ( 'NONE',  ( -0.02181900108494707127, 0.000000000000000000, 0.9997619372588931741 ) ) ;
#3485=FACE_BOUND ( 'NONE', #8055, .T. ) ;
#3496=DIRECTION ( 'NONE',  ( -0.000000000000000000, 1.000000000000000000, -0.000000000000000000 ) ) ;
#3501=TOROIDAL_SURFACE ( 'NONE', #9172, 1.250000000000002220, 1.750000000000000000 ) ;
#3504=CARTESIAN_POINT ( 'NONE',  ( 4.505624869885556549, 8.673617379884035472E-16, -107.9937432812489675 ) ) ;
#3507=B_SPLINE_CURVE_WITH_KNOTS ( 'NONE', 3,
 ( #12625, #12472, #5511, #1958, #8916, #11463, #3267, #810, #13645, #730, #3188, #11309, #3046, #6444, #6673, #8992 ),
 .UNSPECIFIED., .F., .F.,
 ( 4, 2, 2, 2, 2, 2, 2, 4 ),
 ( 0.0004752521799440825390, 0.007644733457695613091, 0.01122947409657133917, 0.01481421473544706699, 0.02198369601319844976, 0.02915317729094983254, 0.04349213984645259462, 0.05783110240195536711 ),
 .UNSPECIFIED. ) ;
#3510=CARTESIAN_POINT ( 'NONE',  ( 9.410602039242014882, 1.734723475976807094E-15, -119.1126025278262972 ) ) ;
#3515=EDGE_LOOP ( 'NONE', ( #11061, #5637, #13314, #3210, #2265 ) ) ;
#3520=CARTESIAN_POINT ( 'NONE',  ( 5.000000000000000000, 14.99999999999999822, -100.6237003951525537 ) ) ;
#3527=ADVANCED_FACE ( 'NONE', ( #2584 ), #10985, .T. ) ;
#3528=DIRECTION ( 'NONE',  ( 0.5205261093005589812, 0.000000000000000000, -0.8538457527776445177 ) ) ;
#3535=CARTESIAN_POINT ( 'NONE',  ( -6.288157641191917335, 6.000000000000000000, -124.9981450708252595 ) ) ;
#3547=CARTESIAN_POINT ( 'NONE',  ( 6.122889832264990062, 5.000000000000000888, 5.281130614573720017 ) ) ;
#3554=CARTESIAN_POINT ( 'NONE',  ( 6.491365067585770809, 15.00000000000000000, 0.2705411889128687131 ) ) ;
#3560=DIRECTION ( 'NONE',  ( -0.02181900108494707127, 8.601065436648711846E-18, 0.9997619372588932851 ) ) ;
#3566=CARTESIAN_POINT ( 'NONE',  ( 1.114947364559093712, 6.000000000000000000, -139.4079432275550232 ) ) ;
#3573=ORIENTED_EDGE ( 'NONE', *, *, #4309, .T. ) ;
#3576=CARTESIAN_POINT ( 'NONE',  ( 4.641633639902737585, 8.673617379884035472E-16, -171.4570495182728394 ) ) ;
#3582=CARTESIAN_POINT ( 'NONE',  ( -8.207841483266339111, 1.782382842934248757, -115.8806436028926754 ) ) ;
#3585=CARTESIAN_POINT ( 'NONE',  ( 1.727947212398772889E-15, 5.000000000000000888, -101.3854116612075558 ) ) ;
#3586=CARTESIAN_POINT ( 'NONE',  ( 3.495361625530554406, 8.673617379884035472E-16, -116.4903051220812245 ) ) ;
#3591=CARTESIAN_POINT ( 'NONE',  ( 8.694046762359278091, 4.317799523304588693E-13, -116.9683691484218429 ) ) ;
#3596=ORIENTED_EDGE ( 'NONE', *, *, #162, .T. ) ;
#3601=CARTESIAN_POINT ( 'NONE',  ( 6.146364248477357961, 12.22024339317073505, 4.771788172891424651 ) ) ;
#3605=CARTESIAN_POINT ( 'NONE',  ( 6.410190855677554644, 14.99999999999999645, -118.0482597935656059 ) ) ;
#3615=CARTESIAN_POINT ( 'NONE',  ( 10.61533446930841329, 2.427390659569241826, -106.1975553300598847 ) ) ;
#3619=LINE ( 'NONE', #14376, #10626 ) ;
#3620=EDGE_LOOP ( 'NONE', ( #14113, #13518, #4964, #7899 ) ) ;
#3621=CARTESIAN_POINT ( 'NONE',  ( 5.039641941650827128, 0.1039572970898357956, -1.141581774561155616 ) ) ;
#3634=CARTESIAN_POINT ( 'NONE',  ( -3.025102703132704018, 8.666684749742557836E-31, -116.3639557890653293 ) ) ;
#3639=CARTESIAN_POINT ( 'NONE',  ( -0.2990415025319886344, 3.999999999999993783, -140.3882592102232820 ) ) ;
#3643=ORIENTED_EDGE ( 'NONE', *, *, #1668, .F. ) ;
#3646=CARTESIAN_POINT ( 'NONE',  ( 12.60805090540101681, 8.673617379884035472E-16, -165.7379246688466310 ) ) ;
#3653=EDGE_CURVE ( 'NONE', #11204, #10207, #12572, .T. ) ;
#3655=DIRECTION ( 'NONE',  ( 0.000000000000000000, 0.000000000000000000, 1.000000000000000000 ) ) ;
#3660=CARTESIAN_POINT ( 'NONE',  ( 10.82638304853600530, 14.99999999999719336, -107.3456397789498169 ) ) ;
#3661=CARTESIAN_POINT ( 'NONE',  ( 9.723706525202544526, 5.000000000000000888, -119.8316069321735284 ) ) ;
#3671=CARTESIAN_POINT ( 'NONE',  ( 6.491365067585774362, 15.00000000000000000, 0.2705411889128706004 ) ) ;
#3673=EDGE_CURVE ( 'NONE', #16, #11237, #1972, .T. ) ;
#3675=CARTESIAN_POINT ( 'NONE',  ( 9.044950117654433797, 0.000000000000000000, -137.9826476090360643 ) ) ;
#3685=CARTESIAN_POINT ( 'NONE',  ( 10.39131294298060837, 2.427390659499539360, -106.7954589000411829 ) ) ;
#3689=CARTESIAN_POINT ( 'NONE',  ( 1.041770615072654671, 4.863578055268357403, -139.4526175671829549 ) ) ;
#3690=CIRCLE ( 'NONE', #9124, 16.00000000006737721 ) ;
#3692=CARTESIAN_POINT ( 'NONE',  ( 5.335252549867767868, 0.09849780990753932708, 1.313236408779714814 ) ) ;
#3701=CARTESIAN_POINT ( 'NONE',  ( 10.43370164639825326, 14.41280555657135309, -106.2140181855886425 ) ) ;
#3704=AXIS2_PLACEMENT_3D ( 'NONE', #257, #8439, #9455 ) ;
#3709=CARTESIAN_POINT ( 'NONE',  ( 9.541413199640935261, 1.119725504013711048E-15, -163.5385917027302867 ) ) ;
#3710=DIRECTION ( 'NONE',  ( 0.000000000000000000, 0.000000000000000000, 1.000000000000000000 ) ) ;
#3712=EDGE_CURVE ( 'NONE', #587, #3245, #12580, .T. ) ;
#3713=CARTESIAN_POINT ( 'NONE',  ( 1.004809442601847236, 6.000000000000000000, -139.4752805618705906 ) ) ;
#3716=AXIS2_PLACEMENT_3D ( 'NONE', #14024, #5742, #7987 ) ;
#3717=CARTESIAN_POINT ( 'NONE',  ( 7.490632659013988892, 1.449414178213610072, 1.923996036189850267 ) ) ;
#3719=AXIS2_PLACEMENT_3D ( 'NONE', #4014, #7556, #12421 ) ;
#3724=CARTESIAN_POINT ( 'NONE',  ( -21.23553893743079257, 8.673617379884035472E-16, -200.3363993825013836 ) ) ;
#3728=VERTEX_POINT ( 'NONE', #3140 ) ;
#3730=B_SPLINE_CURVE_WITH_KNOTS ( 'NONE', 3,
 ( #9968, #5331, #11427, #6714, #7722, #849, #4177, #12286, #12586, #4255, #6639, #1927, #4329, #1696, #5552, #8882, #8956, #9032 ),
 .UNSPECIFIED., .F., .F.,
 ( 4, 2, 2, 2, 2, 2, 2, 2, 4 ),
 ( 0.000000000000000000, 0.001049529208182857888, 0.002099058416365715777, 0.003148587624548573882, 0.004198116832731431554, 0.005247646040914289225, 0.006297175249097147764, 0.007346704457280005436, 0.008396233665462863108 ),
 .UNSPECIFIED. ) ;
#3735=CARTESIAN_POINT ( 'NONE',  ( -2.546424457856566903, 15.00000000000000711, -122.2590118678561879 ) ) ;
#3738=CARTESIAN_POINT ( 'NONE',  ( -0.6967232357644530527, 6.071532165918824830E-15, -126.1497135265504710 ) ) ;
#3739=CARTESIAN_POINT ( 'NONE',  ( 11.09126156221322468, 5.000000000000000888, -122.3351348874415123 ) ) ;
#3740=VERTEX_POINT ( 'NONE', #1677 ) ;
#3741=ADVANCED_FACE ( 'NONE', ( #9949 ), #4088, .F. ) ;
#3751=CARTESIAN_POINT ( 'NONE',  ( -5.318033920939080339, 14.99999999999999645, -111.4753907371158306 ) ) ;
#3756=CARTESIAN_POINT ( 'NONE',  ( 13.13192191588670887, 4.000000000000000000, -166.1703390355876877 ) ) ;
#3759=CARTESIAN_POINT ( 'NONE',  ( 14.32267195561841611, 15.00000000000000000, -126.6197849905234278 ) ) ;
#3761=EDGE_CURVE ( 'NONE', #2185, #9168, #3690, .T. ) ;
#3770=CARTESIAN_POINT ( 'NONE',  ( 3.434326385468031368E-15, 9.999999999999998224, -105.0258972447171857 ) ) ;
#3772=CARTESIAN_POINT ( 'NONE',  ( 11.03724132942435077, 3.288823991935399871, -106.7036158171736560 ) ) ;
#3774=CARTESIAN_POINT ( 'NONE',  ( -1.381864148822929517, 14.99999999999999467, -125.5243971703837502 ) ) ;
#3777=CARTESIAN_POINT ( 'NONE',  ( 6.640721414892046148, 0.6192446679225036554, 3.208961039068100263 ) ) ;
#3779=VECTOR ( 'NONE', #1289, 1000.000000000000114 ) ;
#3785=FACE_OUTER_BOUND ( 'NONE', #9361, .T. ) ;
#3786=FACE_OUTER_BOUND ( 'NONE', #13267, .T. ) ;
#3794=CARTESIAN_POINT ( 'NONE',  ( 5.000000000000000888, 9.999999999999998224, -1.663700395152567513 ) ) ;
#3796=CARTESIAN_POINT ( 'NONE',  ( 0.1498948966650933412, 8.673617379884034486E-16, -141.0708338584945238 ) ) ;
#3798=CARTESIAN_POINT ( 'NONE',  ( -22.08223501799798782, 8.673617379884035472E-16, -175.4757740284503882 ) ) ;
#3804=CARTESIAN_POINT ( 'NONE',  ( -19.14087761289907874, 8.673617379884035472E-16, -189.8783295055868621 ) ) ;
#3808=CIRCLE ( 'NONE', #12442, 2.000000000000001776 ) ;
#3811=CARTESIAN_POINT ( 'NONE',  ( -4.234402844927157794, 4.336808689942017736E-16, -117.4888040839639558 ) ) ;
#3819=CARTESIAN_POINT ( 'NONE',  ( 19.86183279998939710, 6.000000000000000000, -197.2308909269244168 ) ) ;
#3821=CARTESIAN_POINT ( 'NONE',  ( 2.094832066372632084, 4.336808689942017736E-15, -130.8460463719122799 ) ) ;
#3822=CARTESIAN_POINT ( 'NONE',  ( 6.092154713215619743, 1.734723475976807094E-15, -123.6955108764303048 ) ) ;
#3824=DIRECTION ( 'NONE',  ( 0.000000000000000000, 1.000000000000000000, 0.000000000000000000 ) ) ;
#3827=ORIENTED_EDGE ( 'NONE', *, *, #3372, .F. ) ;
#3832=ADVANCED_FACE ( 'NONE', ( #3442 ), #11966, .T. ) ;
#3833=ORIENTED_EDGE ( 'NONE', *, *, #2995, .T. ) ;
#3834=CARTESIAN_POINT ( 'NONE',  ( -7.070709739118031578, 8.673617379884037444E-16, -176.2010769231267489 ) ) ;
#3837=CARTESIAN_POINT ( 'NONE',  ( -24.62038850795502043, 3.897326768351937698, -208.8858515350064806 ) ) ;
#3839=DIRECTION ( 'NONE',  ( 0.000000000000000000, 0.000000000000000000, 1.000000000000000000 ) ) ;
#3841=FACE_OUTER_BOUND ( 'NONE', #6749, .T. ) ;
#3846=CARTESIAN_POINT ( 'NONE',  ( 10.97171279554003043, 8.773889247172311556, -44.61149169061435060 ) ) ;
#3849=EDGE_CURVE ( 'NONE', #6985, #11984, #1543, .T. ) ;
#3854=CARTESIAN_POINT ( 'NONE',  ( 6.612393103706271091, -6.831570436677307681E-13, -105.0937218669710944 ) ) ;
#3856=DIRECTION ( 'NONE',  ( 0.000000000000000000, -0.000000000000000000, 1.000000000000000000 ) ) ;
#3859=CARTESIAN_POINT ( 'NONE',  ( 4.697001853051453679, 0.007744268132012307668, -0.2236376289218673930 ) ) ;
#3866=CARTESIAN_POINT ( 'NONE',  ( 9.846296305695277695, 14.78380347570996456, -106.2491606183390047 ) ) ;
#3874=CARTESIAN_POINT ( 'NONE',  ( 10.53129000145030325, 0.3802680776936400719, -164.5383768468789754 ) ) ;
#3878=CARTESIAN_POINT ( 'NONE',  ( 6.222862683364174252, 0.008970098793881749535, -139.3955611241877079 ) ) ;
#3879=CARTESIAN_POINT ( 'NONE',  ( 6.268325292624917999, 0.5457983033243376525, 0.8953897332030867906 ) ) ;
#3886=CARTESIAN_POINT ( 'NONE',  ( 9.068716941525991615, 0.000000000000000000, -163.1923081219560174 ) ) ;
#3900=CARTESIAN_POINT ( 'NONE',  ( -1.898078448822344777, -8.673617379884035472E-16, -123.6789374535451316 ) ) ;
#3904=CARTESIAN_POINT ( 'NONE',  ( 10.98449875134631348, 11.68766637954128029, -45.34906074712609581 ) ) ;
#3905=ORIENTED_EDGE ( 'NONE', *, *, #8058, .T. ) ;
#3907=ORIENTED_EDGE ( 'NONE', *, *, #1491, .T. ) ;
#3914=CARTESIAN_POINT ( 'NONE',  ( -1.586855474368330077, 14.99999999999999822, -114.8059160835097714 ) ) ;
#3917=CARTESIAN_POINT ( 'NONE',  ( 4.083862360612559250, 0.1767556829816783193, -0.01992505507647806748 ) ) ;
#3929=CARTESIAN_POINT ( 'NONE',  ( 11.32911568800036761, 5.000000000000000888, -106.8195553349435301 ) ) ;
#3932=CARTESIAN_POINT ( 'NONE',  ( 11.04730217088347644, 12.49999999999999822, -107.1178495010082656 ) ) ;
#3934=CARTESIAN_POINT ( 'NONE',  ( 5.625964192004158981, 0.1718480277638484433, 1.809263816539721015 ) ) ;
#3952=CARTESIAN_POINT ( 'NONE',  ( 1.114947364559086829, 6.000000000000000000, -139.4079432275550232 ) ) ;
#3953=CARTESIAN_POINT ( 'NONE',  ( 26.58801926426209405, 6.000000000000000000, -139.0072983920785532 ) ) ;
#3955=CARTESIAN_POINT ( 'NONE',  ( -9.695200183287226992, 8.673617379884037444E-16, -155.2279384737427108 ) ) ;
#3956=ORIENTED_EDGE ( 'NONE', *, *, #12449, .F. ) ;
#3959=ORIENTED_EDGE ( 'NONE', *, *, #11381, .T. ) ;
#3962=CARTESIAN_POINT ( 'NONE',  ( -12.21562406281302415, 3.999999999997721378, -189.0327199747631255 ) ) ;
#3965=AXIS2_PLACEMENT_3D ( 'NONE', #10687, #105, #3655 ) ;
#3972=CARTESIAN_POINT ( 'NONE',  ( 26.17093350124942219, 5.000000000000000888, -137.7213801722282653 ) ) ;
#3976=CARTESIAN_POINT ( 'NONE',  ( -0.9552437115555381109, 15.00000000000000711, -125.6272940116446364 ) ) ;
#3978=CARTESIAN_POINT ( 'NONE',  ( -4.665009673976214799, 5.000000000003948841, -129.3402154207116155 ) ) ;
#3979=CARTESIAN_POINT ( 'NONE',  ( 3.294401254219998965, 1.734723475976807094E-15, -113.2772910607207848 ) ) ;
#3981=DIRECTION ( 'NONE',  ( -0.02181900108494707127, 0.000000000000000000, 0.9997619372588930631 ) ) ;
#3989=ORIENTED_EDGE ( 'NONE', *, *, #7231, .T. ) ;
#3995=CARTESIAN_POINT ( 'NONE',  ( 0.000000000000000000, 9.999999999999998224, -100.6237003951525679 ) ) ;
#3996=CARTESIAN_POINT ( 'NONE',  ( 13.21422700454708909, 13.96506978500478802, -126.0492241132350415 ) ) ;
#4002=EDGE_LOOP ( 'NONE', ( #7512, #4853, #14242, #10312 ) ) ;
#4007=AXIS2_PLACEMENT_3D ( 'NONE', #1898, #2906, #1823 ) ;
#4014=CARTESIAN_POINT ( 'NONE',  ( 9.971950858281140029, 8.773889247172311556, -44.63331069169930032 ) ) ;
#4021=CARTESIAN_POINT ( 'NONE',  ( 4.544676675852343806, 6.000000000000000000, -126.1782412829290934 ) ) ;
#4023=CARTESIAN_POINT ( 'NONE',  ( 10.62587365868640710, 14.24122074427556583, -106.5450489676481283 ) ) ;
#4027=EDGE_CURVE ( 'NONE', #6914, #9763, #10384, .T. ) ;
#4032=CARTESIAN_POINT ( 'NONE',  ( 12.77611550990255829, 4.050274393866083678, -166.6173057128717687 ) ) ;
#4035=CARTESIAN_POINT ( 'NONE',  ( -30.46290170330349056, 4.000000000000174971, -196.8214803422608270 ) ) ;
#4037=CARTESIAN_POINT ( 'NONE',  ( 8.894904190497955554, 4.261448547226525996, 2.831834529235428999 ) ) ;
#4040=CARTESIAN_POINT ( 'NONE',  ( 10.32040002734022188, 15.00000000000000000, -106.4311084481271763 ) ) ;
#4041=CARTESIAN_POINT ( 'NONE',  ( -20.62911563925012359, 8.673617379884035472E-16, -191.9171239689855781 ) ) ;
#4051=B_SPLINE_CURVE_WITH_KNOTS ( 'NONE', 3,
 ( #4479, #15239, #1077, #9188, #8028, #9342 ),
 .UNSPECIFIED., .F., .F.,
 ( 4, 2, 4 ),
 ( 1.398578778534940505E-17, 0.001339092541177541208, 0.002678185082355068539 ),
 .UNSPECIFIED. ) ;
#4053=EDGE_CURVE ( 'NONE', #3728, #16, #12965, .T. ) ;
#4054=EDGE_CURVE ( 'NONE', #9168, #8798, #4661, .T. ) ;
#4059=CARTESIAN_POINT ( 'NONE',  ( -9.756303285186646690, 6.071532165918825619E-15, -116.2179163664056176 ) ) ;
#4060=CARTESIAN_POINT ( 'NONE',  ( 8.300023318320116417, 5.000000000000000888, -113.4762057881877553 ) ) ;
#4067=CARTESIAN_POINT ( 'NONE',  ( 8.937017960089326252, 10.66147458959636296, 2.788040780850042921 ) ) ;
#4074=AXIS2_PLACEMENT_3D ( 'NONE', #6784, #8085, #1364 ) ;
#4075=CARTESIAN_POINT ( 'NONE',  ( -5.309262520577839872, 13.40945642053105225, -125.0911079416483176 ) ) ;
#4076=B_SPLINE_CURVE_WITH_KNOTS ( 'NONE', 3,
 ( #3886, #7426, #14563, #13550, #2950, #12525 ),
 .UNSPECIFIED., .F., .F.,
 ( 4, 2, 4 ),
 ( 0.000000000000000000, 0.01347348681404525635, 0.02694697362809051269 ),
 .UNSPECIFIED. ) ;
#4081=ORIENTED_EDGE ( 'NONE', *, *, #9105, .F. ) ;
#4088=CYLINDRICAL_SURFACE ( 'NONE', #9871, 1.000000000000028644 ) ;
#4090=( BOUNDED_SURFACE ( )  B_SPLINE_SURFACE ( 3, 2, ( 
 ( #4258, #7570, #13618 ),
 ( #2940, #11280, #14862 ),
 ( #13761, #7726, #3157 ),
 ( #1628, #6341, #11055 ) ),
 .UNSPECIFIED., .F., .F., .F. ) 
 B_SPLINE_SURFACE_WITH_KNOTS ( ( 4, 4 ),
 ( 3, 3 ),
 ( 4.517782591535513426, 4.712388980384689674 ),
 ( 0.000000000000000000, 1.000000000000000000 ),
 .UNSPECIFIED. ) 
 GEOMETRIC_REPRESENTATION_ITEM ( )  RATIONAL_B_SPLINE_SURFACE ( (
 ( 1.000000000000000000, 0.9811261306835552531, 1.000000000000000000),
 ( 1.000000000000000000, 0.9936732040629523421, 1.000000000000000000),
 ( 1.000000000000000000, 1.000004256428960625, 1.000000000000000000),
 ( 1.000000000000000000, 1.000000000000000000, 1.000000000000000000) ) ) 
 REPRESENTATION_ITEM ( '' )  SURFACE ( )  );
#4111=CARTESIAN_POINT ( 'NONE',  ( 12.51486264971105733, 2.933442265364648804, -166.3745327125327833 ) ) ;
#4112=CARTESIAN_POINT ( 'NONE',  ( 9.173792667211671414, 1.005434785423204858, -106.2279553762535755 ) ) ;
#4113=CARTESIAN_POINT ( 'NONE',  ( -29.53813527096436431, 1.100700607699333011E-12, -197.6188592682773333 ) ) ;
#4127=CARTESIAN_POINT ( 'NONE',  ( 11.00345249570077044, 12.49999999999999822, -46.06582701958618742 ) ) ;
#4134=CARTESIAN_POINT ( 'NONE',  ( 4.532353106082944727, 1.734723475976807094E-15, -107.9759262171523204 ) ) ;
#4136=CARTESIAN_POINT ( 'NONE',  ( 10.99551757066058322, 11.56847231179307478, -45.70224318734323532 ) ) ;
#4139=CARTESIAN_POINT ( 'NONE',  ( 8.946941325060613792, 11.53387151411719103, 2.333345235934940476 ) ) ;
#4146=AXIS2_PLACEMENT_3D ( 'NONE', #14662, #4285, #1957 ) ;
#4151=CARTESIAN_POINT ( 'NONE',  ( -7.409205697916631195, 14.09412780555631706, -116.8849570398035240 ) ) ;
#4153=CARTESIAN_POINT ( 'NONE',  ( 8.110048856218389446, 15.00000000000000000, -122.2108563474139800 ) ) ;
#4166=CARTESIAN_POINT ( 'NONE',  ( 26.13050938914192756, 4.000000000000000000, -138.2605953772281566 ) ) ;
#4172=CARTESIAN_POINT ( 'NONE',  ( -0.7311112071359824327, 9.999999999999996447, -104.2753208119124366 ) ) ;
#4177=CARTESIAN_POINT ( 'NONE',  ( -8.648486276335429324, 2.383983337347815201, -115.6868502166757651 ) ) ;
#4178=ORIENTED_EDGE ( 'NONE', *, *, #8436, .T. ) ;
#4179=CARTESIAN_POINT ( 'NONE',  ( 1.243260443319662123, 4.000000000000000000, -139.4020581015306846 ) ) ;
#4182=CARTESIAN_POINT ( 'NONE',  ( 11.29845382488883310, 0.7750707670031977692, -164.8261590475616742 ) ) ;
#4184=CARTESIAN_POINT ( 'NONE',  ( -23.05980621591842450, 8.673617379884035472E-16, -178.1170512941666573 ) ) ;
#4185=CARTESIAN_POINT ( 'NONE',  ( 10.12997330464346568, 0.1923925221388024520, -164.1683766026968669 ) ) ;
#4191=CARTESIAN_POINT ( 'NONE',  ( 7.591307135477617152, 0.1275065550641042156, -105.3485349477005570 ) ) ;
#4208=CARTESIAN_POINT ( 'NONE',  ( 4.999961331844611223, 1.213798585976041210E-15, -31.08261130664305938 ) ) ;
#4209=ORIENTED_EDGE ( 'NONE', *, *, #7305, .T. ) ;
#4210=CARTESIAN_POINT ( 'NONE',  ( 8.957197456629506505, 11.99561947282018437, 1.863402092058872528 ) ) ;
#4211=CARTESIAN_POINT ( 'NONE',  ( 2.860422134859788024, 14.99999999999999645, -108.4900984580837502 ) ) ;
#4221=CARTESIAN_POINT ( 'NONE',  ( -24.61436772009224327, 4.000000000000000000, -208.9121151917288728 ) ) ;
#4222=CARTESIAN_POINT ( 'NONE',  ( -9.486278975406271741, 11.85996688994955939, -115.8846352400755819 ) ) ;
#4223=EDGE_CURVE ( 'NONE', #13403, #6054, #2978, .T. ) ;
#4224=MECHANICAL_CONTEXT ( 'NONE', #12422, 'mechanical' ) ;
#4225=CARTESIAN_POINT ( 'NONE',  ( 6.088601725813743037, 15.00000000000000000, -116.7323803970391225 ) ) ;
#4226=CARTESIAN_POINT ( 'NONE',  ( 24.58980970989934534, 1.007048232791107889, -138.5289917632123888 ) ) ;
#4228=CIRCLE ( 'NONE', #1243, 1.000000000000000888 ) ;
#4230=CARTESIAN_POINT ( 'NONE',  ( -5.778809769431745735, 4.000000000000000000, -144.4900924413740313 ) ) ;
#4232=VECTOR ( 'NONE', #544, 1000.000000000000000 ) ;
#4233=EDGE_LOOP ( 'NONE', ( #4829, #12087, #3146, #6571, #4825, #828, #68, #2833, #2347, #3044, #1365, #8345 ) ) ;
#4244=CARTESIAN_POINT ( 'NONE',  ( 0.5944212552585367293, 6.000000000000000000, -138.5540974747773930 ) ) ;
#4252=CARTESIAN_POINT ( 'NONE',  ( 10.98443295445820134, 13.18102764312297381, -107.0804917692757812 ) ) ;
#4255=CARTESIAN_POINT ( 'NONE',  ( -7.548446295636292547, 1.142345851352394304, -116.1647996692329343 ) ) ;
#4256=DIRECTION ( 'NONE',  ( 0.9989498407774362043, 0.000000000000000000, 0.04581719776170026237 ) ) ;
#4258=CARTESIAN_POINT ( 'NONE',  ( 4.033098156699469250, 0.09438068890153242241, -1.663700395152505118 ) ) ;
#4260=CARTESIAN_POINT ( 'NONE',  ( 5.826207324873307059, 15.00000000000000711, -114.9748398223660075 ) ) ;
#4261=CARTESIAN_POINT ( 'NONE',  ( 11.32016196459912649, 12.49999999999999822, -106.4092894470390291 ) ) ;
#4263=CARTESIAN_POINT ( 'NONE',  ( -30.57574746150116596, 4.000000000000477840, -189.7345312606148582 ) ) ;
#4268=CYLINDRICAL_SURFACE ( 'NONE', #1091, 1.000000000000042633 ) ;
#4269=CARTESIAN_POINT ( 'NONE',  ( 10.04877821836624996, 1.662336431860132357, -106.0315262505607450 ) ) ;
#4271=CARTESIAN_POINT ( 'NONE',  ( -15.55390927925940758, 8.673617379884033500E-16, -185.3651796119466439 ) ) ;
#4272=CARTESIAN_POINT ( 'NONE',  ( -3.294555838739222420, 5.000000000000000888, -108.9576586820894732 ) ) ;
#4283=CARTESIAN_POINT ( 'NONE',  ( -7.751437813422534795, 5.000000000000000000, -124.5369783794910319 ) ) ;
#4284=ORIENTED_EDGE ( 'NONE', *, *, #13361, .F. ) ;
#4285=DIRECTION ( 'NONE',  ( 0.000000000000000000, 1.000000000000000000, 0.000000000000000000 ) ) ;
#4287=CARTESIAN_POINT ( 'NONE',  ( 13.63124210137304537, 12.50000000000000000, -125.8318412418369121 ) ) ;
#4289=AXIS2_PLACEMENT_3D ( 'NONE', #4021, #10971, #9811 ) ;
#4294=CARTESIAN_POINT ( 'NONE',  ( 9.940211158120410673, 12.49999999999999645, -43.17897536272746351 ) ) ;
#4297=CARTESIAN_POINT ( 'NONE',  ( -9.385448347264278013, 10.00000000000000000, -115.3551636530117293 ) ) ;
#4298=VECTOR ( 'NONE', #11292, 1000.000000000000000 ) ;
#4301=CARTESIAN_POINT ( 'NONE',  ( 9.815018941082433557, 15.00000000000000000, -124.9446060552849218 ) ) ;
#4302=DIRECTION ( 'NONE',  ( 0.000000000000000000, 0.000000000000000000, 1.000000000000000000 ) ) ;
#4303=CARTESIAN_POINT ( 'NONE',  ( 26.71007981443008816, 5.000000000000001776, -136.8791680534697832 ) ) ;
#4308=EDGE_LOOP ( 'NONE', ( #2280, #4637, #4365, #2926, #12759, #7898, #4449 ) ) ;
#4309=EDGE_CURVE ( 'NONE', #8407, #10451, #14251, .T. ) ;
#4318=CARTESIAN_POINT ( 'NONE',  ( 22.16272538625586108, 5.000000000000000888, -133.7353905083487575 ) ) ;
#4324=CARTESIAN_POINT ( 'NONE',  ( 10.74700110368927675, 13.76866009450032458, -106.9415428707061295 ) ) ;
#4325=ADVANCED_FACE ( 'NONE', ( #1183 ), #5885, .F. ) ;
#4329=CARTESIAN_POINT ( 'NONE',  ( -6.442579204135247650, 0.4622145201094847722, -116.6257450304696874 ) ) ;
#4330=VERTEX_POINT ( 'NONE', #2658 ) ;
#4331=CARTESIAN_POINT ( 'NONE',  ( -4.580007248825209487, 7.420008617947661109E-16, -117.4298695725520929 ) ) ;
#4334=CARTESIAN_POINT ( 'NONE',  ( 6.147223190827659778, 15.00000000000000000, -110.9794920126036004 ) ) ;
#4335=DIRECTION ( 'NONE',  ( -0.02181900108494679719, 0.000000000000000000, 0.9997619372588931741 ) ) ;
#4337=CARTESIAN_POINT ( 'NONE',  ( -29.65136226273812170, 8.190558003531155927E-13, -196.7288660786858827 ) ) ;
#4341=VERTEX_POINT ( 'NONE', #2418 ) ;
#4343=CARTESIAN_POINT ( 'NONE',  ( 6.288457687488933523, 0.000000000000000000, -105.0111312234435985 ) ) ;
#4344=EDGE_CURVE ( 'NONE', #11904, #5461, #11837, .T. ) ;
#4346=CARTESIAN_POINT ( 'NONE',  ( 8.942877807459197470, 11.25919951447419010, 2.519538463272103179 ) ) ;
#4347=CARTESIAN_POINT ( 'NONE',  ( -4.869293993580057212, 1.734723475976807094E-15, -118.1204535358569530 ) ) ;
#4350=CARTESIAN_POINT ( 'NONE',  ( 10.95001698349728336, 5.943472311793079221, -43.61737436169475046 ) ) ;
#4351=CYLINDRICAL_SURFACE ( 'NONE', #509, 3.000000000000011990 ) ;
#4359=CARTESIAN_POINT ( 'NONE',  ( 10.95001698349729047, 5.943472311793079221, -43.61737436169475046 ) ) ;
#4360=CARTESIAN_POINT ( 'NONE',  ( 8.672589136283018973, 12.50000000000000000, -116.8319891675733828 ) ) ;
#4363=EDGE_CURVE ( 'NONE', #11204, #14187, #5684, .T. ) ;
#4365=ORIENTED_EDGE ( 'NONE', *, *, #8374, .F. ) ;
#4372=CARTESIAN_POINT ( 'NONE',  ( 11.32055997317818985, 15.00000000000186517, -122.6997364776348576 ) ) ;
#4373=CARTESIAN_POINT ( 'NONE',  ( -5.599106598293994708, 14.85395790697270257, -117.2453520682029904 ) ) ;
#4378=CARTESIAN_POINT ( 'NONE',  ( -1.713579061006052839, 4.000000000000000000, -141.3534686916246983 ) ) ;
#4380=VECTOR ( 'NONE', #10226, 1000.000000000000000 ) ;
#4382=CARTESIAN_POINT ( 'NONE',  ( -9.385448347264265578, 10.35017622395433357, -115.3551636530117719 ) ) ;
#4386=CARTESIAN_POINT ( 'NONE',  ( -25.63704293604745743, 1.707693810710474880, -207.0033111944292727 ) ) ;
#4390=DIRECTION ( 'NONE',  ( -0.02181900108494696719, 0.000000000000000000, 0.9997619372588931741 ) ) ;
#4393=CARTESIAN_POINT ( 'NONE',  ( 11.04730217088350663, 12.49999999999999822, -107.1178495010082941 ) ) ;
#4398=CARTESIAN_POINT ( 'NONE',  ( -9.721966606378854792, 4.649066463566643215, -116.3614657639810019 ) ) ;
#4400=CARTESIAN_POINT ( 'NONE',  ( -24.61436772009224327, 4.000000000000000000, -208.9121151917288728 ) ) ;
#4403=CARTESIAN_POINT ( 'NONE',  ( 5.907106717946758678, 3.280814621631571004, 4.948311739797290443 ) ) ;
#4409=CARTESIAN_POINT ( 'NONE',  ( 3.717577911061880958, 0.000000000000000000, -143.6771719914432879 ) ) ;
#4412=CARTESIAN_POINT ( 'NONE',  ( 6.223671794703586890, 13.99084746319145722, 3.305819595603176175 ) ) ;
#4413=FACE_OUTER_BOUND ( 'NONE', #11190, .T. ) ;
#4415=CARTESIAN_POINT ( 'NONE',  ( 16.38488885224993652, 8.673617379884035472E-16, -147.4012479123365154 ) ) ;
#4417=LINE ( 'NONE', #3334, #9721 ) ;
#4418=AXIS2_PLACEMENT_3D ( 'NONE', #14864, #7729, #631 ) ;
#4419=DIRECTION ( 'NONE',  ( 0.000000000000000000, 0.000000000000000000, 1.000000000000000000 ) ) ;
#4427=CARTESIAN_POINT ( 'NONE',  ( 26.58801926426209405, 5.000000000000000888, -139.0072983920785532 ) ) ;
#4428=DIRECTION ( 'NONE',  ( 0.000000000000000000, 1.000000000000000000, 0.000000000000000000 ) ) ;
#4429=ORIENTED_EDGE ( 'NONE', *, *, #14828, .F. ) ;
#4431=CARTESIAN_POINT ( 'NONE',  ( 5.000000000000000888, 15.00000000000000000, -100.6237003951525679 ) ) ;
#4435=ORIENTED_EDGE ( 'NONE', *, *, #11584, .T. ) ;
#4440=CARTESIAN_POINT ( 'NONE',  ( -7.978007822725404097, 13.46737988729077706, -115.9805901612444927 ) ) ;
#4443=CARTESIAN_POINT ( 'NONE',  ( 10.31224696304875010, 12.49999999999999822, -121.0233796644210429 ) ) ;
#4444=CARTESIAN_POINT ( 'NONE',  ( -9.721966606378853015, 10.35093353643332570, -116.3614657639809309 ) ) ;
#4445=ORIENTED_EDGE ( 'NONE', *, *, #14746, .F. ) ;
#4446=CARTESIAN_POINT ( 'NONE',  ( 20.87131526946576443, 1.301042606982605321E-15, -138.9752963459259547 ) ) ;
#4449=ORIENTED_EDGE ( 'NONE', *, *, #7718, .T. ) ;
#4451=CARTESIAN_POINT ( 'NONE',  ( 16.43549277046052026, 8.749999999999998224, -88.72346770343305877 ) ) ;
#4454=VERTEX_POINT ( 'NONE', #5125 ) ;
#4456=CARTESIAN_POINT ( 'NONE',  ( -8.256868333794654902, 13.15908446542855970, -115.8592241392984477 ) ) ;
#4460=CARTESIAN_POINT ( 'NONE',  ( -25.11906781955737600, 1.301042606982605321E-15, -198.9681998140721078 ) ) ;
#4461=CARTESIAN_POINT ( 'NONE',  ( 1.050483441592383604, -6.071532165918824042E-15, -129.2792135173282873 ) ) ;
#4464=CARTESIAN_POINT ( 'NONE',  ( 9.195819311509541905, 5.000000000000000888, -109.7388120284761897 ) ) ;
#4469=DIRECTION ( 'NONE',  ( 0.01091012466144563632, -0.002150395083030232687, -0.9999381705789908148 ) ) ;
#4478=PRODUCT_DEFINITION_SHAPE ( 'NONE', 'NONE',  #2439 ) ;
#4479=CARTESIAN_POINT ( 'NONE',  ( 10.00087860767147063, 5.000000000000000888, -45.95880046359209103 ) ) ;
#4482=FACE_OUTER_BOUND ( 'NONE', #3091, .T. ) ;
#4490=CARTESIAN_POINT ( 'NONE',  ( -25.44041662983336849, 3.773872472838732506, -208.9707249988738340 ) ) ;
#4491=CARTESIAN_POINT ( 'NONE',  ( 6.146471803482498331, 12.22506747196939614, 4.769516544308691763 ) ) ;
#4493=CARTESIAN_POINT ( 'NONE',  ( -9.721966606379332632, 5.000000000000002665, -116.3614657639789414 ) ) ;
#4497=DIRECTION ( 'NONE',  ( 0.000000000000000000, -0.9314983497198060514, 0.3637455490714327500 ) ) ;
#4498=CARTESIAN_POINT ( 'NONE',  ( -6.525249091262845802, 11.54687804473151758, -124.9828182402523851 ) ) ;
#4507=CARTESIAN_POINT ( 'NONE',  ( -6.345149115697418019, 2.442921369471867893E-15, -181.1746449140297841 ) ) ;
#4513=VECTOR ( 'NONE', #2343, 1000.000000000000114 ) ;
#4524=ORIENTED_EDGE ( 'NONE', *, *, #14346, .T. ) ;
#4525=AXIS2_PLACEMENT_3D ( 'NONE', #846, #6857, #13753 ) ;
#4526=CARTESIAN_POINT ( 'NONE',  ( 25.85064958816917624, 2.055286875431564297, -138.3708915003257971 ) ) ;
#4528=ORIENTED_EDGE ( 'NONE', *, *, #10366, .T. ) ;
#4531=DIRECTION ( 'NONE',  ( -0.02181900108494707127, -0.000000000000000000, 0.9997619372588931741 ) ) ;
#4534=ORIENTED_EDGE ( 'NONE', *, *, #8545, .F. ) ;
#4535=CARTESIAN_POINT ( 'NONE',  ( -9.385448347264267355, 9.999999999999998224, -115.3551636530117150 ) ) ;
#4542=DIRECTION ( 'NONE',  ( 0.000000000000000000, 0.000000000000000000, 1.000000000000000000 ) ) ;
#4543=CARTESIAN_POINT ( 'NONE',  ( -0.8977508794915173285, -8.673617379884037444E-16, -125.7548904922300181 ) ) ;
#4548=VECTOR ( 'NONE', #789, 1000.000000000000000 ) ;
#4550=DIRECTION ( 'NONE',  ( -0.000000000000000000, 1.000000000000000000, -0.000000000000000000 ) ) ;
#4554=CARTESIAN_POINT ( 'NONE',  ( -1.871645213090456616, 5.000000000000011546, -133.9039370687633834 ) ) ;
#4561=CARTESIAN_POINT ( 'NONE',  ( 8.783361249427379391, 3.744510042675810446, 2.765904461544427928 ) ) ;
#4568=CARTESIAN_POINT ( 'NONE',  ( 6.257758434032409944, 14.35016516265838682, 2.760946016300349637 ) ) ;
#4569=CARTESIAN_POINT ( 'NONE',  ( -2.027137927705678688, 3.249798772148220769E-12, -107.0032022125478761 ) ) ;
#4575=CARTESIAN_POINT ( 'NONE',  ( -5.538366777589915912, 13.14664760303528901, -125.0671679570068164 ) ) ;
#4576=( BOUNDED_SURFACE ( )  B_SPLINE_SURFACE ( 3, 1, ( 
 ( #3262, #14886 ),
 ( #12850, #2111 ),
 ( #10152, #4283 ),
 ( #6816, #8989 ) ),
 .UNSPECIFIED., .F., .F., .F. ) 
 B_SPLINE_SURFACE_WITH_KNOTS ( ( 4, 4 ),
 ( 2, 2 ),
 ( 0.000000000000000000, 1.000000000000000000 ),
 ( 0.000000000000000000, 1.000000000000000000 ),
 .UNSPECIFIED. ) 
 GEOMETRIC_REPRESENTATION_ITEM ( )  RATIONAL_B_SPLINE_SURFACE ( (
 ( 1.000000000000000000, 1.000000000000000000),
 ( 0.8750842653720394271, 0.8750842653720394271),
 ( 0.8750842653720394271, 0.8750842653720394271),
 ( 1.000000000000000000, 1.000000000000000000) ) ) 
 REPRESENTATION_ITEM ( '' )  SURFACE ( )  );
#4585=CARTESIAN_POINT ( 'NONE',  ( 8.820757121451897831, 15.00000000000000000, -106.4638369497514105 ) ) ;
#4589=ORIENTED_EDGE ( 'NONE', *, *, #412, .T. ) ;
#4596=DIRECTION ( 'NONE',  ( -0.000000000000000000, -1.000000000000000000, 0.000000000000000000 ) ) ;
#4599=EDGE_CURVE ( 'NONE', #5461, #3224, #8152, .T. ) ;
#4609=CARTESIAN_POINT ( 'NONE',  ( 6.208467851984790009, 13.77618473890310291, 3.570604971030389319 ) ) ;
#4612=CARTESIAN_POINT ( 'NONE',  ( -25.60675101229562500, 1.982032305613783407, -207.4180151373524268 ) ) ;
#4614=CARTESIAN_POINT ( 'NONE',  ( 6.012727666029630491, 15.00000000000000000, -116.3088615718675385 ) ) ;
#4617=FACE_OUTER_BOUND ( 'NONE', #11386, .T. ) ;
#4621=CARTESIAN_POINT ( 'NONE',  ( 9.884674853941351813, 8.773889247172311556, -40.63426294266372452 ) ) ;
#4626=CARTESIAN_POINT ( 'NONE',  ( -8.628312869877936109, 5.000000000000000888, -120.2932534013991130 ) ) ;
#4632=ORIENTED_EDGE ( 'NONE', *, *, #11230, .F. ) ;
#4637=ORIENTED_EDGE ( 'NONE', *, *, #1168, .T. ) ;
#4639=CARTESIAN_POINT ( 'NONE',  ( -25.48272420619116474, 0.09695822977917610552, -201.3338006394713204 ) ) ;
#4640=CARTESIAN_POINT ( 'NONE',  ( 8.987202726980132894, 12.50000000278589596, 0.4885395538092229262 ) ) ;
#4647=CARTESIAN_POINT ( 'NONE',  ( 25.31442990777252433, 1.743671408225548891, -137.3942114566015675 ) ) ;
#4652=ORIENTED_EDGE ( 'NONE', *, *, #7305, .F. ) ;
#4654=CARTESIAN_POINT ( 'NONE',  ( -5.617373260391812728, 0.000000000000000000, -174.7795128502804403 ) ) ;
#4660=CIRCLE ( 'NONE', #4418, 4.999999999999995559 ) ;
#4661=B_SPLINE_CURVE_WITH_KNOTS ( 'NONE', 3,
 ( #5147, #12480, #7461, #14594, #1822, #12176, #1595, #3996, #9859, #6611, #12401, #11090 ),
 .UNSPECIFIED., .F., .F.,
 ( 4, 2, 2, 2, 2, 4 ),
 ( 1.734723475976807094E-18, 0.001027444902010466940, 0.002054889804020932145, 0.003082334706031397351, 0.003596057157036637326, 0.004109779608041877301 ),
 .UNSPECIFIED. ) ;
#4664=CARTESIAN_POINT ( 'NONE',  ( 16.10717976051956413, 8.673617379884033500E-16, -135.3045475799466999 ) ) ;
#4673=ORIENTED_EDGE ( 'NONE', *, *, #6874, .T. ) ;
#4678=CARTESIAN_POINT ( 'NONE',  ( 6.134605308603925167, 11.61845493593924417, 5.022560416558600416 ) ) ;
#4680=EDGE_CURVE ( 'NONE', #7347, #1934, #7406, .T. ) ;
#4682=CARTESIAN_POINT ( 'NONE',  ( -25.62274278772851943, 0.2453806450821310603, -202.6740962663072025 ) ) ;
#4692=ADVANCED_FACE ( 'NONE', ( #2178 ), #4351, .T. ) ;
#4695=CARTESIAN_POINT ( 'NONE',  ( -6.790153584124040798, 13.40945642053105225, -124.9643354754709748 ) ) ;
#4701=CARTESIAN_POINT ( 'NONE',  ( 1.243260443319662123, 4.000000000000000000, -139.4020581015306846 ) ) ;
#4704=VECTOR ( 'NONE', #7157, 1000.000000000000000 ) ;
#4706=CARTESIAN_POINT ( 'NONE',  ( 9.044950117654433797, 6.000000000000000000, -137.9826476090360643 ) ) ;
#4707=ORIENTED_EDGE ( 'NONE', *, *, #3062, .T. ) ;
#4708=CARTESIAN_POINT ( 'NONE',  ( -22.51849958723530776, 8.673617379884035472E-16, -204.9231702217275028 ) ) ;
#4713=ORIENTED_EDGE ( 'NONE', *, *, #1256, .F. ) ;
#4726=CARTESIAN_POINT ( 'NONE',  ( 25.05271902006223783, 1.500039406472921222, -137.4898610820562510 ) ) ;
#4731=ORIENTED_EDGE ( 'NONE', *, *, #1491, .F. ) ;
#4732=VERTEX_POINT ( 'NONE', #3335 ) ;
#4734=CARTESIAN_POINT ( 'NONE',  ( 6.162973360166584591, 8.673617379884035472E-16, -165.1928244853837384 ) ) ;
#4737=VERTEX_POINT ( 'NONE', #14880 ) ;
#4738=CARTESIAN_POINT ( 'NONE',  ( -6.679542461294181166, 0.5769591943446209514, -116.5285319886242803 ) ) ;
#4740=FACE_OUTER_BOUND ( 'NONE', #1661, .T. ) ;
#4745=CARTESIAN_POINT ( 'NONE',  ( 10.54086443187302891, 12.49999999999999822, -107.6778029779925276 ) ) ;
#4748=DIRECTION ( 'NONE',  ( -0.000000000000000000, -1.000000000000000000, -0.000000000000000000 ) ) ;
#4749=ORIENTED_EDGE ( 'NONE', *, *, #5370, .F. ) ;
#4750=ORIENTED_EDGE ( 'NONE', *, *, #6495, .T. ) ;
#4755=CARTESIAN_POINT ( 'NONE',  ( 4.246495378555050770, 14.99999999999999822, -105.2373590921481536 ) ) ;
#4756=( BOUNDED_SURFACE ( )  B_SPLINE_SURFACE ( 3, 1, ( 
 ( #6377, #4695 ),
 ( #3535, #9935 ),
 ( #9410, #8243 ),
 ( #14671, #4075 ) ),
 .UNSPECIFIED., .F., .F., .F. ) 
 B_SPLINE_SURFACE_WITH_KNOTS ( ( 4, 4 ),
 ( 2, 2 ),
 ( 0.000000000000000000, 1.000000000000000000 ),
 ( 0.000000000000000000, 1.000000000000000000 ),
 .UNSPECIFIED. ) 
 GEOMETRIC_REPRESENTATION_ITEM ( )  RATIONAL_B_SPLINE_SURFACE ( (
 ( 1.000000000000000000, 1.000000000000000000),
 ( 0.9998070924708732932, 0.9998070924708732932),
 ( 0.9998070924708732932, 0.9998070924708732932),
 ( 1.000000000000000000, 1.000000000000000000) ) ) 
 REPRESENTATION_ITEM ( '' )  SURFACE ( )  );
#4759=CARTESIAN_POINT ( 'NONE',  ( 3.863626520209246795, -4.336808689942017736E-15, -133.2112599781813174 ) ) ;
#4760=AXIS2_PLACEMENT_3D ( 'NONE', #768, #917, #3080 ) ;
#4761=CARTESIAN_POINT ( 'NONE',  ( 7.865309076558498091, 15.00000000000000000, -121.7325209303464959 ) ) ;
#4763=DIRECTION ( 'NONE',  ( -0.02181900108494737658, 0.000000000000000000, 0.9997619372588931741 ) ) ;
#4769=CARTESIAN_POINT ( 'NONE',  ( 1.114947364559091492, 5.000000000000000888, -139.4079432275549948 ) ) ;
#4771=CARTESIAN_POINT ( 'NONE',  ( 29.28282515376967865, 8.773889247172311556, -47.21258073259075871 ) ) ;
#4773=CARTESIAN_POINT ( 'NONE',  ( 6.599362577383862671, 5.362371901635187827E-13, -105.1339869880811477 ) ) ;
#4781=CARTESIAN_POINT ( 'NONE',  ( 5.249698980305105955, 0.08115359711835153089, 1.152527031878756159 ) ) ;
#4783=EDGE_CURVE ( 'NONE', #11984, #14278, #13325, .T. ) ;
#4788=UNCERTAINTY_MEASURE_WITH_UNIT (LENGTH_MEASURE( 1.000000000000000082E-05 ), #12712, 'distance_accuracy_value', 'NONE');
#4795=CARTESIAN_POINT ( 'NONE',  ( -1.885039096047290252, 8.673617379884034486E-16, -115.1740262261674843 ) ) ;
#4802=AXIS2_PLACEMENT_3D ( 'NONE', #9751, #10818, #9900 ) ;
#4807=VERTEX_POINT ( 'NONE', #6960 ) ;
#4814=CARTESIAN_POINT ( 'NONE',  ( -4.907357056062867429, 4.733476084610204568E-16, -117.3740583286320884 ) ) ;
#4818=CARTESIAN_POINT ( 'NONE',  ( 5.292461965453085782, 8.673617379884045333E-16, -106.4530418762676476 ) ) ;
#4820=CARTESIAN_POINT ( 'NONE',  ( 11.00064054493036458, 5.000000000000000888, -45.93698146250716263 ) ) ;
#4823=CARTESIAN_POINT ( 'NONE',  ( 10.02128254437710098, 12.49999999999999822, -108.3753986617891343 ) ) ;
#4824=CARTESIAN_POINT ( 'NONE',  ( 13.25562203920985382, 8.452217897303065567E-13, -125.4200107874790717 ) ) ;
#4825=ORIENTED_EDGE ( 'NONE', *, *, #648, .F. ) ;
#4827=CARTESIAN_POINT ( 'NONE',  ( 17.54434971314415037, 8.749999999999998224, -93.70045838864260190 ) ) ;
#4828=ORIENTED_EDGE ( 'NONE', *, *, #6609, .F. ) ;
#4829=ORIENTED_EDGE ( 'NONE', *, *, #14544, .F. ) ;
#4834=CARTESIAN_POINT ( 'NONE',  ( -1.499260709786591317, 9.999999999999998224, -106.0110764665439547 ) ) ;
#4837=CARTESIAN_POINT ( 'NONE',  ( 12.48509882908383872, 2.151549674844647431, -165.6960548549982946 ) ) ;
#4844=B_SPLINE_CURVE_WITH_KNOTS ( 'NONE', 3,
 ( #9081, #4444, #11323, #14904, #7919, #12790, #896, #2128, #11624, #6616, #9157, #5670, #6831, #10172, #4373, #9233, #13885, #13732 ),
 .UNSPECIFIED., .F., .F.,
 ( 4, 2, 2, 2, 2, 2, 2, 2, 4 ),
 ( 0.000000000000000000, 0.001051779247122088066, 0.002103558494244176132, 0.003155337741366264197, 0.004207116988488352263, 0.005258896235610439895, 0.006310675482732528395, 0.007362454729854616894, 0.008414233976976704527 ),
 .UNSPECIFIED. ) ;
#4845=EDGE_CURVE ( 'NONE', #11140, #273, #995, .T. ) ;
#4847=CYLINDRICAL_SURFACE ( 'NONE', #6943, 5.000000000000000000 ) ;
#4849=CARTESIAN_POINT ( 'NONE',  ( 9.502539846137461055, 1.145151035800988648, -106.1191373047704190 ) ) ;
#4852=DIRECTION ( 'NONE',  ( 0.9989498407774362043, 0.000000000000000000, 0.04581719776170026237 ) ) ;
#4853=ORIENTED_EDGE ( 'NONE', *, *, #4599, .T. ) ;
#4854=CARTESIAN_POINT ( 'NONE',  ( 7.659091881109533873, 1.637990805669089056, 2.041194214175461763 ) ) ;
#4861=CARTESIAN_POINT ( 'NONE',  ( 14.22910372453204353, 6.000000000000000000, -126.5134921567817941 ) ) ;
#4862=CARTESIAN_POINT ( 'NONE',  ( 10.03403318997453297, 14.68779660170870649, -106.1276578890943085 ) ) ;
#4874=CARTESIAN_POINT ( 'NONE',  ( 8.935548306746154523, 5.000000000000000888, 2.855381328098136162 ) ) ;
#4886=CARTESIAN_POINT ( 'NONE',  ( -4.234402844927158682, 4.336808689942017736E-16, -117.4888040839639558 ) ) ;
#4892=CARTESIAN_POINT ( 'NONE',  ( 8.432993291281569270, 8.673617379884034486E-16, -127.3575301229172538 ) ) ;
#4894=CARTESIAN_POINT ( 'NONE',  ( -4.658423462441079188, 15.00000000000000355, -116.0378842123784153 ) ) ;
#4895=CARTESIAN_POINT ( 'NONE',  ( -4.665009674110688564, 6.318137159033122024E-12, -129.3402154207890362 ) ) ;
#4896=CARTESIAN_POINT ( 'NONE',  ( 18.82489474304439270, 0.000000000000000000, -131.0518286717526735 ) ) ;
#4900=ORIENTED_EDGE ( 'NONE', *, *, #8545, .T. ) ;
#4902=CARTESIAN_POINT ( 'NONE',  ( 25.92962511641389156, 2.144787619503913501, -138.3608807550390907 ) ) ;
#4906=CARTESIAN_POINT ( 'NONE',  ( 6.182874915598739918, 13.31144022244639658, 4.038793072555847630 ) ) ;
#4909=CARTESIAN_POINT ( 'NONE',  ( 9.540264233613143574, 0.02433988461803952494, -163.5377607276927563 ) ) ;
#4911=VECTOR ( 'NONE', #13152, 1000.000000000000000 ) ;
#4918=CARTESIAN_POINT ( 'NONE',  ( -3.323869592214536706, 15.00000000000000533, -120.2528461472343082 ) ) ;
#4923=CARTESIAN_POINT ( 'NONE',  ( 10.20171492915204503, 1.831415644534537757, -106.3803253616011943 ) ) ;
#4926=CARTESIAN_POINT ( 'NONE',  ( -1.779087990637969519, 14.96619511928228263, -125.4805735508361693 ) ) ;
#4928=AXIS2_PLACEMENT_3D ( 'NONE', #1902, #8067, #4302 ) ;
#4930=CARTESIAN_POINT ( 'NONE',  ( 5.394780522009475554, 1.937363519424163405, 4.074339615067635201 ) ) ;
#4947=CARTESIAN_POINT ( 'NONE',  ( 9.068716941525982733, 1.734723475976807094E-15, -163.1923081219560174 ) ) ;
#4950=CARTESIAN_POINT ( 'NONE',  ( 1.243260443319662123, 4.000000000000000000, -139.4020581015306846 ) ) ;
#4952=CARTESIAN_POINT ( 'NONE',  ( 8.735174570882092482, 3.542760715477264011, 2.737195459111058771 ) ) ;
#4955=B_SPLINE_CURVE_WITH_KNOTS ( 'NONE', 3,
 ( #1357, #6061, #15286, #196, #4678, #3601, #10483, #1198, #4906, #4609, #7130, #5900, #14041, #10623, #5982, #11934, #2519, #3671 ),
 .UNSPECIFIED., .F., .F.,
 ( 4, 2, 2, 2, 2, 2, 2, 2, 4 ),
 ( 0.000000000000000000, 0.0009867360918462263642, 0.001973472183692452728, 0.002960208275538679309, 0.003946944367384905457, 0.004933680459231131604, 0.005920416551077358619, 0.006907152642923583899, 0.007893888734769809179 ),
 .UNSPECIFIED. ) ;
#4956=EDGE_CURVE ( 'NONE', #6908, #11832, #7420, .T. ) ;
#4958=ORIENTED_EDGE ( 'NONE', *, *, #5908, .F. ) ;
#4960=CARTESIAN_POINT ( 'NONE',  ( -17.29863105483956787, -2.690463824762831016E-12, -194.2807859071518521 ) ) ;
#4964=ORIENTED_EDGE ( 'NONE', *, *, #317, .T. ) ;
#4965=CARTESIAN_POINT ( 'NONE',  ( -6.465967782647407347, 0.3928012870235511600, -116.8537262797278800 ) ) ;
#4970=CARTESIAN_POINT ( 'NONE',  ( 3.810793737614490695, 8.673617379884037444E-16, -110.0325487313770481 ) ) ;
#4972=FACE_OUTER_BOUND ( 'NONE', #2672, .T. ) ;
#4973=CARTESIAN_POINT ( 'NONE',  ( -6.451063615524601502, 4.999999999999201528, -125.7472547710055721 ) ) ;
#4974=CARTESIAN_POINT ( 'NONE',  ( 10.46664703702157695, -1.287459477862190473E-12, -121.2724779345652024 ) ) ;
#4976=CARTESIAN_POINT ( 'NONE',  ( 1.243260443319662123, 4.179859613694246079, -139.4020581015306846 ) ) ;
#4981=CARTESIAN_POINT ( 'NONE',  ( -25.42939282183900573, 4.000000000000000000, -209.0516719515502473 ) ) ;
#4986=ADVANCED_FACE ( 'NONE', ( #9581, #3485 ), #7031, .T. ) ;
#4990=CARTESIAN_POINT ( 'NONE',  ( -10.68385489208660211, 8.673617379884034486E-16, -179.9329437176981799 ) ) ;
#5002=ADVANCED_FACE ( 'NONE', ( #7097 ), #7225, .T. ) ;
#5010=CARTESIAN_POINT ( 'NONE',  ( 7.837953251846155212, 0.2318755756027173209, -105.5268984575482420 ) ) ;
#5015=CARTESIAN_POINT ( 'NONE',  ( 4.911596535478627068, 1.131903148223331934, 3.093215885358307382 ) ) ;
#5017=TOROIDAL_SURFACE ( 'NONE', #334, 5.999999999999995559, 5.000000000000000000 ) ;
#5032=CARTESIAN_POINT ( 'NONE',  ( 13.02262923224196811, 4.033366868162254981, -166.4500998287084883 ) ) ;
#5033=CARTESIAN_POINT ( 'NONE',  ( 9.044950117654433797, -4.000000000000000000, -144.9826476090360643 ) ) ;
#5035=CARTESIAN_POINT ( 'NONE',  ( 11.44399236068192671, -4.000000000000000000, -138.9341978221715976 ) ) ;
#5036=CARTESIAN_POINT ( 'NONE',  ( -25.46076704144856961, 8.673617379884034486E-16, -188.0253354884488601 ) ) ;
#5038=VERTEX_POINT ( 'NONE', #13308 ) ;
#5046=CARTESIAN_POINT ( 'NONE',  ( 17.50071171097425804, 8.749999999999998224, -91.70093451412481045 ) ) ;
#5048=CARTESIAN_POINT ( 'NONE',  ( -8.208951728224439748, 1.532620112797828726, -116.7121244410437129 ) ) ;
#5058=CARTESIAN_POINT ( 'NONE',  ( 4.312410837866842428, -4.336808689942017736E-15, -133.7542242696550829 ) ) ;
#5062=DIRECTION ( 'NONE',  ( 0.000000000000000000, 0.000000000000000000, 1.000000000000000000 ) ) ;
#5065=CARTESIAN_POINT ( 'NONE',  ( 8.895558325401111688, 6.000000000000000000, -141.4560052469132643 ) ) ;
#5070=DIRECTION ( 'NONE',  ( -0.000000000000000000, 1.000000000000000000, -0.000000000000000000 ) ) ;
#5074=CARTESIAN_POINT ( 'NONE',  ( 9.068716941525991615, 0.000000000000000000, -163.1923081219560174 ) ) ;
#5077=CARTESIAN_POINT ( 'NONE',  ( -24.63184704799750691, 3.774669349862838974, -208.8347861833674131 ) ) ;
#5078=( BOUNDED_SURFACE ( )  B_SPLINE_SURFACE ( 3, 2, ( 
 ( #13513, #3759, #8466 ),
 ( #13198, #1828, #671 ),
 ( #9005, #14755, #7771 ),
 ( #9156, #11250, #14903 ),
 ( #4301, #6688, #7844 ),
 ( #8930, #4372, #13658 ),
 ( #10020, #13581, #13884 ),
 ( #4153, #15048, #4443 ),
 ( #5526, #11402, #8853 ),
 ( #1973, #821, #10245 ),
 ( #13731, #10091, #9080 ),
 ( #4225, #2050, #3059 ),
 ( #14977, #6615, #2127 ),
 ( #3130, #12715, #10171 ),
 ( #3279, #13801, #742 ),
 ( #1901, #12484, #7994 ),
 ( #3201, #6538, #12560 ),
 ( #7918, #2983, #6830 ),
 ( #12638, #11322, #7692 ),
 ( #10310, #12405, #11546 ),
 ( #5449, #5377, #14825 ),
 ( #6764, #11476, #961 ),
 ( #895, #5595, #13959 ),
 ( #5970, #9459, #4823 ),
 ( #1041, #6903, #109 ),
 ( #13091, #12866, #4745 ),
 ( #12789, #3660, #15204 ),
 ( #2278, #6983, #5819 ) ),
 .UNSPECIFIED., .F., .F., .T. ) 
 B_SPLINE_SURFACE_WITH_KNOTS ( ( 4, 2, 2, 2, 2, 2, 2, 2, 2, 2, 2, 2, 2, 4 ),
 ( 3, 3 ),
 ( 0.05714059389823637758, 0.06030189704985427362, 0.06188254862566322512, 0.06346320020147216967, 0.06662450335309007265, 0.06978580650470797564, 0.07136645808051692019, 0.07294710965632586475, 0.07452776123213480930, 0.07610841280794376773, 0.07926971595956167072, 0.08006004174746614299, 0.08085036753537061527, 0.08243101911117955982 ),
 ( 0.000000000000000000, 1.000000000000000000 ),
 .UNSPECIFIED. ) 
 GEOMETRIC_REPRESENTATION_ITEM ( )  RATIONAL_B_SPLINE_SURFACE ( (
 ( 1.000000000000000000, 0.7071067811865475727, 1.000000000000000000),
 ( 1.000000000000000000, 0.7071067811865475727, 1.000000000000000000),
 ( 1.000000000000000000, 0.7071067811865475727, 1.000000000000000000),
 ( 1.000000000000000000, 0.7071067811865475727, 1.000000000000000000),
 ( 1.000000000000000000, 0.7071067811865464625, 1.000000000000000000),
 ( 1.000000000000000000, 0.7071067811865464625, 1.000000000000000000),
 ( 1.000000000000000000, 0.7071067811865475727, 1.000000000000000000),
 ( 1.000000000000000000, 0.7071067811865475727, 1.000000000000000000),
 ( 1.000000000000000000, 0.7071067811865473507, 1.000000000000000000),
 ( 1.000000000000000000, 0.7071067811865473507, 1.000000000000000000),
 ( 1.000000000000000000, 0.7071067811865471286, 1.000000000000000000),
 ( 1.000000000000000000, 0.7071067811865471286, 1.000000000000000000),
 ( 1.000000000000000000, 0.7071067811865473507, 1.000000000000000000),
 ( 1.000000000000000000, 0.7071067811865473507, 1.000000000000000000),
 ( 1.000000000000000000, 0.7071067811865475727, 1.000000000000000000),
 ( 1.000000000000000000, 0.7071067811865475727, 1.000000000000000000),
 ( 1.000000000000000000, 0.7071067811865476838, 1.000000000000000000),
 ( 1.000000000000000000, 0.7071067811865476838, 1.000000000000000000),
 ( 1.000000000000000000, 0.7071067811865475727, 1.000000000000000000),
 ( 1.000000000000000000, 0.7071067811865475727, 1.000000000000000000),
 ( 1.000000000000000000, 0.7071067811865475727, 1.000000000000000000),
 ( 1.000000000000000000, 0.7071067811865475727, 1.000000000000000000),
 ( 1.000000000000000000, 0.7071067811865475727, 1.000000000000000000),
 ( 1.000000000000000000, 0.7071067811865475727, 1.000000000000000000),
 ( 1.000000000000000000, 0.7071067811865487940, 1.000000000000000000),
 ( 1.000000000000000000, 0.7071067811865487940, 1.000000000000000000),
 ( 1.000000000000000000, 0.7071067811865475727, 1.000000000000000000),
 ( 1.000000000000000000, 0.7071067811865475727, 1.000000000000000000) ) ) 
 REPRESENTATION_ITEM ( '' )  SURFACE ( )  );
#5079=ORIENTED_EDGE ( 'NONE', *, *, #5448, .T. ) ;
#5087=CARTESIAN_POINT ( 'NONE',  ( 8.469560671982707234, 0.4830037559895700716, -105.5866725495891245 ) ) ;
#5093=CARTESIAN_POINT ( 'NONE',  ( 4.516489297218283738, -0.0008961263519764209014, -1.658221315986036393 ) ) ;
#5100=CARTESIAN_POINT ( 'NONE',  ( 10.73687333765669294, 14.11987504264111060, -106.5879302472600756 ) ) ;
#5108=CARTESIAN_POINT ( 'NONE',  ( 14.22910372453204353, 6.000000000000000000, -126.5134921567817941 ) ) ;
#5109=CARTESIAN_POINT ( 'NONE',  ( -6.790153584124027475, 6.000000000000000000, -124.9643354754709748 ) ) ;
#5110=CARTESIAN_POINT ( 'NONE',  ( 26.58801926426209405, 5.000000000000000888, -139.0072983920785532 ) ) ;
#5116=CARTESIAN_POINT ( 'NONE',  ( -25.49759732579816074, -1.965429835991842803E-15, -208.9099396872309740 ) ) ;
#5125=CARTESIAN_POINT ( 'NONE',  ( 9.943023108890811201, 5.000000000000000888, -43.30782091980646697 ) ) ;
#5129=CARTESIAN_POINT ( 'NONE',  ( -8.589347325819183254, 14.99999999999673683, -120.3237211900380714 ) ) ;
#5131=CARTESIAN_POINT ( 'NONE',  ( -4.681294236308613854, 6.071532165918824830E-15, -115.9486516925368846 ) ) ;
#5132=CARTESIAN_POINT ( 'NONE',  ( 4.006117301121300045, 8.673617379884035472E-16, -109.3626630931961614 ) ) ;
#5135=CARTESIAN_POINT ( 'NONE',  ( 17.50071171097425804, 8.749999999999998224, -91.70093451412481045 ) ) ;
#5138=CARTESIAN_POINT ( 'NONE',  ( 10.00369055844187649, 12.49999999999999822, -46.08764602067113714 ) ) ;
#5139=CARTESIAN_POINT ( 'NONE',  ( 9.068716941525991615, 0.000000000000000000, -163.1923081219560174 ) ) ;
#5143=VERTEX_POINT ( 'NONE', #8888 ) ;
#5147=CARTESIAN_POINT ( 'NONE',  ( 10.22352057816269699, 15.00000000000000000, -125.5112093480189657 ) ) ;
#5151=CARTESIAN_POINT ( 'NONE',  ( -25.11906781955738310, 0.000000000000000000, -198.9681998140721078 ) ) ;
#5152=VERTEX_POINT ( 'NONE', #13619 ) ;
#5161=FACE_OUTER_BOUND ( 'NONE', #10428, .T. ) ;
#5172=EDGE_CURVE ( 'NONE', #11237, #1120, #12444, .T. ) ;
#5175=EDGE_CURVE ( 'NONE', #11904, #4807, #11379, .T. ) ;
#5178=CARTESIAN_POINT ( 'NONE',  ( 11.32016196459919755, 12.49999999999999822, -106.4092894470421271 ) ) ;
#5185=CARTESIAN_POINT ( 'NONE',  ( 1.041519256436086005, 6.000000000000000000, -139.4527716894432956 ) ) ;
#5188=CARTESIAN_POINT ( 'NONE',  ( 12.73368604874516485, 3.759190274397234521, -166.5778610917592175 ) ) ;
#5189=DIRECTION ( 'NONE',  ( 0.000000000000000000, 1.000000000000000000, 0.000000000000000000 ) ) ;
#5191=DIRECTION ( 'NONE',  ( -0.000000000000000000, 1.000000000000000000, -0.000000000000000000 ) ) ;
#5195=CARTESIAN_POINT ( 'NONE',  ( 4.033098156699464809, 0.09438068890155107415, -1.663700395152567513 ) ) ;
#5201=VERTEX_POINT ( 'NONE', #15006 ) ;
#5213=CARTESIAN_POINT ( 'NONE',  ( 8.348030713307990069, 8.673617379884035472E-16, -112.8139498890285068 ) ) ;
#5214=FACE_OUTER_BOUND ( 'NONE', #12931, .T. ) ;
#5217=CARTESIAN_POINT ( 'NONE',  ( 8.941167358697452272, 11.11422854771078050, 2.597912425534024017 ) ) ;
#5219=DIRECTION ( 'NONE',  ( 0.000000000000000000, 0.000000000000000000, 1.000000000000000000 ) ) ;
#5225=CIRCLE ( 'NONE', #284, 2.499999999999999556 ) ;
#5228=CARTESIAN_POINT ( 'NONE',  ( 5.228075279701640099, 1.000000000000000000, -163.7939279834373849 ) ) ;
#5234=ORIENTED_EDGE ( 'NONE', *, *, #728, .F. ) ;
#5237=ORIENTED_EDGE ( 'NONE', *, *, #5908, .T. ) ;
#5247=ORIENTED_EDGE ( 'NONE', *, *, #4599, .F. ) ;
#5258=CARTESIAN_POINT ( 'NONE',  ( -9.681086997240697656, 4.299422167715417409, -116.3713800322179992 ) ) ;
#5261=CARTESIAN_POINT ( 'NONE',  ( 12.18930925058789860, 2.167092202807543000, -166.0723187315431915 ) ) ;
#5262=EDGE_CURVE ( 'NONE', #13240, #9168, #6494, .T. ) ;
#5265=CARTESIAN_POINT ( 'NONE',  ( -25.24054375344501722, 4.000000000000112799, -170.3561389648133400 ) ) ;
#5272=CARTESIAN_POINT ( 'NONE',  ( 9.318502292199219994, 1.005413715383896456, -105.8229423371888345 ) ) ;
#5276=CARTESIAN_POINT ( 'NONE',  ( -9.868623142791424385, 4.607815636209187993, -115.7530035201766765 ) ) ;
#5281=DIRECTION ( 'NONE',  ( 0.9989498407774362043, 0.000000000000000000, 0.04581719776170026237 ) ) ;
#5288=CARTESIAN_POINT ( 'NONE',  ( 8.425472749221725621, 5.000000000000000888, -115.5475827924929035 ) ) ;
#5291=CIRCLE ( 'NONE', #10707, 1.000000000000000888 ) ;
#5301=AXIS2_PLACEMENT_3D ( 'NONE', #1265, #7051, #11768 ) ;
#5305=CARTESIAN_POINT ( 'NONE',  ( -8.195495352953928503, 13.58490726914820002, -116.3141769265031655 ) ) ;
#5316=CARTESIAN_POINT ( 'NONE',  ( 11.32016196458614488, 4.659658575830587068, -106.4092894464441486 ) ) ;
#5319=CARTESIAN_POINT ( 'NONE',  ( 26.71007981443201018, 5.000000000000000888, -136.8791680534710054 ) ) ;
#5331=CARTESIAN_POINT ( 'NONE',  ( -9.385448347264265578, 4.649823776045643342, -115.3551636530116866 ) ) ;
#5337=CARTESIAN_POINT ( 'NONE',  ( -29.14779469708810566, 3.999999999999993783, -181.3194353810159498 ) ) ;
#5342=CARTESIAN_POINT ( 'NONE',  ( 8.673617379884035472E-16, 5.000000000000000888, -1.663700395152567513 ) ) ;
#5343=DIRECTION ( 'NONE',  ( 0.000000000000000000, 0.000000000000000000, 1.000000000000000000 ) ) ;
#5345=CARTESIAN_POINT ( 'NONE',  ( 26.58801926426210116, 5.000000000000000888, -139.0072983920785532 ) ) ;
#5356=AXIS2_PLACEMENT_3D ( 'NONE', #12617, #3258, #15184 ) ;
#5358=CARTESIAN_POINT ( 'NONE',  ( 9.550372275008729872, 0.000000000000000000, -109.1178429856683181 ) ) ;
#5361=EDGE_LOOP ( 'NONE', ( #8142, #6905, #351, #3905 ) ) ;
#5362=CARTESIAN_POINT ( 'NONE',  ( 9.993646670323888870, 5.943472311793079221, -45.62742802061889336 ) ) ;
#5368=EDGE_CURVE ( 'NONE', #6054, #8964, #3730, .T. ) ;
#5370=EDGE_CURVE ( 'NONE', #6769, #3728, #10387, .T. ) ;
#5372=CARTESIAN_POINT ( 'NONE',  ( 9.969726460969127402, 12.69562161215808516, -44.88270096458933978 ) ) ;
#5374=CARTESIAN_POINT ( 'NONE',  ( -25.37350819791483403, 4.000000000000000000, -209.1133945293850900 ) ) ;
#5375=CARTESIAN_POINT ( 'NONE',  ( 26.73766085848595964, 6.000000000000000000, -138.7442440334353364 ) ) ;
#5377=CARTESIAN_POINT ( 'NONE',  ( 9.136110106120531427, 14.99999999999624833, -109.8557328640159483 ) ) ;
#5378=CARTESIAN_POINT ( 'NONE',  ( 20.87131526946576443, 1.301042606982605321E-15, -138.9752963459259547 ) ) ;
#5384=CARTESIAN_POINT ( 'NONE',  ( -4.234402844927150689, 15.00000000000000000, -117.4888040839639558 ) ) ;
#5391=CARTESIAN_POINT ( 'NONE',  ( 8.885817745189735106, 5.000000000000000000, -110.4710698842959573 ) ) ;
#5393=ORIENTED_EDGE ( 'NONE', *, *, #1537, .F. ) ;
#5397=CARTESIAN_POINT ( 'NONE',  ( 10.93110029320957821, 13.31722294372111470, -107.0492663392355297 ) ) ;
#5399=CARTESIAN_POINT ( 'NONE',  ( 10.56872662651230854, 14.06121913168272108, -106.8383111373542107 ) ) ;
#5402=CARTESIAN_POINT ( 'NONE',  ( 10.96001076296047394, 5.773884160794588105, -44.27064330819454341 ) ) ;
#5407=CARTESIAN_POINT ( 'NONE',  ( 8.807773658247754156, 15.00000000000000000, -105.8689255569352667 ) ) ;
#5411=CARTESIAN_POINT ( 'NONE',  ( -27.13173129639779901, 4.000000000000835776, -174.9559605998265681 ) ) ;
#5416=CARTESIAN_POINT ( 'NONE',  ( 5.000000000000000000, 5.000000000000000888, -100.6237003951525679 ) ) ;
#5418=CARTESIAN_POINT ( 'NONE',  ( -19.41689661852894844, 8.673617379884033500E-16, -190.2656566201660837 ) ) ;
#5419=CARTESIAN_POINT ( 'NONE',  ( 4.892302586675363330, 0.000000000000000000, -102.5092683516849661 ) ) ;
#5421=FACE_OUTER_BOUND ( 'NONE', #11361, .T. ) ;
#5424=CARTESIAN_POINT ( 'NONE',  ( -5.309262520577839872, 13.36526483154179523, -125.0911079416483176 ) ) ;
#5428=EDGE_CURVE ( 'NONE', #6005, #8015, #10344, .T. ) ;
#5429=CARTESIAN_POINT ( 'NONE',  ( 10.97171279554003043, 8.773889247172311556, -44.61149169061435060 ) ) ;
#5431=CIRCLE ( 'NONE', #13348, 3.500000000000003109 ) ;
#5434=CARTESIAN_POINT ( 'NONE',  ( 8.983524629129894024, 12.48417253965678064, 0.6570725777486732255 ) ) ;
#5435=CARTESIAN_POINT ( 'NONE',  ( 29.15191114725999455, 8.773889247172311556, -41.21400910903738435 ) ) ;
#5442=CARTESIAN_POINT ( 'NONE',  ( 10.01611035499524682, 11.63253765721051636, -45.55947799121552322 ) ) ;
#5444=CIRCLE ( 'NONE', #3719, 4.000000000000002665 ) ;
#5447=CARTESIAN_POINT ( 'NONE',  ( -7.687033461059231243, 13.90392860197237823, -116.8257989789342730 ) ) ;
#5448=EDGE_CURVE ( 'NONE', #5038, #3740, #14858, .T. ) ;
#5449=CARTESIAN_POINT ( 'NONE',  ( 6.854384957879182672, 15.00000000000000000, -108.8103024308010589 ) ) ;
#5450=FACE_OUTER_BOUND ( 'NONE', #955, .T. ) ;
#5452=CARTESIAN_POINT ( 'NONE',  ( 23.60198427277999755, 0.4374050601044401354, -138.3407798013068657 ) ) ;
#5455=ORIENTED_EDGE ( 'NONE', *, *, #5428, .T. ) ;
#5458=CARTESIAN_POINT ( 'NONE',  ( -30.17038736920199682, 4.000000000000000888, -186.2979594716615566 ) ) ;
#5461=VERTEX_POINT ( 'NONE', #9556 ) ;
#5462=CARTESIAN_POINT ( 'NONE',  ( -8.031487215395609169, 13.41211965017131469, -115.9574366882090146 ) ) ;
#5465=AXIS2_PLACEMENT_3D ( 'NONE', #5624, #5920, #10646 ) ;
#5470=CARTESIAN_POINT ( 'NONE',  ( 10.02605224556585384, 4.999999999999999112, -108.3589403638364530 ) ) ;
#5471=ADVANCED_FACE ( 'NONE', ( #8778 ), #8315, .F. ) ;
#5472=VERTEX_POINT ( 'NONE', #3995 ) ;
#5486=CARTESIAN_POINT ( 'NONE',  ( 8.513076393186699065, 14.99999999999999822, -106.2110621154036494 ) ) ;
#5487=CARTESIAN_POINT ( 'NONE',  ( 11.04730217088350663, 5.000000000000000888, -107.1178495010082941 ) ) ;
#5489=CARTESIAN_POINT ( 'NONE',  ( -27.18350272990648264, 1.080414591133489251E-12, -177.5702011201350103 ) ) ;
#5495=CARTESIAN_POINT ( 'NONE',  ( 7.000000000000000888, 15.00000000000000000, -1.663700395152567513 ) ) ;
#5497=CARTESIAN_POINT ( 'NONE',  ( -9.868623143902821582, 5.000000000000003553, -115.7530035192419433 ) ) ;
#5509=ORIENTED_EDGE ( 'NONE', *, *, #13763, .T. ) ;
#5511=CARTESIAN_POINT ( 'NONE',  ( -22.63089125489394604, 3.999999999999999112, -204.5592954525788514 ) ) ;
#5516=VERTEX_POINT ( 'NONE', #5228 ) ;
#5522=CARTESIAN_POINT ( 'NONE',  ( -6.465967782645682504, 14.60719871297730243, -116.8537262797239151 ) ) ;
#5525=CIRCLE ( 'NONE', #3300, 1.750000000000001554 ) ;
#5526=CARTESIAN_POINT ( 'NONE',  ( 7.622624992407810218, 15.00000000000000000, -121.2625470869670181 ) ) ;
#5528=CARTESIAN_POINT ( 'NONE',  ( 26.11837629089787782, 1.928122897211196340, -137.7354575184153589 ) ) ;
#5533=ORIENTED_EDGE ( 'NONE', *, *, #837, .T. ) ;
#5534=CARTESIAN_POINT ( 'NONE',  ( -7.548446295636298764, 13.85765414864760459, -116.1647996692329485 ) ) ;
#5535=CIRCLE ( 'NONE', #7509, 0.4999999999999726885 ) ;
#5536=CARTESIAN_POINT ( 'NONE',  ( 6.321352278304661176, 5.000000000000000888, -106.5183844524637635 ) ) ;
#5539=CARTESIAN_POINT ( 'NONE',  ( -25.29096338392381327, 1.168513153268224259E-15, -199.8929960699789206 ) ) ;
#5543=CARTESIAN_POINT ( 'NONE',  ( 9.971950858281140029, 8.773889247172311556, -44.63331069169930032 ) ) ;
#5546=EDGE_LOOP ( 'NONE', ( #7367, #7542, #5079, #1478, #10297, #3418 ) ) ;
#5548=CARTESIAN_POINT ( 'NONE',  ( 9.391154601535028235, 14.93751321453985170, -106.1795410437272551 ) ) ;
#5550=EDGE_CURVE ( 'NONE', #14561, #7952, #436, .T. ) ;
#5552=CARTESIAN_POINT ( 'NONE',  ( -5.525175898872280555, 0.1455664706284490462, -116.9935625178451772 ) ) ;
#5553=ORIENTED_EDGE ( 'NONE', *, *, #6104, .T. ) ;
#5554=CARTESIAN_POINT ( 'NONE',  ( -8.926802767664643312, 2.381696043666894358, -116.5496838980187562 ) ) ;
#5558=CARTESIAN_POINT ( 'NONE',  ( 5.856634129115241727, 14.99999999999999822, -112.7529454488145859 ) ) ;
#5561=CARTESIAN_POINT ( 'NONE',  ( -25.72606948156193951, 8.673617379884035472E-16, -194.7310816857908549 ) ) ;
#5567=CARTESIAN_POINT ( 'NONE',  ( 5.228075279701640099, 1.000000000000000000, -165.7939279834373849 ) ) ;
#5568=LINE ( 'NONE', #10284, #2573 ) ;
#5570=CARTESIAN_POINT ( 'NONE',  ( 8.937327444046795577, 10.65305643749201181, 2.773860008794248433 ) ) ;
#5571=CARTESIAN_POINT ( 'NONE',  ( -8.199037228201154548, 5.000000000000000888, -114.3845095685560835 ) ) ;
#5578=CARTESIAN_POINT ( 'NONE',  ( 22.25537508876543313, 0.1342633940746081334, -138.4925780178333810 ) ) ;
#5583=ORIENTED_EDGE ( 'NONE', *, *, #3653, .F. ) ;
#5589=ORIENTED_EDGE ( 'NONE', *, *, #797, .T. ) ;
#5595=CARTESIAN_POINT ( 'NONE',  ( 9.781725384962639325, 15.00000000000000000, -108.7377634488996136 ) ) ;
#5596=FACE_OUTER_BOUND ( 'NONE', #10773, .T. ) ;
#5599=CARTESIAN_POINT ( 'NONE',  ( 26.02337256472977245, 2.644888176801018176, -137.1336233889525715 ) ) ;
#5612=CARTESIAN_POINT ( 'NONE',  ( -24.89144347233892773, 2.130041083117732992, -207.5316459546360193 ) ) ;
#5615=DIRECTION ( 'NONE',  ( -0.000000000000000000, -1.000000000000000000, -0.000000000000000000 ) ) ;
#5616=EDGE_LOOP ( 'NONE', ( #2848, #9033, #656, #2342 ) ) ;
#5617=ADVANCED_FACE ( 'NONE', ( #1664 ), #2000, .T. ) ;
#5619=CARTESIAN_POINT ( 'NONE',  ( -5.082498805844316792, 10.00000000000000178, -111.2070015758558839 ) ) ;
#5623=EDGE_LOOP ( 'NONE', ( #1753, #8664, #2270, #6234 ) ) ;
#5624=CARTESIAN_POINT ( 'NONE',  ( 9.044950117654433797, 4.000000000000000000, -141.4826476090360643 ) ) ;
#5626=CARTESIAN_POINT ( 'NONE',  ( 10.97846948146473700, 13.76924748112251784, -106.3333921311819523 ) ) ;
#5629=ORIENTED_EDGE ( 'NONE', *, *, #3372, .T. ) ;
#5631=CARTESIAN_POINT ( 'NONE',  ( -24.98726638638703790, 3.999999999999993783, -209.5206582725076032 ) ) ;
#5633=ADVANCED_FACE ( 'NONE', ( #14591 ), #4756, .F. ) ;
#5637=ORIENTED_EDGE ( 'NONE', *, *, #11002, .T. ) ;
#5640=CARTESIAN_POINT ( 'NONE',  ( 2.304446043347688100, 8.673617379884041389E-16, -168.0449129170526419 ) ) ;
#5641=CARTESIAN_POINT ( 'NONE',  ( -1.030030361949073603, 5.000000000000000888, -105.0143096064271901 ) ) ;
#5646=CARTESIAN_POINT ( 'NONE',  ( -6.790153584124027475, 9.999999999999998224, -124.9643354754709748 ) ) ;
#5647=( BOUNDED_CURVE ( )  B_SPLINE_CURVE ( 3, ( #13691, #5185, #9896, #6568 ),
 .UNSPECIFIED., .F., .F. ) 
 B_SPLINE_CURVE_WITH_KNOTS ( ( 4, 4 ),
 ( 2.234491175284466280, 2.237794841200465790 ),
 .UNSPECIFIED. ) 
 CURVE ( )  GEOMETRIC_REPRESENTATION_ITEM ( )  RATIONAL_B_SPLINE_CURVE ( ( 1.000000000000000000, 0.9999990904828330862, 0.9999990904828330862, 1.000000000000000000 ) ) 
 REPRESENTATION_ITEM ( '' )  );
#5656=CARTESIAN_POINT ( 'NONE',  ( 2.735681601764421877, 0.000000000000000000, -172.9928595839035665 ) ) ;
#5660=EDGE_LOOP ( 'NONE', ( #4435, #10787, #8373, #1173 ) ) ;
#5670=CARTESIAN_POINT ( 'NONE',  ( -6.885999823355373195, 14.39196139387547468, -116.9934166929402295 ) ) ;
#5672=CARTESIAN_POINT ( 'NONE',  ( 27.42902907614759656, 4.089980352809128306, -137.4133472663777127 ) ) ;
#5674=VERTEX_POINT ( 'NONE', #6533 ) ;
#5682=DIRECTION ( 'NONE',  ( 0.02181900108494707821, 0.000000000000000000, -0.9997619372588931741 ) ) ;
#5684=CIRCLE ( 'NONE', #3965, 0.4999999999999726885 ) ;
#5686=CARTESIAN_POINT ( 'NONE',  ( -25.47867862103529646, 0.2061871876987354246, -202.7017271924692068 ) ) ;
#5690=CARTESIAN_POINT ( 'NONE',  ( 8.316464637237423574, 5.000000000000000000, -114.4073620934065048 ) ) ;
#5694=B_SPLINE_CURVE_WITH_KNOTS ( 'NONE', 3,
 ( #15079, #5780, #8246, #15303, #4554, #8317, #13043, #10501, #11725, #4626, #2453, #14060 ),
 .UNSPECIFIED., .F., .F.,
 ( 4, 2, 2, 2, 2, 4 ),
 ( 2.168404344971008868E-18, 0.003032381943411205719, 0.006064763886822409703, 0.01212952777364481594, 0.01819429166046722390, 0.02425905554728963187 ),
 .UNSPECIFIED. ) ;
#5697=FACE_OUTER_BOUND ( 'NONE', #10906, .T. ) ;
#5709=ORIENTED_EDGE ( 'NONE', *, *, #9382, .T. ) ;
#5717=CARTESIAN_POINT ( 'NONE',  ( -25.31996789051264685, 0.02318398216220063368, -200.1489047904456129 ) ) ;
#5718=CARTESIAN_POINT ( 'NONE',  ( 8.904552045041942421, 13.48516601183745500, 4.275651785405313099 ) ) ;
#5719=CARTESIAN_POINT ( 'NONE',  ( 0.000000000000000000, 8.673617379884035472E-16, -100.6237003951525679 ) ) ;
#5725=ADVANCED_FACE ( 'NONE', ( #11318 ), #3000, .F. ) ;
#5727=CARTESIAN_POINT ( 'NONE',  ( 1.004809442601927394, 6.000000000000000000, -139.4752805618705622 ) ) ;
#5733=ORIENTED_EDGE ( 'NONE', *, *, #9666, .F. ) ;
#5735=CARTESIAN_POINT ( 'NONE',  ( -12.84530548741220990, -1.035315611211759139E-11, -188.5128586801774020 ) ) ;
#5742=DIRECTION ( 'NONE',  ( -0.000000000000000000, -1.000000000000000000, -0.000000000000000000 ) ) ;
#5747=CARTESIAN_POINT ( 'NONE',  ( 0.5944212552585367293, 15.00000000000000000, -138.5540974747773930 ) ) ;
#5751=AXIS2_PLACEMENT_3D ( 'NONE', #6150, #13282, #14527 ) ;
#5754=ORIENTED_EDGE ( 'NONE', *, *, #4053, .T. ) ;
#5755=ORIENTED_EDGE ( 'NONE', *, *, #7602, .T. ) ;
#5757=DIRECTION ( 'NONE',  ( 0.000000000000000000, 1.000000000000000000, 0.000000000000000000 ) ) ;
#5760=ORIENTED_EDGE ( 'NONE', *, *, #552, .T. ) ;
#5766=CARTESIAN_POINT ( 'NONE',  ( -25.65051852152078737, 1.581731481231831049, -206.7883074467665097 ) ) ;
#5769=CARTESIAN_POINT ( 'NONE',  ( 6.436143463598921421, 5.000000000000000888, 2.800833825385760090 ) ) ;
#5770=VERTEX_POINT ( 'NONE', #6451 ) ;
#5771=AXIS2_PLACEMENT_3D ( 'NONE', #13379, #9886, #12493 ) ;
#5780=CARTESIAN_POINT ( 'NONE',  ( 0.6118422199237436576, 5.000000000000000888, -137.1181811292527470 ) ) ;
#5786=CARTESIAN_POINT ( 'NONE',  ( -25.78198310901690959, 3.999999999999627853, -208.7111422138455907 ) ) ;
#5791=EDGE_LOOP ( 'NONE', ( #8068, #7684 ) ) ;
#5793=CARTESIAN_POINT ( 'NONE',  ( -25.42939282183900573, 4.000000000000000000, -209.0516719515502473 ) ) ;
#5794=CARTESIAN_POINT ( 'NONE',  ( 8.955009189050604945, 14.88563060951957340, 1.963670047743441449 ) ) ;
#5795=DIRECTION ( 'NONE',  ( 0.02181900108494707127, 0.000000000000000000, -0.9997619372588931741 ) ) ;
#5797=CARTESIAN_POINT ( 'NONE',  ( 20.84482309861724048, -1.169407659665303564E-12, -149.6621754078184665 ) ) ;
#5801=CARTESIAN_POINT ( 'NONE',  ( 24.19680568221177452, 0.8824476403469397878, -137.8004069206694453 ) ) ;
#5814=ORIENTED_EDGE ( 'NONE', *, *, #733, .T. ) ;
#5819=CARTESIAN_POINT ( 'NONE',  ( 11.13433036043491242, 12.49999999999999822, -107.0267359326556829 ) ) ;
#5820=CARTESIAN_POINT ( 'NONE',  ( 5.178267505235062629, 8.673617379884035472E-16, -121.9231527573877258 ) ) ;
#5836=CARTESIAN_POINT ( 'NONE',  ( -25.42793803927663987, 0.04176024464420144411, -200.8198567788932110 ) ) ;
#5846=CARTESIAN_POINT ( 'NONE',  ( 1.114947364559091714, 4.793811891163896277, -139.4079432275550801 ) ) ;
#5850=LINE ( 'NONE', #4701, #11690 ) ;
#5854=ORIENTED_EDGE ( 'NONE', *, *, #14897, .F. ) ;
#5855=CARTESIAN_POINT ( 'NONE',  ( -25.04988596881782570, 8.673617379884035472E-16, -199.3167991962343706 ) ) ;
#5865=CARTESIAN_POINT ( 'NONE',  ( 11.32016196459912649, 15.00000000000000000, -106.4092894470390291 ) ) ;
#5869=CARTESIAN_POINT ( 'NONE',  ( 8.935548306746156300, 9.999999999999998224, 2.855381328098127725 ) ) ;
#5874=EDGE_LOOP ( 'NONE', ( #6292, #13971, #12630, #3232 ) ) ;
#5875=ORIENTED_EDGE ( 'NONE', *, *, #728, .T. ) ;
#5877=CARTESIAN_POINT ( 'NONE',  ( 10.43870542337790930, 12.49999999999999822, -107.8020611273035883 ) ) ;
#5882=CARTESIAN_POINT ( 'NONE',  ( -4.873637833199961911, 1.564568837530078786E-16, -117.2491930705948988 ) ) ;
#5885=CYLINDRICAL_SURFACE ( 'NONE', #8387, 2.000000000000001776 ) ;
#5886=ADVANCED_FACE ( 'NONE', ( #4740 ), #9454, .T. ) ;
#5889=DIRECTION ( 'NONE',  ( 0.000000000000000000, 0.000000000000000000, -1.000000000000000000 ) ) ;
#5890=CARTESIAN_POINT ( 'NONE',  ( 22.59539982210069553, 8.673617379884035472E-16, -140.1889075229756259 ) ) ;
#5894=ORIENTED_EDGE ( 'NONE', *, *, #8014, .T. ) ;
#5900=CARTESIAN_POINT ( 'NONE',  ( 6.256842659011002006, 14.34211104607853393, 2.774933013893350786 ) ) ;
#5904=B_SPLINE_CURVE_WITH_KNOTS ( 'NONE', 3,
 ( #4874, #14640, #4037, #4952, #167, #9586, #9826, #1705, #6189, #6271, #3717, #7421, #14312, #3879, #10750, #8742, #7266, #1401, #10986, #8422, #10904, #13474 ),
 .UNSPECIFIED., .F., .F.,
 ( 4, 2, 2, 2, 2, 2, 2, 2, 2, 2, 4 ),
 ( 8.673617379884035472E-19, 0.001106625736872399440, 0.002213251473744798012, 0.002766564342180997081, 0.003319877210617196584, 0.004426502947489592554, 0.005533128684361988958, 0.006639754421234385362, 0.007746380158106782633, 0.008299693026542979968, 0.008853005894979178170 ),
 .UNSPECIFIED. ) ;
#5905=CARTESIAN_POINT ( 'NONE',  ( -7.398315985760856250, 9.999999999999998224, -123.5712579988217072 ) ) ;
#5908=EDGE_CURVE ( 'NONE', #6054, #7799, #6847, .T. ) ;
#5913=VERTEX_POINT ( 'NONE', #6826 ) ;
#5920=DIRECTION ( 'NONE',  ( 0.000000000000000000, 1.000000000000000000, 0.000000000000000000 ) ) ;
#5922=CARTESIAN_POINT ( 'NONE',  ( 9.508011421805740326, 1.297355693583747804, -106.3802021279168031 ) ) ;
#5929=CARTESIAN_POINT ( 'NONE',  ( 7.906415743051303124, 1.937363517912831012, 2.211849553340444530 ) ) ;
#5931=B_SPLINE_CURVE_WITH_KNOTS ( 'NONE', 3,
 ( #3141, #12573, #6704, #15290, #6780, #7067, #4543, #3216, #4461, #2295, #12885, #4759, #14125, #9398 ),
 .UNSPECIFIED., .F., .F.,
 ( 4, 2, 2, 2, 2, 2, 4 ),
 ( 0.000000000000000000, 0.004869271879394969707, 0.007303907819092454561, 0.009738543758789939414, 0.01460781563818490912, 0.01704245157788239484, 0.01947708751757987883 ),
 .UNSPECIFIED. ) ;
#5943=CARTESIAN_POINT ( 'NONE',  ( 0.2116200952963268878, 8.673617379884035472E-16, -112.6243614187691975 ) ) ;
#5955=ORIENTED_EDGE ( 'NONE', *, *, #648, .T. ) ;
#5957=CARTESIAN_POINT ( 'NONE',  ( 9.010117806275914631, 12.49999999999999822, -110.1316647874338202 ) ) ;
#5963=CARTESIAN_POINT ( 'NONE',  ( -4.234402844927157794, 4.336808689942017736E-16, -117.4888040839639558 ) ) ;
#5965=CARTESIAN_POINT ( 'NONE',  ( -0.4873557683217199510, 5.000000000000001776, -103.5659326153046038 ) ) ;
#5970=CARTESIAN_POINT ( 'NONE',  ( 7.965741386218653020, 15.00000000000000000, -106.9514265361661387 ) ) ;
#5971=CARTESIAN_POINT ( 'NONE',  ( 15.55587903137338834, -8.452217897303065567E-13, -128.0070267004813900 ) ) ;
#5972=EDGE_LOOP ( 'NONE', ( #10754, #14567, #8034, #13582, #7710, #2428 ) ) ;
#5976=ORIENTED_EDGE ( 'NONE', *, *, #1166, .T. ) ;
#5977=CYLINDRICAL_SURFACE ( 'NONE', #12936, 1.000000000000000888 ) ;
#5981=EDGE_CURVE ( 'NONE', #2589, #8920, #7889, .T. ) ;
#5982=CARTESIAN_POINT ( 'NONE',  ( 6.347577276663199264, 14.84036095819059220, 1.566136529894637253 ) ) ;
#5987=CARTESIAN_POINT ( 'NONE',  ( 7.125599087756446792, 15.00000000000000000, -120.1321298350141831 ) ) ;
#5989=DIRECTION ( 'NONE',  ( -0.02181900108494732801, 0.000000000000000000, 0.9997619372588931741 ) ) ;
#5994=VECTOR ( 'NONE', #13468, 1000.000000000000114 ) ;
#5999=CARTESIAN_POINT ( 'NONE',  ( 10.58852313474634421, 2.370005426030849627, -106.5284185414804199 ) ) ;
#6001=DIRECTION ( 'NONE',  ( 0.000000000000000000, 1.000000000000000000, 0.000000000000000000 ) ) ;
#6002=CIRCLE ( 'NONE', #11698, 1.000000000000000888 ) ;
#6005=VERTEX_POINT ( 'NONE', #4350 ) ;
#6006=CARTESIAN_POINT ( 'NONE',  ( 4.033098156701212744, 0.09438068890001453937, -1.663700395152667211 ) ) ;
#6024=DIRECTION ( 'NONE',  ( 2.672056983927306126E-18, 1.000000000000000000, -1.224355256373460583E-16 ) ) ;
#6025=LINE ( 'NONE', #5033, #2442 ) ;
#6026=CARTESIAN_POINT ( 'NONE',  ( 1.078231930479242484, 5.000000000000000888, -139.4303258909232852 ) ) ;
#6047=CARTESIAN_POINT ( 'NONE',  ( -9.492276966213163192, 10.00000000001546674, -117.3221826544872215 ) ) ;
#6049=CARTESIAN_POINT ( 'NONE',  ( 4.544676675852343806, 15.00000000000000000, -126.1782412829290934 ) ) ;
#6050=CARTESIAN_POINT ( 'NONE',  ( 23.85593715798673031, 8.673617379884035472E-16, -134.9913929664622287 ) ) ;
#6054=VERTEX_POINT ( 'NONE', #10067 ) ;
#6061=CARTESIAN_POINT ( 'NONE',  ( 6.122889832264990950, 10.33058039608724954, 5.281130614573721793 ) ) ;
#6069=ORIENTED_EDGE ( 'NONE', *, *, #10183, .T. ) ;
#6081=CARTESIAN_POINT ( 'NONE',  ( -2.935443650368948276, 14.73055553252727634, -125.3529989061166532 ) ) ;
#6084=CARTESIAN_POINT ( 'NONE',  ( 4.892667292236299481, 0.02568563158750709549, 0.3754323223072091875 ) ) ;
#6104=EDGE_CURVE ( 'NONE', #16, #4737, #1231, .T. ) ;
#6105=CARTESIAN_POINT ( 'NONE',  ( 2.394576890926103818, 8.673617379884035472E-16, -144.4837070969091712 ) ) ;
#6107=CARTESIAN_POINT ( 'NONE',  ( 2.538752285253552454, -6.419766481290676335E-32, -144.3958141051384985 ) ) ;
#6112=ORIENTED_EDGE ( 'NONE', *, *, #2154, .T. ) ;
#6114=CARTESIAN_POINT ( 'NONE',  ( -24.29516989927810400, 3.999999999999602096, -208.1346784444976095 ) ) ;
#6117=FACE_OUTER_BOUND ( 'NONE', #14781, .T. ) ;
#6120=B_SPLINE_CURVE_WITH_KNOTS ( 'NONE', 3,
 ( #10817, #10671, #13065, #10982, #8576, #9750 ),
 .UNSPECIFIED., .F., .F.,
 ( 4, 2, 4 ),
 ( 0.0002107453662977397553, 0.01553454269887521305, 0.03085834003145268567 ),
 .UNSPECIFIED. ) ;
#6123=CARTESIAN_POINT ( 'NONE',  ( 3.704461453187086750, 8.673617379884037444E-16, -110.4530743311176479 ) ) ;
#6129=CARTESIAN_POINT ( 'NONE',  ( 10.87631271617703987, 5.000000000000000888, -121.9832090783556140 ) ) ;
#6133=DIRECTION ( 'NONE',  ( 0.000000000000000000, 0.000000000000000000, -1.000000000000000000 ) ) ;
#6140=ORIENTED_EDGE ( 'NONE', *, *, #3371, .F. ) ;
#6141=CARTESIAN_POINT ( 'NONE',  ( -12.80600979999658762, 8.673617379884035472E-16, -182.2240817400024184 ) ) ;
#6148=ORIENTED_EDGE ( 'NONE', *, *, #8477, .T. ) ;
#6150=CARTESIAN_POINT ( 'NONE',  ( 16.54458777588525820, 8.749999999999998224, -93.72227738972755162 ) ) ;
#6153=CARTESIAN_POINT ( 'NONE',  ( 14.10364480454416736, 12.78325705495013409, -126.3882374904445953 ) ) ;
#6155=CARTESIAN_POINT ( 'NONE',  ( 10.32514698675680087, 14.49901653209251151, -106.1904513033518356 ) ) ;
#6159=CARTESIAN_POINT ( 'NONE',  ( 26.15341798802279527, 4.000000000000000000, -138.7600702976168066 ) ) ;
#6162=CARTESIAN_POINT ( 'NONE',  ( 4.763827962848262487, 0.9384448409284688042, 2.740567078347254881 ) ) ;
#6172=DIRECTION ( 'NONE',  ( 0.8538457527776451839, 0.000000000000000000, 0.5205261093005582040 ) ) ;
#6181=CARTESIAN_POINT ( 'NONE',  ( 13.09348522998630848, 3.759190269696439657, -166.1421527720724782 ) ) ;
#6188=AXIS2_PLACEMENT_3D ( 'NONE', #11745, #2257, #160 ) ;
#6189=CARTESIAN_POINT ( 'NONE',  ( 8.029176165208181004, 2.106883416375387341, 2.293638343255871348 ) ) ;
#6199=ORIENTED_EDGE ( 'NONE', *, *, #10368, .F. ) ;
#6200=CARTESIAN_POINT ( 'NONE',  ( -8.195495352952498536, 1.415092730851200020, -116.3141769264971259 ) ) ;
#6211=CARTESIAN_POINT ( 'NONE',  ( -5.134731047605749943, 5.000000000000798472, -128.4544621779346585 ) ) ;
#6213=EDGE_LOOP ( 'NONE', ( #8106, #710, #10376, #2461, #4429 ) ) ;
#6230=CARTESIAN_POINT ( 'NONE',  ( 4.033098156699464809, 0.09438068890155107415, -1.663700395152567513 ) ) ;
#6233=CARTESIAN_POINT ( 'NONE',  ( -25.07602529789992118, 1.361017155774153053, -206.3226864593361256 ) ) ;
#6234=ORIENTED_EDGE ( 'NONE', *, *, #8923, .F. ) ;
#6237=FACE_OUTER_BOUND ( 'NONE', #12721, .T. ) ;
#6248=ORIENTED_EDGE ( 'NONE', *, *, #15190, .F. ) ;
#6249=CARTESIAN_POINT ( 'NONE',  ( 5.592662329148081923, 2.365617111880286672, 4.427078738979575157 ) ) ;
#6251=AXIS2_PLACEMENT_3D ( 'NONE', #3846, #6462, #10025 ) ;
#6255=FACE_OUTER_BOUND ( 'NONE', #3515, .T. ) ;
#6266=CARTESIAN_POINT ( 'NONE',  ( 11.10165801154622933, 0.7750707670001704130, -165.0650903923130102 ) ) ;
#6267=LINE ( 'NONE', #5108, #10043 ) ;
#6269=FACE_OUTER_BOUND ( 'NONE', #13442, .T. ) ;
#6270=DIRECTION ( 'NONE',  ( 1.420304845956009546E-14, 0.000000000000000000, 1.000000000000000000 ) ) ;
#6271=CARTESIAN_POINT ( 'NONE',  ( 7.721531454929292160, 1.697151707906022766, 2.086477409661676052 ) ) ;
#6276=CARTESIAN_POINT ( 'NONE',  ( -12.98043033971411120, 4.000000000000098588, -189.9700568513258077 ) ) ;
#6287=VECTOR ( 'NONE', #10713, 1000.000000000000000 ) ;
#6288=CARTESIAN_POINT ( 'NONE',  ( -8.249568998113842255, 15.00000000000488676, -121.3053947661176011 ) ) ;
#6291=CARTESIAN_POINT ( 'NONE',  ( -4.439363805772839733, 8.673617379884035472E-16, -116.8256146818904284 ) ) ;
#6292=ORIENTED_EDGE ( 'NONE', *, *, #14235, .T. ) ;
#6294=CARTESIAN_POINT ( 'NONE',  ( 4.999999999999998224, 0.000000000000000000, -45.97309604003007877 ) ) ;
#6302=CARTESIAN_POINT ( 'NONE',  ( -4.869293993583121427, 14.99999999999999822, -118.1204535358624668 ) ) ;
#6304=CARTESIAN_POINT ( 'NONE',  ( 4.033098156699464809, 0.09438068890155107415, -1.663700395152567513 ) ) ;
#6306=CARTESIAN_POINT ( 'NONE',  ( 9.990846742651561030, 12.61469588961295685, -45.61014022669046142 ) ) ;
#6310=EDGE_CURVE ( 'NONE', #5770, #3245, #4417, .T. ) ;
#6311=CARTESIAN_POINT ( 'NONE',  ( -25.10304974847495885, 1.257220125218194262, -206.1099825640657457 ) ) ;
#6322=CARTESIAN_POINT ( 'NONE',  ( 11.32911568598997398, 4.648160439535026001, -106.8195553340705715 ) ) ;
#6327=CARTESIAN_POINT ( 'NONE',  ( 27.03835353835733102, 4.606906972193065997, -138.2189567786153361 ) ) ;
#6341=CARTESIAN_POINT ( 'NONE',  ( 5.000000000000000000, 1.301042606982605321E-15, -45.97309604003012851 ) ) ;
#6345=CARTESIAN_POINT ( 'NONE',  ( 1.041519256436020280, 6.000000000000000000, -139.4527716894433240 ) ) ;
#6346=CARTESIAN_POINT ( 'NONE',  ( -6.790153584124027475, 6.000000000000000000, -124.9643354754709748 ) ) ;
#6347=CARTESIAN_POINT ( 'NONE',  ( -25.27664434398002413, -9.897139991990234887E-31, -198.2936395105848817 ) ) ;
#6352=CARTESIAN_POINT ( 'NONE',  ( -28.78613703841196170, 8.673617379884035472E-16, -206.1746911135453786 ) ) ;
#6355=CARTESIAN_POINT ( 'NONE',  ( 8.895558325401111688, 6.000000000000000000, -141.4560052469132643 ) ) ;
#6357=CARTESIAN_POINT ( 'NONE',  ( -9.678328886309413903, 4.277268689446015237, -116.3720502296793597 ) ) ;
#6364=CARTESIAN_POINT ( 'NONE',  ( -6.790153584124027475, 9.999999999999998224, -124.9643354754709748 ) ) ;
#6365=CARTESIAN_POINT ( 'NONE',  ( 8.769209038263809930, 8.673617379884035472E-16, -110.8932515379864583 ) ) ;
#6367=CARTESIAN_POINT ( 'NONE',  ( 5.228075279701640099, 4.000000000000000000, -163.7939279834373849 ) ) ;
#6376=ADVANCED_FACE ( 'NONE', ( #779 ), #4090, .T. ) ;
#6377=CARTESIAN_POINT ( 'NONE',  ( -6.790153584124040798, 6.000000000000000000, -124.9643354754709748 ) ) ;
#6379=CARTESIAN_POINT ( 'NONE',  ( 5.841195078839528598, 3.026373079034796465, 4.845806430354895333 ) ) ;
#6390=EDGE_CURVE ( 'NONE', #10045, #8206, #7743, .T. ) ;
#6391=DIRECTION ( 'NONE',  ( -0.9997619372588932851, 0.000000000000000000, -0.02181900108494707474 ) ) ;
#6396=CARTESIAN_POINT ( 'NONE',  ( 9.933893833910557802, 5.000000000000000000, -126.1398084322751885 ) ) ;
#6402=PLANE ( 'NONE',  #4289 ) ;
#6403=CARTESIAN_POINT ( 'NONE',  ( 11.32016196453114709, 12.84598696167400966, -106.4092894439239956 ) ) ;
#6409=CARTESIAN_POINT ( 'NONE',  ( 10.97489477031424343, 5.773894334217324342, -44.95261552234883595 ) ) ;
#6414=CARTESIAN_POINT ( 'NONE',  ( 10.60542511503523144, 0.3690892158839738646, -164.4558062555837807 ) ) ;
#6415=CARTESIAN_POINT ( 'NONE',  ( 4.999884908348398049, 0.09438068890155060231, -1.653151978968578462 ) ) ;
#6416=CARTESIAN_POINT ( 'NONE',  ( -27.69328214320417914, 3.999999999999152678, -176.5249485101540472 ) ) ;
#6427=DIRECTION ( 'NONE',  ( 0.000000000000000000, 0.000000000000000000, 1.000000000000000000 ) ) ;
#6431=VECTOR ( 'NONE', #14580, 1000.000000000000000 ) ;
#6439=CARTESIAN_POINT ( 'NONE',  ( 4.739435512632367953, 0.000000000000000000, -107.5260682476390599 ) ) ;
#6441=CARTESIAN_POINT ( 'NONE',  ( 0.5944212552585367293, 0.000000000000000000, -138.5540974747773930 ) ) ;
#6444=CARTESIAN_POINT ( 'NONE',  ( 4.995485589807067583, 4.000000000000000888, -172.1291219214232626 ) ) ;
#6451=CARTESIAN_POINT ( 'NONE',  ( 6.122889832264990062, 5.000000000000000888, 5.281130614573720905 ) ) ;
#6453=CARTESIAN_POINT ( 'NONE',  ( 5.017237182712672272, 1.294471991313842052, 3.318667728194383049 ) ) ;
#6456=DIRECTION ( 'NONE',  ( 0.9997619372588931741, 0.000000000000000000, 0.02181900108494707474 ) ) ;
#6462=DIRECTION ( 'NONE',  ( -0.9997619372588932851, 0.000000000000000000, -0.02181900108494707474 ) ) ;
#6471=CARTESIAN_POINT ( 'NONE',  ( 3.902875325215932723, 5.000000000000000000, -114.6800873586639824 ) ) ;
#6473=ORIENTED_EDGE ( 'NONE', *, *, #9323, .T. ) ;
#6474=EDGE_CURVE ( 'NONE', #4341, #788, #5647, .T. ) ;
#6480=CARTESIAN_POINT ( 'NONE',  ( 13.78275167297412906, 6.000000000000000000, -126.2206732457524794 ) ) ;
#6487=CARTESIAN_POINT ( 'NONE',  ( -6.885999823355456684, 0.6080386061245605100, -116.9934166929402153 ) ) ;
#6492=VECTOR ( 'NONE', #4550, 1000.000000000000000 ) ;
#6494=B_SPLINE_CURVE_WITH_KNOTS ( 'NONE', 3,
 ( #5407, #5486, #9039, #14126, #7068, #10204, #10122, #4334, #11787, #14863, #5558, #3158, #4260, #4614, #13692, #10711, #3605, #1284, #5987, #4761, #8307, #13035, #7136, #2443 ),
 .UNSPECIFIED., .F., .F.,
 ( 4, 2, 2, 2, 2, 2, 2, 2, 2, 2, 2, 4 ),
 ( 1.734723475976807094E-18, 0.001351098920114992023, 0.002702197840229982311, 0.005404395680459964622, 0.006755494600574955127, 0.008106593520689946500, 0.01080879136091992924, 0.01215989028103492062, 0.01351098920114990852, 0.01621318704137988953, 0.01891538488160987574, 0.02161758272183985502 ),
 .UNSPECIFIED. ) ;
#6495=EDGE_CURVE ( 'NONE', #10451, #14561, #8736, .T. ) ;
#6496=CARTESIAN_POINT ( 'NONE',  ( -17.26415303358039921, 3.151119262966928298E-15, -158.1413053092271070 ) ) ;
#6504=DIRECTION ( 'NONE',  ( -0.000000000000000000, 1.000000000000000000, -0.000000000000000000 ) ) ;
#6517=DIRECTION ( 'NONE',  ( 0.000000000000000000, -1.000000000000000000, 0.000000000000000000 ) ) ;
#6518=CARTESIAN_POINT ( 'NONE',  ( 8.425472749275192186, 2.176832918059240114E-13, -115.5475827924868071 ) ) ;
#6530=ORIENTED_EDGE ( 'NONE', *, *, #14256, .F. ) ;
#6532=AXIS2_PLACEMENT_3D ( 'NONE', #5769, #1138, #7138 ) ;
#6533=CARTESIAN_POINT ( 'NONE',  ( 12.76858567064540217, 3.999999999993260502, -166.6103056774037441 ) ) ;
#6534=CARTESIAN_POINT ( 'NONE',  ( 9.948235151679879706, 12.61502403974950326, -43.65837861547728238 ) ) ;
#6538=CARTESIAN_POINT ( 'NONE',  ( 8.330271663116334935, 14.99999999999953282, -113.1592731357334003 ) ) ;
#6541=CARTESIAN_POINT ( 'NONE',  ( -24.38883959582580729, 4.000000000000000888, -168.5529178378782262 ) ) ;
#6543=ORIENTED_EDGE ( 'NONE', *, *, #11272, .F. ) ;
#6552=DIRECTION ( 'NONE',  ( -0.000000000000000000, -1.000000000000000000, -0.000000000000000000 ) ) ;
#6559=CARTESIAN_POINT ( 'NONE',  ( 10.93719894220377320, 13.85079060082045466, -106.6657003074759587 ) ) ;
#6568=CARTESIAN_POINT ( 'NONE',  ( 1.114947364559093712, 6.000000000000000000, -139.4079432275550232 ) ) ;
#6571=ORIENTED_EDGE ( 'NONE', *, *, #2786, .T. ) ;
#6572=CARTESIAN_POINT ( 'NONE',  ( -17.92852900003595806, 3.999999999999993783, -157.6654428080335890 ) ) ;
#6577=DIRECTION ( 'NONE',  ( -0.02058562339462809143, 0.3314513491899346298, 0.9432477061883728364 ) ) ;
#6578=CARTESIAN_POINT ( 'NONE',  ( 11.32016196459912649, 5.000000000000000888, -106.4092894470390291 ) ) ;
#6579=CYLINDRICAL_SURFACE ( 'NONE', #10218, 16.00000000006737721 ) ;
#6581=CARTESIAN_POINT ( 'NONE',  ( -6.992168204689655830, 14.99999999999999645, -113.2636094677312855 ) ) ;
#6582=CARTESIAN_POINT ( 'NONE',  ( -9.385448347264278013, 5.000000000000000888, -115.3551636530117293 ) ) ;
#6599=CARTESIAN_POINT ( 'NONE',  ( 9.943023108890812978, 5.000000000000002665, -43.30782091980648829 ) ) ;
#6605=CIRCLE ( 'NONE', #9316, 0.9999999999999988898 ) ;
#6607=B_SPLINE_CURVE_WITH_KNOTS ( 'NONE', 3,
 ( #4535, #4382, #12569, #1835, #12729, #679, #11331, #4456, #5462, #5534, #9090, #9015, #9247, #13972, #10254, #7700, #7852, #5384 ),
 .UNSPECIFIED., .F., .F.,
 ( 4, 2, 2, 2, 2, 2, 2, 2, 4 ),
 ( 1.734723475976807094E-18, 0.001049529208182716509, 0.002099058416365431282, 0.003148587624548146273, 0.004198116832730860830, 0.005247646040913573652, 0.006297175249096287342, 0.007346704457279000164, 0.008396233665461712986 ),
 .UNSPECIFIED. ) ;
#6608=CARTESIAN_POINT ( 'NONE',  ( 9.991047690016531035, 12.61351667247251740, -45.61670005978161413 ) ) ;
#6609=EDGE_CURVE ( 'NONE', #3281, #11204, #5850, .T. ) ;
#6611=CARTESIAN_POINT ( 'NONE',  ( 13.58051105728158880, 13.61566402447629365, -126.1567731084821702 ) ) ;
#6613=CARTESIAN_POINT ( 'NONE',  ( -9.868623142304215889, 10.39218436379010591, -115.7530035197778631 ) ) ;
#6615=CARTESIAN_POINT ( 'NONE',  ( 8.459890227587649747, 14.99999999999906386, -115.7934283673361477 ) ) ;
#6616=CARTESIAN_POINT ( 'NONE',  ( -7.749031843371196437, 13.85782642611278170, -116.8124745394366641 ) ) ;
#6618=VERTEX_POINT ( 'NONE', #4400 ) ;
#6620=FACE_OUTER_BOUND ( 'NONE', #1442, .T. ) ;
#6623=CARTESIAN_POINT ( 'NONE',  ( -4.234402844927150689, 0.000000000000000000, -117.4888040839639558 ) ) ;
#6630=CARTESIAN_POINT ( 'NONE',  ( 20.29380258822241956, 5.000000000000000888, -132.2785196063218223 ) ) ;
#6639=CARTESIAN_POINT ( 'NONE',  ( -7.289398910521280861, 0.9469664532186193862, -116.2745874757426776 ) ) ;
#6645=VERTEX_POINT ( 'NONE', #6796 ) ;
#6646=CARTESIAN_POINT ( 'NONE',  ( -12.67859807986386400, 2.739772825377753718E-13, -152.4516537531287099 ) ) ;
#6648=( BOUNDED_SURFACE ( )  B_SPLINE_SURFACE ( 3, 2, ( 
 ( #1554, #13310, #7177 ),
 ( #3639, #3796, #6105 ),
 ( #400, #9584, #8501 ),
 ( #14480, #14310, #9824 ),
 ( #8341, #2482, #14556 ),
 ( #10983, #8659, #13392 ),
 ( #13236, #8420, #2637 ),
 ( #12053, #11058, #321 ),
 ( #7499, #12219, #475 ),
 ( #11900, #7651, #12367 ),
 ( #10125, #6646, #10051 ),
 ( #13544, #7874, #2874 ),
 ( #6572, #6496, #8965 ),
 ( #7573, #1935, #553 ),
 ( #10208, #11284, #11356 ),
 ( #5265, #14790, #11213 ),
 ( #12292, #2943, #632 ),
 ( #705, #1785, #1702 ),
 ( #5411, #9975, #7807 ),
 ( #6416, #12447, #4184 ),
 ( #784, #5489, #8890 ),
 ( #9043, #13766, #14867 ),
 ( #5337, #859, #11135 ),
 ( #13622, #3023, #7730 ),
 ( #14714, #1867, #3161 ),
 ( #4263, #12595, #11437 ),
 ( #13695, #14942, #8815 ),
 ( #14638, #3093, #12519 ),
 ( #6724, #2014, #5561 ),
 ( #4035, #4337, #8740 ),
 ( #13471, #4113, #10507 ),
 ( #1080, #3392, #2166 ),
 ( #11514, #12673, #5855 ),
 ( #7018, #12827, #929 ),
 ( #6868, #2237, #7953 ),
 ( #11582, #2088, #6945 ),
 ( #3240, #10347, #11661 ),
 ( #9190, #2386, #13838 ),
 ( #15241, #6799, #14145 ),
 ( #10276, #15313, #4708 ),
 ( #5786, #10574, #1152 ),
 ( #5631, #9112, #12981 ) ),
 .UNSPECIFIED., .F., .F., .T. ) 
 B_SPLINE_SURFACE_WITH_KNOTS ( ( 4, 2, 2, 2, 2, 2, 2, 2, 2, 2, 2, 2, 2, 2, 2, 2, 2, 2, 2, 2, 4 ),
 ( 3, 3 ),
 ( 0.09990852050945690788, 0.1044989422773630605, 0.1090893640452691993, 0.1136797858131753519, 0.1159749966971284352, 0.1182702075810815046, 0.1274510511168938098, 0.1366318946527061151, 0.1412223164206122816, 0.1435175273045653510, 0.1458127381885184204, 0.1504031599564245592, 0.1549935817243306979, 0.1595840034922368367, 0.1618792143761899061, 0.1641744252601430032, 0.1664696361440961003, 0.1687648470280491697, 0.1699124524700257044, 0.1710600579120022391, 0.1733552687959553085 ),
 ( 0.1371266450457513664, 1.000000000000000000 ),
 .UNSPECIFIED. ) 
 GEOMETRIC_REPRESENTATION_ITEM ( )  RATIONAL_B_SPLINE_SURFACE ( (
 ( 0.9306880333625024981, 0.7472702456390873937, 1.000000000000000000),
 ( 0.9306880333625024981, 0.7472702456390873937, 1.000000000000000000),
 ( 0.9306880333625024981, 0.7472702456390873937, 1.000000000000000000),
 ( 0.9306880333625024981, 0.7472702456390873937, 1.000000000000000000),
 ( 0.9306880333625024981, 0.7472702456390873937, 1.000000000000000000),
 ( 0.9306880333625024981, 0.7472702456390873937, 1.000000000000000000),
 ( 0.9306880333625024981, 0.7472702456390873937, 1.000000000000000000),
 ( 0.9306880333625024981, 0.7472702456390873937, 1.000000000000000000),
 ( 0.9306880333625024981, 0.7472702456390873937, 1.000000000000000000),
 ( 0.9306880333625024981, 0.7472702456390873937, 1.000000000000000000),
 ( 0.9306880333625024981, 0.7472702456390873937, 1.000000000000000000),
 ( 0.9306880333625024981, 0.7472702456390873937, 1.000000000000000000),
 ( 0.9306880333625024981, 0.7472702456390875048, 1.000000000000000000),
 ( 0.9306880333625024981, 0.7472702456390875048, 1.000000000000000000),
 ( 0.9306880333625024981, 0.7472702456390873937, 1.000000000000000000),
 ( 0.9306880333625024981, 0.7472702456390873937, 1.000000000000000000),
 ( 0.9306880333625022761, 0.7472702456390867276, 1.000000000000000000),
 ( 0.9306880333625022761, 0.7472702456390867276, 1.000000000000000000),
 ( 0.9306880333625024981, 0.7472702456390873937, 1.000000000000000000),
 ( 0.9306880333625024981, 0.7472702456390873937, 1.000000000000000000),
 ( 0.9306880333625022761, 0.7472702456390867276, 1.000000000000000000),
 ( 0.9306880333625022761, 0.7472702456390867276, 1.000000000000000000),
 ( 0.9306880333625024981, 0.7472702456390873937, 1.000000000000000000),
 ( 0.9306880333625024981, 0.7472702456390873937, 1.000000000000000000),
 ( 0.9306880333625024981, 0.7472702456390876158, 1.000000000000000000),
 ( 0.9306880333625024981, 0.7472702456390876158, 1.000000000000000000),
 ( 0.9306880333625024981, 0.7472702456390873937, 1.000000000000000000),
 ( 0.9306880333625024981, 0.7472702456390873937, 1.000000000000000000),
 ( 0.9306880333625024981, 0.7472702456390873937, 1.000000000000000000),
 ( 0.9306880333625024981, 0.7472702456390873937, 1.000000000000000000),
 ( 0.9306880333625024981, 0.7472702456390873937, 1.000000000000000000),
 ( 0.9306880333625024981, 0.7472702456390873937, 1.000000000000000000),
 ( 0.9306880333625024981, 0.7472702456390873937, 1.000000000000000000),
 ( 0.9306880333625024981, 0.7472702456390873937, 1.000000000000000000),
 ( 0.9306880333625024981, 0.7472702456390873937, 1.000000000000000000),
 ( 0.9306880333625024981, 0.7472702456390873937, 1.000000000000000000),
 ( 0.9306880333625024981, 0.7472702456390873937, 1.000000000000000000),
 ( 0.9306880333625024981, 0.7472702456390873937, 1.000000000000000000),
 ( 0.9306880333625024981, 0.7472702456390875048, 1.000000000000000000),
 ( 0.9306880333625024981, 0.7472702456390875048, 1.000000000000000000),
 ( 0.9306880333625024981, 0.7472702456390875048, 1.000000000000000000),
 ( 0.9306880333625024981, 0.7472702456390875048, 1.000000000000000000) ) ) 
 REPRESENTATION_ITEM ( '' )  SURFACE ( )  );
#6650=EDGE_CURVE ( 'NONE', #881, #13240, #12544, .T. ) ;
#6655=CARTESIAN_POINT ( 'NONE',  ( 27.03835354040200301, 5.000000000000000888, -138.2189567750508843 ) ) ;
#6656=CARTESIAN_POINT ( 'NONE',  ( -8.199037228205272143, 9.999999999999998224, -114.3845095685594515 ) ) ;
#6657=CARTESIAN_POINT ( 'NONE',  ( -0.9685250182421367704, 1.734723475976807094E-15, -114.0968640496182758 ) ) ;
#6659=CARTESIAN_POINT ( 'NONE',  ( 25.81993756852972055, 5.000000000000000888, -140.3392227823892711 ) ) ;
#6669=CARTESIAN_POINT ( 'NONE',  ( 26.58801926426209405, 5.000000000000000888, -139.0072983920785532 ) ) ;
#6671=EDGE_CURVE ( 'NONE', #2663, #4737, #2316, .T. ) ;
#6672=CARTESIAN_POINT ( 'NONE',  ( 10.95703558056505500, 5.830465020145126687, -43.93897169094196187 ) ) ;
#6673=CARTESIAN_POINT ( 'NONE',  ( 8.779290816849703916, 4.000000000000000888, -169.2528061090708036 ) ) ;
#6676=ADVANCED_FACE ( 'NONE', ( #12028 ), #8818, .T. ) ;
#6685=CARTESIAN_POINT ( 'NONE',  ( 6.122889832264990062, 5.000000000000000888, 5.281130614573720905 ) ) ;
#6686=CARTESIAN_POINT ( 'NONE',  ( -9.678328886308937840, 10.72273131055397499, -116.3720502296813351 ) ) ;
#6688=CARTESIAN_POINT ( 'NONE',  ( 11.86796838807922683, 14.99999999999814904, -123.5172601095007394 ) ) ;
#6690=CARTESIAN_POINT ( 'NONE',  ( 24.96080173480166664, 1.421781986531464703, -137.5233644729144089 ) ) ;
#6691=ORIENTED_EDGE ( 'NONE', *, *, #2786, .F. ) ;
#6694=CARTESIAN_POINT ( 'NONE',  ( -30.70919553297256854, 4.000000000000000000, -193.1083921911521202 ) ) ;
#6697=EDGE_CURVE ( 'NONE', #12980, #191, #6742, .T. ) ;
#6699=DIRECTION ( 'NONE',  ( 0.000000000000000000, 0.000000000000000000, 1.000000000000000000 ) ) ;
#6703=CARTESIAN_POINT ( 'NONE',  ( -25.11906781955737600, 1.301042606982605321E-15, -198.9681998140721078 ) ) ;
#6704=CARTESIAN_POINT ( 'NONE',  ( -3.209935562023551459, -4.336808689942017736E-15, -120.5710852812284486 ) ) ;
#6708=ORIENTED_EDGE ( 'NONE', *, *, #11316, .F. ) ;
#6711=CARTESIAN_POINT ( 'NONE',  ( 9.926458935752712875, 14.67694112073403545, -106.4744043681741488 ) ) ;
#6714=CARTESIAN_POINT ( 'NONE',  ( -9.203922670347726154, 3.629878870852026651, -115.4376859600374416 ) ) ;
#6724=CARTESIAN_POINT ( 'NONE',  ( -30.61853078688893248, 3.999999999999813483, -195.0175678202491554 ) ) ;
#6732=CARTESIAN_POINT ( 'NONE',  ( 6.323089772814207699, 14.75164004108358640, 1.862046969705240640 ) ) ;
#6733=CARTESIAN_POINT ( 'NONE',  ( -9.476787056091270145, 8.673617379884035472E-16, -115.4301398046334839 ) ) ;
#6742=( BOUNDED_CURVE ( )  B_SPLINE_CURVE ( 3, ( #3001, #12418, #610, #526 ),
 .UNSPECIFIED., .F., .F. ) 
 B_SPLINE_CURVE_WITH_KNOTS ( ( 4, 4 ),
 ( 2.332122453023544040, 2.380236920682249568 ),
 .UNSPECIFIED. ) 
 CURVE ( )  GEOMETRIC_REPRESENTATION_ITEM ( )  RATIONAL_B_SPLINE_CURVE ( ( 1.000000000000000000, 0.9998070924708732932, 0.9998070924708732932, 1.000000000000000000 ) ) 
 REPRESENTATION_ITEM ( '' )  );
#6749=EDGE_LOOP ( 'NONE', ( #14946, #3203 ) ) ;
#6750=CARTESIAN_POINT ( 'NONE',  ( 4.624333745513747651, 15.00000000000000000, -103.8844720882033954 ) ) ;
#6752=VECTOR ( 'NONE', #5070, 1000.000000000000000 ) ;
#6754=CARTESIAN_POINT ( 'NONE',  ( 12.93066528927006331, 3.999999999993260502, -166.5029444825368614 ) ) ;
#6764=CARTESIAN_POINT ( 'NONE',  ( 7.523470539541117219, 15.00000000000000000, -107.6366068479289311 ) ) ;
#6766=ORIENTED_EDGE ( 'NONE', *, *, #12216, .F. ) ;
#6767=CARTESIAN_POINT ( 'NONE',  ( 25.97223239244240389, 2.194422113489858717, -138.3554727711511134 ) ) ;
#6769=VERTEX_POINT ( 'NONE', #1069 ) ;
#6771=CARTESIAN_POINT ( 'NONE',  ( -16.34918561525985936, 4.000000000000000888, -155.5261654759235057 ) ) ;
#6773=EDGE_LOOP ( 'NONE', ( #12346, #9013, #4589, #2604 ) ) ;
#6774=FACE_OUTER_BOUND ( 'NONE', #11730, .T. ) ;
#6778=CARTESIAN_POINT ( 'NONE',  ( -25.11906781955737600, 1.301042606982605321E-15, -198.9681998140721078 ) ) ;
#6780=CARTESIAN_POINT ( 'NONE',  ( -1.947391641747792779, -6.071532165918824830E-15, -123.5657085572418339 ) ) ;
#6784=CARTESIAN_POINT ( 'NONE',  ( 1.266169042200451900, 4.000000000000000000, -139.9015330219193913 ) ) ;
#6786=ORIENTED_EDGE ( 'NONE', *, *, #837, .F. ) ;
#6789=DIRECTION ( 'NONE',  ( 0.000000000000000000, 1.000000000000000000, 0.000000000000000000 ) ) ;
#6796=CARTESIAN_POINT ( 'NONE',  ( 10.90625579228518838, 8.773889247172311556, -41.61220587883767053 ) ) ;
#6799=CARTESIAN_POINT ( 'NONE',  ( -26.63481489508266975, 3.005459392714369724E-12, -206.0878104404494309 ) ) ;
#6805=CARTESIAN_POINT ( 'NONE',  ( 8.983555716587311224, 12.48436874840615474, 0.6556481286397073394 ) ) ;
#6806=CARTESIAN_POINT ( 'NONE',  ( -3.294555838623477229, 1.734723475976807094E-15, -108.9576586821670929 ) ) ;
#6812=FACE_OUTER_BOUND ( 'NONE', #1871, .T. ) ;
#6813=CARTESIAN_POINT ( 'NONE',  ( 1.320501113854927633, 6.000000000000000000, -137.8664870916819893 ) ) ;
#6816=CARTESIAN_POINT ( 'NONE',  ( -9.721966606378851239, 10.00000000000000000, -116.3614657639809309 ) ) ;
#6820=CARTESIAN_POINT ( 'NONE',  ( 2.112978062913205779, 8.673617379884035472E-16, -168.2508114127782903 ) ) ;
#6824=EDGE_LOOP ( 'NONE', ( #3989, #268, #2356 ) ) ;
#6826=CARTESIAN_POINT ( 'NONE',  ( 30.99422529207408772, 8.773889247172311556, -45.42481409048903629 ) ) ;
#6830=CARTESIAN_POINT ( 'NONE',  ( 8.428994341650765776, 12.49999999999999822, -112.3028785388504218 ) ) ;
#6831=CARTESIAN_POINT ( 'NONE',  ( -6.572203743845812518, 14.53696891565361327, -117.0568686706825332 ) ) ;
#6833=CARTESIAN_POINT ( 'NONE',  ( 26.90873434660125341, 2.875118758487606563, -137.5417689853771606 ) ) ;
#6836=ORIENTED_EDGE ( 'NONE', *, *, #7622, .T. ) ;
#6838=DIRECTION ( 'NONE',  ( 0.9997619372588930631, 0.000000000000000000, 0.02181900108494949642 ) ) ;
#6842=ORIENTED_EDGE ( 'NONE', *, *, #11652, .F. ) ;
#6844=DIRECTION ( 'NONE',  ( 0.000000000000000000, 1.000000000000000000, 0.000000000000000000 ) ) ;
#6847=B_SPLINE_CURVE_WITH_KNOTS ( 'NONE', 3,
 ( #6978, #8210, #2417, #12709, #10536, #11762, #12941, #11542, #10464, #1182, #15269, #15122, #14180, #5965, #14254, #2122, #3585, #957 ),
 .UNSPECIFIED., .F., .F.,
 ( 4, 2, 2, 2, 2, 2, 2, 2, 4 ),
 ( 1.734723475976807094E-18, 0.004481983308881167319, 0.006722974963321751846, 0.008963966617762334638, 0.01120495827220291916, 0.01344594992664350716, 0.01456644575386379682, 0.01568694158108408648, 0.01792793323552462764 ),
 .UNSPECIFIED. ) ;
#6848=CARTESIAN_POINT ( 'NONE',  ( -25.44770677137621107, 3.658198091069090996, -208.9169813633941430 ) ) ;
#6852=CARTESIAN_POINT ( 'NONE',  ( 10.42535907228127279, 5.000000000000000000, -121.1971725648922700 ) ) ;
#6853=CARTESIAN_POINT ( 'NONE',  ( 30.96695154071790412, 8.773889247172311556, -44.17511166891541308 ) ) ;
#6857=DIRECTION ( 'NONE',  ( 1.000000000000000000, 0.000000000000000000, -8.764770998266003672E-18 ) ) ;
#6868=CARTESIAN_POINT ( 'NONE',  ( -28.93490687045225229, 4.000000000000780709, -203.2856232654508517 ) ) ;
#6872=ORIENTED_EDGE ( 'NONE', *, *, #13598, .F. ) ;
#6874=EDGE_CURVE ( 'NONE', #14600, #5913, #5525, .T. ) ;
#6875=CARTESIAN_POINT ( 'NONE',  ( -25.45473766001728322, 3.555369740890242269, -208.8630699688340826 ) ) ;
#6876=CARTESIAN_POINT ( 'NONE',  ( 8.899585189996612300, 13.22278168266239717, 4.503236568198851764 ) ) ;
#6877=CARTESIAN_POINT ( 'NONE',  ( -0.8896971555406301135, 5.000000000000000888, -104.6801027822243100 ) ) ;
#6879=CARTESIAN_POINT ( 'NONE',  ( 15.16156648847430688, 6.947217876059453517E-12, -161.5519024490983213 ) ) ;
#6883=CARTESIAN_POINT ( 'NONE',  ( 26.71007981443199952, 5.000000000000000888, -136.8791680534710054 ) ) ;
#6890=CARTESIAN_POINT ( 'NONE',  ( 5.147364755317443752, 4.000000000000000000, -172.0982971393951289 ) ) ;
#6894=ORIENTED_EDGE ( 'NONE', *, *, #8374, .T. ) ;
#6901=CIRCLE ( 'NONE', #11352, 0.4999999999999726885 ) ;
#6903=CARTESIAN_POINT ( 'NONE',  ( 10.14688567197878477, 15.00000000000115996, -108.1982192591100755 ) ) ;
#6905=ORIENTED_EDGE ( 'NONE', *, *, #11967, .T. ) ;
#6908=VERTEX_POINT ( 'NONE', #4451 ) ;
#6914=VERTEX_POINT ( 'NONE', #2135 ) ;
#6916=CARTESIAN_POINT ( 'NONE',  ( -1.030030361948892192, 9.999999999999998224, -105.0143096064267780 ) ) ;
#6920=CARTESIAN_POINT ( 'NONE',  ( -25.07851259296351643, 1.351337947789349903, -206.3038523730356815 ) ) ;
#6921=DIRECTION ( 'NONE',  ( 0.02181900108494707127, 0.000000000000000000, -0.9997619372588931741 ) ) ;
#6922=ADVANCED_FACE ( 'NONE', ( #6620 ), #3135, .T. ) ;
#6925=EDGE_CURVE ( 'NONE', #673, #40, #13089, .T. ) ;
#6926=LINE ( 'NONE', #1204, #6287 ) ;
#6928=CARTESIAN_POINT ( 'NONE',  ( 30.96695154071790412, 8.773889247172311556, -44.17511166891541308 ) ) ;
#6931=LINE ( 'NONE', #8017, #12170 ) ;
#6932=AXIS2_PLACEMENT_3D ( 'NONE', #7818, #2954, #9126 ) ;
#6941=EDGE_CURVE ( 'NONE', #14015, #6908, #1827, .T. ) ;
#6942=CARTESIAN_POINT ( 'NONE',  ( 5.228075279701640099, 1.000000000000000000, -167.7939279834373849 ) ) ;
#6943=AXIS2_PLACEMENT_3D ( 'NONE', #11949, #8549, #13125 ) ;
#6945=CARTESIAN_POINT ( 'NONE',  ( -23.88626836071575354, 8.673617379884035472E-16, -202.5895577731797061 ) ) ;
#6949=ORIENTED_EDGE ( 'NONE', *, *, #9600, .T. ) ;
#6951=DIRECTION ( 'NONE',  ( -0.9997619372588932851, -0.000000000000000000, -0.02181900108494707821 ) ) ;
#6952=CARTESIAN_POINT ( 'NONE',  ( 8.921562004896541609, 14.16567896455317843, 3.496243491202363440 ) ) ;
#6953=CARTESIAN_POINT ( 'NONE',  ( -1.334601435094046273, 8.673617379884035472E-16, -105.6792246796767074 ) ) ;
#6960=CARTESIAN_POINT ( 'NONE',  ( 27.03835354040190708, 6.000000000000000000, -138.2189567750509696 ) ) ;
#6962=ADVANCED_FACE ( 'NONE', ( #8369 ), #5977, .T. ) ;
#6963=CARTESIAN_POINT ( 'NONE',  ( 26.07883353259989434, 2.736193318683750597, -137.1131491302461995 ) ) ;
#6971=CARTESIAN_POINT ( 'NONE',  ( -10.64937093114562217, 4.000000000002276401, -187.1793336183638985 ) ) ;
#6975=ORIENTED_EDGE ( 'NONE', *, *, #12555, .F. ) ;
#6978=CARTESIAN_POINT ( 'NONE',  ( -9.385448347264267355, 5.000000000000000888, -115.3551636530117150 ) ) ;
#6983=CARTESIAN_POINT ( 'NONE',  ( 11.13433036043491242, 15.00000000000000000, -107.0267359326556971 ) ) ;
#6984=CARTESIAN_POINT ( 'NONE',  ( 16.81337476694494626, 0.000000000000000000, -129.2521154344591139 ) ) ;
#6985=VERTEX_POINT ( 'NONE', #1125 ) ;
#6986=CIRCLE ( 'NONE', #8463, 2.000000000000000000 ) ;
#6989=ORIENTED_EDGE ( 'NONE', *, *, #8941, .F. ) ;
#6991=CARTESIAN_POINT ( 'NONE',  ( -25.42939282183900573, 4.000000000000000000, -209.0516719515502473 ) ) ;
#6995=CARTESIAN_POINT ( 'NONE',  ( -3.294555838741347831, 9.999999999999998224, -108.9576586820926281 ) ) ;
#6999=CARTESIAN_POINT ( 'NONE',  ( -25.58997729346963013, 2.130041082828657562, -207.6174152824262080 ) ) ;
#7004=ORIENTED_EDGE ( 'NONE', *, *, #5550, .T. ) ;
#7012=VECTOR ( 'NONE', #6517, 1000.000000000000000 ) ;
#7017=ORIENTED_EDGE ( 'NONE', *, *, #11652, .T. ) ;
#7018=CARTESIAN_POINT ( 'NONE',  ( -29.26478672069536913, 4.000000000000235367, -202.3577337911947609 ) ) ;
#7024=CARTESIAN_POINT ( 'NONE',  ( -25.11906781955738310, 0.000000000000000000, -198.9681998140721078 ) ) ;
#7025=CARTESIAN_POINT ( 'NONE',  ( 6.209053725235345489, 13.78527700952190571, 3.560231868336729111 ) ) ;
#7029=CARTESIAN_POINT ( 'NONE',  ( 3.391286578035700217, 8.673617379884033500E-16, -107.3770126362747419 ) ) ;
#7031=PLANE ( 'NONE',  #6188 ) ;
#7032=CARTESIAN_POINT ( 'NONE',  ( 1.004809442601929836, 5.333333333333333925, -139.4752805618705622 ) ) ;
#7037=ORIENTED_EDGE ( 'NONE', *, *, #13014, .F. ) ;
#7039=CARTESIAN_POINT ( 'NONE',  ( 8.360009203849724457, 12.50000000000000000, -115.0372004058238389 ) ) ;
#7047=EDGE_CURVE ( 'NONE', #881, #16, #15282, .T. ) ;
#7049=CARTESIAN_POINT ( 'NONE',  ( 4.184249394548969825, 8.673617379884035472E-16, -108.7922730648138696 ) ) ;
#7051=DIRECTION ( 'NONE',  ( -0.04581719776170027625, 0.000000000000000000, 0.9989498407774363153 ) ) ;
#7054=CYLINDRICAL_SURFACE ( 'NONE', #11120, 5.000000000000000000 ) ;
#7062=CARTESIAN_POINT ( 'NONE',  ( -2.424117393064570525, 15.00000000000080824, -107.6599666632758527 ) ) ;
#7064=EDGE_CURVE ( 'NONE', #15130, #1352, #2514, .T. ) ;
#7067=CARTESIAN_POINT ( 'NONE',  ( -1.258237567103696941, -6.071532165918825619E-15, -125.0317944887032979 ) ) ;
#7068=CARTESIAN_POINT ( 'NONE',  ( 7.484376272073578029, 15.00000000000000000, -107.6919899575756006 ) ) ;
#7076=CARTESIAN_POINT ( 'NONE',  ( 30.96695154071790412, 8.773889247172311556, -44.17511166891541308 ) ) ;
#7078=CARTESIAN_POINT ( 'NONE',  ( 9.292954653762432571, 0.9864195427336619471, -105.8157378072028365 ) ) ;
#7082=ORIENTED_EDGE ( 'NONE', *, *, #1537, .T. ) ;
#7087=ORIENTED_EDGE ( 'NONE', *, *, #1771, .F. ) ;
#7091=CARTESIAN_POINT ( 'NONE',  ( 16.50094977371536231, 8.749999999999998224, -91.72275351520976017 ) ) ;
#7094=CARTESIAN_POINT ( 'NONE',  ( 4.018210755790066813, 8.673617379884037444E-16, -105.8455740756232473 ) ) ;
#7097=FACE_OUTER_BOUND ( 'NONE', #3347, .T. ) ;
#7114=CARTESIAN_POINT ( 'NONE',  ( 5.228075279701640099, 1.000000000000000000, -165.7939279834373849 ) ) ;
#7117=FACE_OUTER_BOUND ( 'NONE', #9269, .T. ) ;
#7118=CARTESIAN_POINT ( 'NONE',  ( 20.97724033793567600, 8.673617379884035472E-16, -139.0817640602418805 ) ) ;
#7121=FACE_OUTER_BOUND ( 'NONE', #3165, .T. ) ;
#7125=CARTESIAN_POINT ( 'NONE',  ( -26.77342622694935059, 4.000000000000000000, -207.3649691462522924 ) ) ;
#7130=CARTESIAN_POINT ( 'NONE',  ( 6.222982598701390700, 13.98190557557194502, 3.317519625265672456 ) ) ;
#7135=CARTESIAN_POINT ( 'NONE',  ( 11.30894640059546852, 0.7539637541287584899, -164.8338407189809232 ) ) ;
#7136=CARTESIAN_POINT ( 'NONE',  ( 9.697783895759762629, 15.00000000000000000, -124.7881275717043650 ) ) ;
#7138=DIRECTION ( 'NONE',  ( 0.000000000000000000, 0.000000000000000000, -1.000000000000000000 ) ) ;
#7152=CARTESIAN_POINT ( 'NONE',  ( 9.025311242897139152, 0.8923617020100302888, -106.1611430900688191 ) ) ;
#7157=DIRECTION ( 'NONE',  ( -0.000000000000000000, -1.000000000000000000, -0.000000000000000000 ) ) ;
#7159=CARTESIAN_POINT ( 'NONE',  ( 8.251486519976570122, 2.457945381532850249, 2.437901666522639399 ) ) ;
#7162=AXIS2_PLACEMENT_3D ( 'NONE', #11171, #11399, #2981 ) ;
#7164=ORIENTED_EDGE ( 'NONE', *, *, #6697, .F. ) ;
#7168=AXIS2_PLACEMENT_3D ( 'NONE', #4127, #7967, #4497 ) ;
#7172=CARTESIAN_POINT ( 'NONE',  ( 3.872594309009199876, 8.673617379884035472E-16, -106.2339216993545818 ) ) ;
#7177=CARTESIAN_POINT ( 'NONE',  ( 3.717577911061872076, 8.673617379884035472E-16, -143.6771719914432595 ) ) ;
#7185=CARTESIAN_POINT ( 'NONE',  ( -16.63253413790094726, 3.999999999999409361, -194.7535182948206511 ) ) ;
#7193=CARTESIAN_POINT ( 'NONE',  ( -7.409205697917243150, 0.9058721944443380858, -116.8849570398053572 ) ) ;
#7196=CARTESIAN_POINT ( 'NONE',  ( 3.312745690571184287, 8.673617379884035472E-16, -113.0297142168659263 ) ) ;
#7202=DIRECTION ( 'NONE',  ( 0.000000000000000000, 1.000000000000000000, 0.000000000000000000 ) ) ;
#7203=CARTESIAN_POINT ( 'NONE',  ( 11.96422411991965618, 8.673617379884035472E-16, -131.4923627482014012 ) ) ;
#7207=ORIENTED_EDGE ( 'NONE', *, *, #8371, .T. ) ;
#7209=CARTESIAN_POINT ( 'NONE',  ( -25.72020873159803855, 4.000000000000001776, -208.7304761312111623 ) ) ;
#7214=EDGE_CURVE ( 'NONE', #12142, #8185, #10956, .T. ) ;
#7215=CARTESIAN_POINT ( 'NONE',  ( 4.999999996894303855, 14.99999999999999822, -101.5775160893471138 ) ) ;
#7217=EDGE_CURVE ( 'NONE', #8407, #3224, #9786, .T. ) ;
#7222=CIRCLE ( 'NONE', #4760, 1.250000000000005107 ) ;
#7225=( BOUNDED_SURFACE ( )  B_SPLINE_SURFACE ( 3, 2, ( 
 ( #4947, #9663, #11818 ),
 ( #14394, #14308, #3709 ),
 ( #14785, #13469, #2872 ),
 ( #3874, #6414, #12048 ),
 ( #8575, #316, #8812 ),
 ( #6266, #1783, #4182 ),
 ( #9749, #2635, #8738 ),
 ( #12290, #1700, #11056 ),
 ( #10900, #10981, #12214 ),
 ( #11132, #7497, #550 ),
 ( #5261, #13233, #473 ),
 ( #9973, #14711, #7337 ),
 ( #4111, #13542, #2941 ),
 ( #14634, #9822, #7571 ),
 ( #5188, #1469, #6181 ),
 ( #4032, #5032, #14477 ) ),
 .UNSPECIFIED., .F., .F., .F. ) 
 B_SPLINE_SURFACE_WITH_KNOTS ( ( 4, 2, 2, 2, 2, 2, 2, 4 ),
 ( 3, 3 ),
 ( -1.714383521174504596E-05, 0.001390813748932505714, 0.002094792541004631119, 0.002798771333076756525, 0.003502750125148881930, 0.004206728917221007336, 0.004910707709293133175, 0.005614686501365258146 ),
 ( 0.000000000000000000, 1.000000000000000000 ),
 .UNSPECIFIED. ) 
 GEOMETRIC_REPRESENTATION_ITEM ( )  RATIONAL_B_SPLINE_SURFACE ( (
 ( 1.000000000000000000, 1.000000000000000000, 1.000000000000000000),
 ( 1.000000000000000000, 1.000000047483659893, 1.000000000000000000),
 ( 1.000000000000000000, 0.9984278383163904813, 1.000000000000000000),
 ( 1.000000000000000000, 0.9939583932889539675, 1.000000000000000000),
 ( 1.000000000000000000, 0.9921436623915373954, 1.000000000000000000),
 ( 1.000000000000000000, 0.9880575292902304962, 1.000000000000000000),
 ( 1.000000000000000000, 0.9857791852598755122, 1.000000000000000000),
 ( 1.000000000000000000, 0.9809189248842778985, 1.000000000000000000),
 ( 1.000000000000000000, 0.9783729182749338893, 1.000000000000000000),
 ( 1.000000000000000000, 0.9733849987678442339, 1.000000000000000000),
 ( 1.000000000000000000, 0.9709255430829486500, 1.000000000000000000),
 ( 1.000000000000000000, 0.9663197370312965884, 1.000000000000000000),
 ( 1.000000000000000000, 0.9642109238660780957, 1.000000000000000000),
 ( 1.000000000000000000, 0.9606928177971931770, 1.000000000000000000),
 ( 1.000000000000000000, 0.9592645092514092697, 1.000000000000000000),
 ( 1.000000000000000000, 0.9582603755229887055, 1.000000000000000000) ) ) 
 REPRESENTATION_ITEM ( '' )  SURFACE ( )  );
#7231=EDGE_CURVE ( 'NONE', #13718, #7952, #10220, .T. ) ;
#7234=CARTESIAN_POINT ( 'NONE',  ( 1.004149434879655578, 5.000000000000000888, -139.4756852570866670 ) ) ;
#7237=LINE ( 'NONE', #14283, #48 ) ;
#7240=CARTESIAN_POINT ( 'NONE',  ( -4.203928810071235311, 14.18377006225550829, -125.2130536027671326 ) ) ;
#7241=CIRCLE ( 'NONE', #604, 4.000000000000002665 ) ;
#7245=CARTESIAN_POINT ( 'NONE',  ( 6.214735144181003257, 0.3805900070242324573, 2.672050388266886678 ) ) ;
#7264=CARTESIAN_POINT ( 'NONE',  ( -1.660557334999934076, 6.000000000000000000, -134.7186485042710729 ) ) ;
#7266=CARTESIAN_POINT ( 'NONE',  ( 5.376722707423876813, 0.1900852925348768263, -0.2357307375419829543 ) ) ;
#7270=ORIENTED_EDGE ( 'NONE', *, *, #4027, .F. ) ;
#7276=VERTEX_POINT ( 'NONE', #5139 ) ;
#7277=CARTESIAN_POINT ( 'NONE',  ( -4.890501715614620437, -7.342728488552128110E-10, -117.3116236002538812 ) ) ;
#7280=CARTESIAN_POINT ( 'NONE',  ( 3.843142374354968638, 8.673617379884033500E-16, -118.1836930616208008 ) ) ;
#7283=CARTESIAN_POINT ( 'NONE',  ( 5.000000000000001776, 15.00000000000000000, -1.663700395152567513 ) ) ;
#7284=CARTESIAN_POINT ( 'NONE',  ( -6.027592498023851775, -1.580622335394386225E-12, -126.6584150166784326 ) ) ;
#7285=CARTESIAN_POINT ( 'NONE',  ( 15.55318939603108852, 0.000000000000000000, -134.8337474659214479 ) ) ;
#7287=DIRECTION ( 'NONE',  ( 0.000000000000000000, 0.000000000000000000, 1.000000000000000000 ) ) ;
#7303=CARTESIAN_POINT ( 'NONE',  ( -24.89426390012435064, 2.111117962734504250, -207.5279892455088202 ) ) ;
#7304=ORIENTED_EDGE ( 'NONE', *, *, #4783, .T. ) ;
#7305=EDGE_CURVE ( 'NONE', #13571, #4732, #14217, .T. ) ;
#7314=CARTESIAN_POINT ( 'NONE',  ( 10.68883385149069198, 14.16521505008430459, -106.2696755902874628 ) ) ;
#7321=CARTESIAN_POINT ( 'NONE',  ( 7.278275680548385473, 1.096586756138080432, 3.954380374118978914 ) ) ;
#7323=EDGE_CURVE ( 'NONE', #6618, #5674, #3507, .T. ) ;
#7329=B_SPLINE_CURVE_WITH_KNOTS ( 'NONE', 3,
 ( #205, #11866, #9633, #4918, #14367, #130 ),
 .UNSPECIFIED., .F., .F.,
 ( 4, 2, 4 ),
 ( 0.000000000000000000, 0.004354769343283191457, 0.008709538686566382915 ),
 .UNSPECIFIED. ) ;
#7337=CARTESIAN_POINT ( 'NONE',  ( 12.74513938997514195, 2.668544226154935028, -165.8867193072528323 ) ) ;
#7341=CARTESIAN_POINT ( 'NONE',  ( 6.387831235576543421, 4.907497138154600617E-16, -139.1888589629733133 ) ) ;
#7343=CARTESIAN_POINT ( 'NONE',  ( -23.68520063642048257, 8.673617379884034486E-16, -180.0072976255214883 ) ) ;
#7347=VERTEX_POINT ( 'NONE', #5435 ) ;
#7349=CARTESIAN_POINT ( 'NONE',  ( -19.98060382417750702, 2.666703424072985286E-12, -198.2865109825601735 ) ) ;
#7354=CARTESIAN_POINT ( 'NONE',  ( -7.653276971142799923, 1.000796838352786100, -116.4876868865816704 ) ) ;
#7358=CARTESIAN_POINT ( 'NONE',  ( 26.71007981443199952, 15.00000000000000000, -136.8791680534710054 ) ) ;
#7362=CARTESIAN_POINT ( 'NONE',  ( 1.101407610004066395, 4.336808689942017736E-15, -129.3199319192200392 ) ) ;
#7363=CARTESIAN_POINT ( 'NONE',  ( 9.719609032807245086, 1.952651032223853462E-12, -108.8314952392251058 ) ) ;
#7367=ORIENTED_EDGE ( 'NONE', *, *, #665, .T. ) ;
#7373=CARTESIAN_POINT ( 'NONE',  ( -6.992168204849981805, 9.999999999999998224, -113.2636094675811762 ) ) ;
#7376=CARTESIAN_POINT ( 'NONE',  ( 13.08366191415227853, 3.715076940595480881, -166.1349492621538957 ) ) ;
#7387=CARTESIAN_POINT ( 'NONE',  ( -3.486117781607304345, 9.999999999999998224, -110.4977313129625145 ) ) ;
#7389=DIRECTION ( 'NONE',  ( 0.9997619372588932851, -0.000000000000000000, 0.02181900108494707474 ) ) ;
#7395=CARTESIAN_POINT ( 'NONE',  ( 4.513688785873243958, -0.0008058231150413114373, -1.375597706563020051 ) ) ;
#7403=CARTESIAN_POINT ( 'NONE',  ( 9.908994292421551719, 14.68779660164460488, -106.4646849496190697 ) ) ;
#7406=CIRCLE ( 'NONE', #11840, 1.750000000000001554 ) ;
#7416=AXIS2_PLACEMENT_3D ( 'NONE', #1849, #2859, #10109 ) ;
#7418=CARTESIAN_POINT ( 'NONE',  ( 8.895558325401111688, 15.00000000000000000, -125.4560052468458906 ) ) ;
#7420=CIRCLE ( 'NONE', #8662, 1.000000000000000888 ) ;
#7421=CARTESIAN_POINT ( 'NONE',  ( 7.013957603348227821, 1.025390859509332619, 1.559562445866058855 ) ) ;
#7426=CARTESIAN_POINT ( 'NONE',  ( 10.81715743844561040, 1.218752542932547250E-31, -159.0533339799537487 ) ) ;
#7434=EDGE_CURVE ( 'NONE', #1605, #5038, #8290, .T. ) ;
#7438=EDGE_CURVE ( 'NONE', #9933, #13240, #15192, .T. ) ;
#7442=CARTESIAN_POINT ( 'NONE',  ( -7.159798565106106238, 14.99999999999025491, -124.1957246867857805 ) ) ;
#7444=CARTESIAN_POINT ( 'NONE',  ( -2.035316908484686937, 5.000000000000002665, -133.6663417172228492 ) ) ;
#7445=CARTESIAN_POINT ( 'NONE',  ( 8.518838221474071659, 5.000000000000000888, -111.8377054444269589 ) ) ;
#7446=ORIENTED_EDGE ( 'NONE', *, *, #1290, .F. ) ;
#7448=DIRECTION ( 'NONE',  ( 0.9997619372588931741, 0.000000000000000000, 0.02181900108494707474 ) ) ;
#7456=ORIENTED_EDGE ( 'NONE', *, *, #1678, .T. ) ;
#7457=CARTESIAN_POINT ( 'NONE',  ( 11.32016196459912649, 15.00000000000000000, -106.4092894470390291 ) ) ;
#7459=B_SPLINE_CURVE_WITH_KNOTS ( 'NONE', 3,
 ( #322, #14943, #12756, #13767, #4185, #706, #13923, #11357, #9044, #2015, #12448, #1936, #10277, #14868, #3162, #633 ),
 .UNSPECIFIED., .F., .F.,
 ( 4, 2, 2, 2, 2, 2, 2, 4 ),
 ( -1.886160231747189032E-05, 0.0008577525216627750800, 0.001734366645643021891, 0.003487594893603512044, 0.004364209017583777286, 0.005240823141564042963, 0.006117437265544308639, 0.006994051389524575182 ),
 .UNSPECIFIED. ) ;
#7461=CARTESIAN_POINT ( 'NONE',  ( 10.90808873753844033, 14.95946075517707108, -125.5795451959731963 ) ) ;
#7465=CARTESIAN_POINT ( 'NONE',  ( -25.17801280822136789, 0.9699280507716093735, -205.4590613150332956 ) ) ;
#7475=CARTESIAN_POINT ( 'NONE',  ( 11.04730217058844843, 4.659658575842277273, -107.1178495013205350 ) ) ;
#7480=VERTEX_POINT ( 'NONE', #96 ) ;
#7481=CARTESIAN_POINT ( 'NONE',  ( 5.193879428909422558, 0.1412401001306463344, -0.6353294446044706056 ) ) ;
#7486=CARTESIAN_POINT ( 'NONE',  ( -0.3803025174127561692, 10.00000000000000000, -103.2080563861792086 ) ) ;
#7497=CARTESIAN_POINT ( 'NONE',  ( 12.23938344417887514, 1.900076854767284829, -165.8029585129606573 ) ) ;
#7498=CARTESIAN_POINT ( 'NONE',  ( 10.79862538543327410, 3.357576456925632780, -106.9941695556743184 ) ) ;
#7499=CARTESIAN_POINT ( 'NONE',  ( -11.63193767996857275, 3.999999999999993783, -150.0779743115209897 ) ) ;
#7501=CARTESIAN_POINT ( 'NONE',  ( -25.79454819560323031, 8.673617379884037444E-16, -193.5088923898361486 ) ) ;
#7505=ORIENTED_EDGE ( 'NONE', *, *, #6671, .F. ) ;
#7507=CARTESIAN_POINT ( 'NONE',  ( -15.21741835282884381, 3.999999999999802380, -192.8143658740737010 ) ) ;
#7509=AXIS2_PLACEMENT_3D ( 'NONE', #10691, #7202, #11920 ) ;
#7511=FACE_OUTER_BOUND ( 'NONE', #15120, .T. ) ;
#7512=ORIENTED_EDGE ( 'NONE', *, *, #4344, .T. ) ;
#7520=CARTESIAN_POINT ( 'NONE',  ( -3.538505488862558224, 15.00000000000000711, -119.6277774347352079 ) ) ;
#7521=CARTESIAN_POINT ( 'NONE',  ( -8.651617673336016168, 2.768730321972320486E-12, -120.1343837247038380 ) ) ;
#7522=CARTESIAN_POINT ( 'NONE',  ( 11.18419171849476790, 1.127570259384924454E-14, -106.9754176129513752 ) ) ;
#7523=ORIENTED_EDGE ( 'NONE', *, *, #13014, .T. ) ;
#7524=CARTESIAN_POINT ( 'NONE',  ( 4.999999999999999112, 0.000000000000000000, -100.6237003951525679 ) ) ;
#7526=VERTEX_POINT ( 'NONE', #10530 ) ;
#7527=EDGE_CURVE ( 'NONE', #14187, #13643, #1251, .T. ) ;
#7529=CARTESIAN_POINT ( 'NONE',  ( 21.60584812306049329, 0.02716718192045389224, -138.8895968602480195 ) ) ;
#7539=CARTESIAN_POINT ( 'NONE',  ( -4.234402844927157794, 15.00000000000000000, -117.4888040839639558 ) ) ;
#7541=DIRECTION ( 'NONE',  ( 0.9939692226109180240, -0.000000000000000000, -0.1096594022519158940 ) ) ;
#7542=ORIENTED_EDGE ( 'NONE', *, *, #7434, .T. ) ;
#7546=ADVANCED_FACE ( 'NONE', ( #15263 ), #11487, .T. ) ;
#7556=DIRECTION ( 'NONE',  ( -0.9997619372588932851, 0.000000000000000000, -0.02181900108494707474 ) ) ;
#7562=CARTESIAN_POINT ( 'NONE',  ( -1.653263949012560463, 10.00000000000000000, -106.3284344075506738 ) ) ;
#7563=CARTESIAN_POINT ( 'NONE',  ( 11.32911568800036584, 12.49999999999999822, -106.8195553349433169 ) ) ;
#7570=CARTESIAN_POINT ( 'NONE',  ( 4.516489297216762289, -0.0008961263506977127508, -1.658221315985885846 ) ) ;
#7571=CARTESIAN_POINT ( 'NONE',  ( 13.02619977026641074, 3.477781664713968990, -166.0928117978999126 ) ) ;
#7573=CARTESIAN_POINT ( 'NONE',  ( -21.49024324108596318, 3.999999999999993783, -163.1063489299302773 ) ) ;
#7574=CARTESIAN_POINT ( 'NONE',  ( 5.536303798911983876, 0.008884980407317709730, -141.3787188740540444 ) ) ;
#7576=CARTESIAN_POINT ( 'NONE',  ( -6.930553666837859339, 8.673617379884034486E-16, -152.1805032840957779 ) ) ;
#7580=CARTESIAN_POINT ( 'NONE',  ( 8.780952025204904032, 0.6450331482581128650, -105.6724537816508729 ) ) ;
#7583=DIRECTION ( 'NONE',  ( -0.000000000000000000, 1.000000000000000000, -0.000000000000000000 ) ) ;
#7592=CARTESIAN_POINT ( 'NONE',  ( 5.228075279701640099, 1.000000000000000000, -163.7939279834373849 ) ) ;
#7593=LINE ( 'NONE', #6049, #2083 ) ;
#7594=CARTESIAN_POINT ( 'NONE',  ( 8.592224267391641135, 8.673617379884035472E-16, -111.5170830772493957 ) ) ;
#7595=DIRECTION ( 'NONE',  ( -0.000000000000000000, -1.000000000000000000, -0.000000000000000000 ) ) ;
#7602=EDGE_CURVE ( 'NONE', #7276, #8407, #4076, .T. ) ;
#7607=CARTESIAN_POINT ( 'NONE',  ( 4.675143156396779354, 2.724689664222763125E-15, -31.08615533255463603 ) ) ;
#7609=CARTESIAN_POINT ( 'NONE',  ( 5.163630139845929889, 1.524494085803895782, 3.626316403462681137 ) ) ;
#7610=CARTESIAN_POINT ( 'NONE',  ( -6.822452048367190436, 14.42304080573416236, -117.0063474466252558 ) ) ;
#7613=CARTESIAN_POINT ( 'NONE',  ( -25.31190114102989597, 0.4153624176314577032, -203.6532684513659888 ) ) ;
#7618=FACE_OUTER_BOUND ( 'NONE', #1600, .T. ) ;
#7621=DIRECTION ( 'NONE',  ( 0.000000000000000000, 0.000000000000000000, -1.000000000000000000 ) ) ;
#7622=EDGE_CURVE ( 'NONE', #7799, #12868, #8453, .T. ) ;
#7628=FACE_OUTER_BOUND ( 'NONE', #13354, .T. ) ;
#7630=ORIENTED_EDGE ( 'NONE', *, *, #12922, .F. ) ;
#7636=SHAPE_REPRESENTATION ( 'PruningShears_Predeterminado', ( #9419 ), #3238 ) ;
#7637=CARTESIAN_POINT ( 'NONE',  ( 10.47455747790057679, 14.18553633661278113, -106.7841271890158765 ) ) ;
#7645=DIRECTION ( 'NONE',  ( 0.000000000000000000, 0.000000000000000000, 1.000000000000000000 ) ) ;
#7649=CARTESIAN_POINT ( 'NONE',  ( 11.01519796548710417, 4.326353643838777074, -107.1017525683475498 ) ) ;
#7651=CARTESIAN_POINT ( 'NONE',  ( -12.13691226097295228, 8.673617379884034486E-16, -151.8391917678144694 ) ) ;
#7652=LINE ( 'NONE', #5035, #10145 ) ;
#7661=CARTESIAN_POINT ( 'NONE',  ( 4.248871783098695509, 6.000000000000000000, -126.1456066832003842 ) ) ;
#7673=CARTESIAN_POINT ( 'NONE',  ( 8.935548306746154523, 15.00000000000000000, 2.855381328098122395 ) ) ;
#7674=CARTESIAN_POINT ( 'NONE',  ( 5.457768971991409757, 8.673617379884035472E-16, -106.2114798315073614 ) ) ;
#7679=CARTESIAN_POINT ( 'NONE',  ( 9.950255046238396517, 5.943472311793079221, -43.63919336277970018 ) ) ;
#7680=CARTESIAN_POINT ( 'NONE',  ( 0.2116200952963270543, 15.00000000000000178, -112.6243614187691975 ) ) ;
#7684=ORIENTED_EDGE ( 'NONE', *, *, #12408, .F. ) ;
#7687=CARTESIAN_POINT ( 'NONE',  ( 9.995755633401696372, 11.56847231179307833, -45.72406218842818504 ) ) ;
#7689=FACE_OUTER_BOUND ( 'NONE', #2359, .T. ) ;
#7690=CARTESIAN_POINT ( 'NONE',  ( -9.192419678266180227, 11.41184093590166349, -115.4428990047099148 ) ) ;
#7692=CARTESIAN_POINT ( 'NONE',  ( 8.507048280435965282, 12.49999999999999822, -111.8750672985880499 ) ) ;
#7696=DIRECTION ( 'NONE',  ( -0.02181900108494707474, 0.000000000000000000, 0.9997619372588932851 ) ) ;
#7698=ORIENTED_EDGE ( 'NONE', *, *, #2677, .F. ) ;
#7700=CARTESIAN_POINT ( 'NONE',  ( -4.887975900231274373, 14.97051500633131305, -117.2415000213202916 ) ) ;
#7707=CARTESIAN_POINT ( 'NONE',  ( 8.432848914831144072, 5.000000000000002665, -115.6062006120311878 ) ) ;
#7708=DIRECTION ( 'NONE',  ( 0.000000000000000000, 0.000000000000000000, 1.000000000000000000 ) ) ;
#7710=ORIENTED_EDGE ( 'NONE', *, *, #2236, .F. ) ;
#7716=VECTOR ( 'NONE', #3496, 1000.000000000000000 ) ;
#7717=EDGE_CURVE ( 'NONE', #5516, #1192, #3808, .T. ) ;
#7718=EDGE_CURVE ( 'NONE', #10451, #1120, #10135, .T. ) ;
#7722=CARTESIAN_POINT ( 'NONE',  ( -9.097645849187591338, 3.303830902112122825, -115.4858344565725616 ) ) ;
#7726=CARTESIAN_POINT ( 'NONE',  ( 4.837808514977005814, -1.933783910781458629E-11, -31.10787113836400763 ) ) ;
#7729=DIRECTION ( 'NONE',  ( -0.6876103830954231055, -9.542510991048287223E-16, 0.7260798585963982310 ) ) ;
#7730=CARTESIAN_POINT ( 'NONE',  ( -25.06351876112395161, 0.000000000000000000, -185.5277672829032838 ) ) ;
#7734=ORIENTED_EDGE ( 'NONE', *, *, #8656, .T. ) ;
#7736=CARTESIAN_POINT ( 'NONE',  ( 11.15078183098557218, 3.671353358600427441, -106.3578943783445823 ) ) ;
#7740=CARTESIAN_POINT ( 'NONE',  ( -9.817351912531890434, 4.222959489602541083, -115.7707972434356378 ) ) ;
#7743=CIRCLE ( 'NONE', #3058, 3.500000000000003109 ) ;
#7749=LINE ( 'NONE', #7592, #4380 ) ;
#7753=AXIS2_PLACEMENT_3D ( 'NONE', #1561, #6504, #13700 ) ;
#7754=CARTESIAN_POINT ( 'NONE',  ( 10.95491677860929869, 11.75663172244964727, -44.24084729402226657 ) ) ;
#7757=CARTESIAN_POINT ( 'NONE',  ( 8.976483039626360849, 12.42182331701315867, 0.9797231489651803127 ) ) ;
#7765=CARTESIAN_POINT ( 'NONE',  ( 9.953425949663817107, 12.69566228043988332, -44.13594640649452572 ) ) ;
#7768=CARTESIAN_POINT ( 'NONE',  ( -6.777586278698688460, 14.47993771880504177, -116.7594943224638087 ) ) ;
#7771=CARTESIAN_POINT ( 'NONE',  ( 13.03594997100189268, 12.49999999999999822, -125.1067209762342145 ) ) ;
#7772=CARTESIAN_POINT ( 'NONE',  ( 22.27832475887074537, 0.09828479602143111449, -138.8103524520464873 ) ) ;
#7782=EDGE_CURVE ( 'NONE', #7799, #13718, #14872, .T. ) ;
#7788=CARTESIAN_POINT ( 'NONE',  ( 10.00087860767147063, 5.000000000000000888, -45.95880046359209103 ) ) ;
#7794=DIRECTION ( 'NONE',  ( -0.9999404825435597166, 0.000000000000000000, -0.01091014988682699645 ) ) ;
#7799=VERTEX_POINT ( 'NONE', #10059 ) ;
#7802=CARTESIAN_POINT ( 'NONE',  ( 6.362474834385803746, 0.000000000000000000, -108.4026488224344291 ) ) ;
#7804=ADVANCED_FACE ( 'NONE', ( #11218 ), #4268, .T. ) ;
#7807=CARTESIAN_POINT ( 'NONE',  ( -22.54029179744063782, 8.673617379884035472E-16, -176.6655142756330861 ) ) ;
#7812=LINE ( 'NONE', #2245, #4548 ) ;
#7813=DIRECTION ( 'NONE',  ( 0.000000000000000000, 0.000000000000000000, 1.000000000000000000 ) ) ;
#7815=CARTESIAN_POINT ( 'NONE',  ( -13.50165587222837438, 8.673617379884035472E-16, -183.0027181781699142 ) ) ;
#7816=CARTESIAN_POINT ( 'NONE',  ( -3.504378794278709019, 8.673617379884035472E-16, -116.8541096786256333 ) ) ;
#7818=CARTESIAN_POINT ( 'NONE',  ( 7.000000000000000888, 9.999999999999998224, -1.663700395152567513 ) ) ;
#7824=EDGE_CURVE ( 'NONE', #6005, #4454, #9700, .T. ) ;
#7831=( BOUNDED_SURFACE ( )  B_SPLINE_SURFACE ( 3, 2, ( 
 ( #12074, #13331, #3976 ),
 ( #1345, #2738, #182 ),
 ( #1498, #7442, #3735 ),
 ( #12158, #6288, #7520 ),
 ( #419, #5129, #9842 ),
 ( #8681, #1421, #13415 ),
 ( #6047, #2818, #4894 ),
 ( #1264, #10689, #9533 ) ),
 .UNSPECIFIED., .F., .F., .F. ) 
 B_SPLINE_SURFACE_WITH_KNOTS ( ( 4, 2, 2, 4 ),
 ( 3, 3 ),
 ( 0.04393710950295283413, 0.04951918683847043867, 0.05231022550622924094, 0.05510126417398804322 ),
 ( 0.000000000000000000, 1.000000000000000000 ),
 .UNSPECIFIED. ) 
 GEOMETRIC_REPRESENTATION_ITEM ( )  RATIONAL_B_SPLINE_SURFACE ( (
 ( 1.000000000000000000, 0.7071067811865473507, 1.000000000000000000),
 ( 1.000000000000000000, 0.7071067811865473507, 1.000000000000000000),
 ( 1.000000000000000000, 0.7071067811865471286, 1.000000000000000000),
 ( 1.000000000000000000, 0.7071067811865471286, 1.000000000000000000),
 ( 1.000000000000000000, 0.7071067811865476838, 1.000000000000000000),
 ( 1.000000000000000000, 0.7071067811865476838, 1.000000000000000000),
 ( 1.000000000000000000, 0.7071067811865473507, 1.000000000000000000),
 ( 1.000000000000000000, 0.7071067811865473507, 1.000000000000000000) ) ) 
 REPRESENTATION_ITEM ( '' )  SURFACE ( )  );
#7833=CARTESIAN_POINT ( 'NONE',  ( 2.469015410240005703, 15.00000000000000000, -109.2094522964932679 ) ) ;
#7837=ORIENTED_EDGE ( 'NONE', *, *, #14807, .F. ) ;
#7842=CARTESIAN_POINT ( 'NONE',  ( -9.392097536374429012, 11.74640706408357005, -116.4406435548276022 ) ) ;
#7844=CARTESIAN_POINT ( 'NONE',  ( 11.86796838824852607, 12.49999999999999822, -123.5172601093923248 ) ) ;
#7845=DIRECTION ( 'NONE',  ( 0.000000000000000000, -0.000000000000000000, 1.000000000000000000 ) ) ;
#7846=CARTESIAN_POINT ( 'NONE',  ( 25.97495963226450755, 1.795150172152642165, -137.7704446659557220 ) ) ;
#7849=CARTESIAN_POINT ( 'NONE',  ( -23.62092208418379258, 4.000000000000000888, -167.0316697996453286 ) ) ;
#7852=CARTESIAN_POINT ( 'NONE',  ( -4.561986575595136983, 15.00000000000000355, -117.3660065143356235 ) ) ;
#7862=ADVANCED_FACE ( 'NONE', ( #8896 ), #12144, .F. ) ;
#7871=CARTESIAN_POINT ( 'NONE',  ( 26.17093350124943640, 6.000000000000000000, -137.7213801722282085 ) ) ;
#7874=CARTESIAN_POINT ( 'NONE',  ( -15.33183641037303069, -1.091572321461162701E-12, -155.5537725507397795 ) ) ;
#7882=CARTESIAN_POINT ( 'NONE',  ( 6.447361309400962526, 15.00000000000000000, 0.5877790035379841793 ) ) ;
#7884=CARTESIAN_POINT ( 'NONE',  ( 3.743303269468425842, 8.673617379884035472E-16, -106.5640776127142004 ) ) ;
#7886=AXIS2_PLACEMENT_3D ( 'NONE', #452, #13447, #7621 ) ;
#7887=CARTESIAN_POINT ( 'NONE',  ( 24.53888684075855409, 5.000000000000000888, -142.6514391812075928 ) ) ;
#7889=LINE ( 'NONE', #14729, #12356 ) ;
#7892=CARTESIAN_POINT ( 'NONE',  ( 20.87131526946579285, 0.000000000000000000, -138.9752963459259547 ) ) ;
#7897=CARTESIAN_POINT ( 'NONE',  ( 26.58801926426209405, 6.000000000000000000, -139.0072983920785532 ) ) ;
#7898=ORIENTED_EDGE ( 'NONE', *, *, #6495, .F. ) ;
#7899=ORIENTED_EDGE ( 'NONE', *, *, #5428, .F. ) ;
#7900=CARTESIAN_POINT ( 'NONE',  ( 3.558820106718695975, 15.00000000000000000, -107.0002797207564242 ) ) ;
#7903=CARTESIAN_POINT ( 'NONE',  ( 26.58801926426209405, 5.000000000000000888, -139.0072983920785532 ) ) ;
#7913=AXIS2_PLACEMENT_3D ( 'NONE', #11264, #8633, #1847 ) ;
#7918=CARTESIAN_POINT ( 'NONE',  ( 5.957819783299798111, 15.00000000000000000, -111.9092042284245707 ) ) ;
#7919=CARTESIAN_POINT ( 'NONE',  ( -9.410661088365813498, 11.69876074752964712, -116.4362230898866386 ) ) ;
#7921=CARTESIAN_POINT ( 'NONE',  ( 24.27947087742526833, 0.8297099930049451899, -138.5673885577481883 ) ) ;
#7929=EDGE_LOOP ( 'NONE', ( #4828, #6112, #7082, #5583 ) ) ;
#7934=CARTESIAN_POINT ( 'NONE',  ( -25.35797282612971770, 0.03589225196800699402, -200.8427820752426953 ) ) ;
#7938=FACE_OUTER_BOUND ( 'NONE', #11551, .T. ) ;
#7941=CARTESIAN_POINT ( 'NONE',  ( 10.81798288406372421, 13.62122652546089618, -106.9829802339604612 ) ) ;
#7946=LINE ( 'NONE', #4179, #14112 ) ;
#7952=VERTEX_POINT ( 'NONE', #5195 ) ;
#7953=CARTESIAN_POINT ( 'NONE',  ( -24.35736811731606366, 8.673617379884035472E-16, -201.5239328345637091 ) ) ;
#7961=CARTESIAN_POINT ( 'NONE',  ( 6.277464105443620213, 14.50508960634419431, 2.466953552936270277 ) ) ;
#7962=CARTESIAN_POINT ( 'NONE',  ( -1.030030362070360139, 8.673617379884035472E-16, -105.0143096063716399 ) ) ;
#7967=DIRECTION ( 'NONE',  ( -0.02032500363964214948, 0.3636704086172903305, 0.9313059261720508797 ) ) ;
#7983=AXIS2_PLACEMENT_3D ( 'NONE', #9165, #7696, #6838 ) ;
#7987=DIRECTION ( 'NONE',  ( 0.000000000000000000, 0.000000000000000000, -1.000000000000000000 ) ) ;
#7994=CARTESIAN_POINT ( 'NONE',  ( 8.308576004039894158, 12.49999999999999822, -113.5907613746754379 ) ) ;
#7998=CARTESIAN_POINT ( 'NONE',  ( 25.22353789337514129, 1.212876488842051792, -137.9529182181685201 ) ) ;
#8005=ORIENTED_EDGE ( 'NONE', *, *, #11002, .F. ) ;
#8009=CARTESIAN_POINT ( 'NONE',  ( -25.05565439364611535, 2.706536666467781682, -208.8267152099942621 ) ) ;
#8012=CARTESIAN_POINT ( 'NONE',  ( 9.697215460253069352, 5.000000000000000000, -119.7729938534562564 ) ) ;
#8013=AXIS2_PLACEMENT_3D ( 'NONE', #5429, #14734, #2961 ) ;
#8014=EDGE_CURVE ( 'NONE', #8185, #7526, #13659, .T. ) ;
#8015=VERTEX_POINT ( 'NONE', #13549 ) ;
#8017=CARTESIAN_POINT ( 'NONE',  ( 11.32016196459912649, 5.000000000000000888, -106.4092894470390291 ) ) ;
#8018=AXIS2_PLACEMENT_3D ( 'NONE', #2011, #15164, #12670 ) ;
#8023=DIRECTION ( 'NONE',  ( -8.764770998266003672E-18, -0.000000000000000000, -1.000000000000000000 ) ) ;
#8028=CARTESIAN_POINT ( 'NONE',  ( 9.952467559749662129, 4.873278229199302203, -43.74057228409819231 ) ) ;
#8030=CARTESIAN_POINT ( 'NONE',  ( 8.935548306886577308, 4.740853562920613662, 2.855381321663926997 ) ) ;
#8034=ORIENTED_EDGE ( 'NONE', *, *, #797, .F. ) ;
#8036=CARTESIAN_POINT ( 'NONE',  ( -25.48627911830238801, 3.148413055323376231, -208.6114731983374782 ) ) ;
#8037=CARTESIAN_POINT ( 'NONE',  ( 6.172424634706433544, 13.06580985397910943, 4.242162613119662140 ) ) ;
#8038=CARTESIAN_POINT ( 'NONE',  ( -5.318033920856502839, 5.000000000000000888, -111.4753907371883059 ) ) ;
#8040=CARTESIAN_POINT ( 'NONE',  ( 12.80648593303889271, 8.673617379884035472E-16, -154.6494596161801098 ) ) ;
#8043=CARTESIAN_POINT ( 'NONE',  ( -5.747484833204142163, 12.90644774961933372, -125.0474022778247587 ) ) ;
#8044=CARTESIAN_POINT ( 'NONE',  ( 23.58041249293978581, 0.5629353006154804717, -138.0219903428570944 ) ) ;
#8051=CARTESIAN_POINT ( 'NONE',  ( -14.35488426859573785, 8.673617379884035472E-16, -183.9742857961890081 ) ) ;
#8055=EDGE_LOOP ( 'NONE', ( #3956, #6872 ) ) ;
#8058=EDGE_CURVE ( 'NONE', #1120, #3740, #3035, .T. ) ;
#8067=DIRECTION ( 'NONE',  ( 0.000000000000000000, 1.000000000000000000, 0.000000000000000000 ) ) ;
#8068=ORIENTED_EDGE ( 'NONE', *, *, #11581, .F. ) ;
#8069=CARTESIAN_POINT ( 'NONE',  ( 26.44917159162123355, 3.476039578930857132, -136.9761077298000203 ) ) ;
#8072=ORIENTED_EDGE ( 'NONE', *, *, #11381, .F. ) ;
#8082=CARTESIAN_POINT ( 'NONE',  ( -25.15625982127824400, 1.053316850513906111, -205.6460296093184184 ) ) ;
#8083=CARTESIAN_POINT ( 'NONE',  ( 16.50094977371536231, 8.749999999999998224, -91.72275351520976017 ) ) ;
#8085=DIRECTION ( 'NONE',  ( -0.000000000000000000, 1.000000000000000000, -0.000000000000000000 ) ) ;
#8089=CARTESIAN_POINT ( 'NONE',  ( 10.28321301342407601, 14.39503880988861262, -106.6749965504387916 ) ) ;
#8090=EDGE_CURVE ( 'NONE', #788, #9763, #7812, .T. ) ;
#8100=CARTESIAN_POINT ( 'NONE',  ( 27.03835354040193195, 15.00000000000000000, -138.2189567750509980 ) ) ;
#8101=ORIENTED_EDGE ( 'NONE', *, *, #552, .F. ) ;
#8102=CARTESIAN_POINT ( 'NONE',  ( 8.117806577086446040, 2.126742365985535343, 4.858884805342907676 ) ) ;
#8106=ORIENTED_EDGE ( 'NONE', *, *, #4054, .F. ) ;
#8107=DIRECTION ( 'NONE',  ( 0.000000000000000000, 0.000000000000000000, -1.000000000000000000 ) ) ;
#8109=CARTESIAN_POINT ( 'NONE',  ( 6.154006371964378275, 12.51839902998314003, 4.611585984674669625 ) ) ;
#8110=CARTESIAN_POINT ( 'NONE',  ( -0.06526978517750199604, -1.215333660157913752E-12, -101.7940732946817235 ) ) ;
#8117=CARTESIAN_POINT ( 'NONE',  ( 25.66515063164039745, 2.145468714964426038, -137.2655343200625282 ) ) ;
#8124=CARTESIAN_POINT ( 'NONE',  ( -5.763889103029394612, 4.000000000000000888, -181.7491934423408964 ) ) ;
#8128=ORIENTED_EDGE ( 'NONE', *, *, #7622, .F. ) ;
#8129=B_SPLINE_CURVE_WITH_KNOTS ( 'NONE', 3,
 ( #10396, #2055, #15131, #823 ),
 .UNSPECIFIED., .F., .F.,
 ( 4, 4 ),
 ( 2.110397319742239368E-07, 0.0001887751033478067336 ),
 .UNSPECIFIED. ) ;
#8130=( BOUNDED_CURVE ( )  B_SPLINE_CURVE ( 3, ( #6813, #7264, #2563, #5109 ),
 .UNSPECIFIED., .F., .T. ) 
 B_SPLINE_CURVE_WITH_KNOTS ( ( 4, 4 ),
 ( 0.8013173358133321988, 1.595733058832763396 ),
 .UNSPECIFIED. ) 
 CURVE ( )  GEOMETRIC_REPRESENTATION_ITEM ( )  RATIONAL_B_SPLINE_CURVE ( ( 1.000000000000000000, 0.9480964748145740417, 0.9480964748145740417, 1.000000000000000000 ) ) 
 REPRESENTATION_ITEM ( '' )  );
#8139=ORIENTED_EDGE ( 'NONE', *, *, #2194, .T. ) ;
#8140=DIRECTION ( 'NONE',  ( -0.9997619372588931741, 0.000000000000000000, -0.02181900108494707127 ) ) ;
#8142=ORIENTED_EDGE ( 'NONE', *, *, #5448, .F. ) ;
#8150=CARTESIAN_POINT ( 'NONE',  ( -2.027137927702660214, 14.99999999999674927, -107.0032022125440818 ) ) ;
#8152=CIRCLE ( 'NONE', #10132, 1.000000000000000888 ) ;
#8153=AXIS2_PLACEMENT_3D ( 'NONE', #6159, #12032, #14216 ) ;
#8155=CARTESIAN_POINT ( 'NONE',  ( -24.98891949655539335, 1.707693810982847449, -206.9370818847572480 ) ) ;
#8163=EDGE_CURVE ( 'NONE', #14341, #6985, #5291, .T. ) ;
#8185=VERTEX_POINT ( 'NONE', #6480 ) ;
#8187=CARTESIAN_POINT ( 'NONE',  ( -25.42339729827660832, 0.05949801409391321932, -200.8587921603110260 ) ) ;
#8190=CARTESIAN_POINT ( 'NONE',  ( 5.000000000000000888, -1.083335593717820167E-31, -101.4583377608209531 ) ) ;
#8194=CARTESIAN_POINT ( 'NONE',  ( 25.77559445462507171, 2.285915182027296488, -137.2249222079316837 ) ) ;
#8202=CARTESIAN_POINT ( 'NONE',  ( -2.274567279739943881, 4.000000000000000000, -178.3664838788908469 ) ) ;
#8205=CARTESIAN_POINT ( 'NONE',  ( 12.76858567064540217, 3.999999999993260502, -166.6103056774037441 ) ) ;
#8206=VERTEX_POINT ( 'NONE', #12281 ) ;
#8207=CARTESIAN_POINT ( 'NONE',  ( -5.492028030076452794, 0.1084047943351758581, -117.0085585369582475 ) ) ;
#8210=CARTESIAN_POINT ( 'NONE',  ( -8.226857985479755442, 5.000000000000000000, -114.4011953629546099 ) ) ;
#8216=CARTESIAN_POINT ( 'NONE',  ( 4.781732708726812220, 1.734723475976807094E-15, -121.0163674326759491 ) ) ;
#8221=ORIENTED_EDGE ( 'NONE', *, *, #14256, .T. ) ;
#8227=VERTEX_POINT ( 'NONE', #8641 ) ;
#8228=CARTESIAN_POINT ( 'NONE',  ( 3.559460973859760013, 15.00000000000000000, -107.0011611385528880 ) ) ;
#8231=AXIS2_PLACEMENT_3D ( 'NONE', #9655, #6172, #14386 ) ;
#8233=CARTESIAN_POINT ( 'NONE',  ( -25.69889708084257762, 0.9650723257009210521, -205.4472600487935665 ) ) ;
#8243=CARTESIAN_POINT ( 'NONE',  ( -5.794432043291358525, 13.40945642053105225, -125.0404107129116085 ) ) ;
#8246=CARTESIAN_POINT ( 'NONE',  ( -0.04436259091852395170, 5.000000000000007105, -136.3368594361672876 ) ) ;
#8249=CARTESIAN_POINT ( 'NONE',  ( 9.161239424535876807, 0.8923617020344253303, -105.7786917259425508 ) ) ;
#8254=CARTESIAN_POINT ( 'NONE',  ( 6.108231453664635602, 4.487270727616577304, 5.259165607916492569 ) ) ;
#8278=CARTESIAN_POINT ( 'NONE',  ( 8.246457104576641939, 8.673617379884035472E-16, -163.7205653903581037 ) ) ;
#8284=B_SPLINE_CURVE_WITH_KNOTS ( 'NONE', 3,
 ( #10880, #10572, #3689, #11801 ),
 .UNSPECIFIED., .F., .F.,
 ( 4, 4 ),
 ( 0.000000000000000000, 0.0004294366880267255987 ),
 .UNSPECIFIED. ) ;
#8287=CARTESIAN_POINT ( 'NONE',  ( 6.117677467307099270, 8.673617379884035472E-16, -123.7586964171227066 ) ) ;
#8290=B_SPLINE_CURVE_WITH_KNOTS ( 'NONE', 3,
 ( #14890, #4287, #13867, #581, #11239, #10079, #14741, #14814, #3119, #4360, #9069, #13790, #7039, #2186, #2411, #10597, #1176, #13946, #5957, #9363, #12853, #5877, #10453, #10679 ),
 .UNSPECIFIED., .F., .F.,
 ( 4, 2, 2, 2, 2, 2, 2, 2, 2, 2, 2, 4 ),
 ( 1.734723475976807094E-18, 0.002712057318076011199, 0.005424114636152054490, 0.008136171954228096914, 0.01084822927230414021, 0.01220425793134216272, 0.01356028659038018523, 0.01491631524941820601, 0.01627234390845622852, 0.01898440122653227008, 0.02034042988557029086, 0.02169645854460831164 ),
 .UNSPECIFIED. ) ;
#8292=CARTESIAN_POINT ( 'NONE',  ( 3.843629782151245955, 8.673617379884035472E-16, -118.2118429041878898 ) ) ;
#8296=VERTEX_POINT ( 'NONE', #8563 ) ;
#8298=CARTESIAN_POINT ( 'NONE',  ( 16.50094977371536231, 8.749999999999998224, -91.72275351520976017 ) ) ;
#8302=CARTESIAN_POINT ( 'NONE',  ( 3.743303269469635097, 14.99999999999999822, -106.5640776127148399 ) ) ;
#8307=CARTESIAN_POINT ( 'NONE',  ( 8.283327938524582379, 15.00000000000000000, -122.5135224137794978 ) ) ;
#8315=CYLINDRICAL_SURFACE ( 'NONE', #2001, 3.500000000000003109 ) ;
#8317=CARTESIAN_POINT ( 'NONE',  ( -3.542861251344865181, 5.000000000000010658, -131.3727830290921190 ) ) ;
#8319=CARTESIAN_POINT ( 'NONE',  ( 10.97171279554003043, 8.773889247172311556, -44.61149169061435060 ) ) ;
#8324=CARTESIAN_POINT ( 'NONE',  ( 4.027501057062753631, 0.09548388211871727815, -1.357275530841774991 ) ) ;
#8336=CARTESIAN_POINT ( 'NONE',  ( 17.33677725113053114, 5.000000000000000888, -156.7678757841025003 ) ) ;
#8341=CARTESIAN_POINT ( 'NONE',  ( -5.661351488087990269, 3.999999999999993783, -144.3936414932596506 ) ) ;
#8345=ORIENTED_EDGE ( 'NONE', *, *, #1644, .F. ) ;
#8349=CARTESIAN_POINT ( 'NONE',  ( 13.05679544828472238, 4.000000000000000000, -166.4200500252868551 ) ) ;
#8359=FACE_OUTER_BOUND ( 'NONE', #1671, .T. ) ;
#8362=CARTESIAN_POINT ( 'NONE',  ( 9.723706525289889768, -3.022969897739336727E-12, -119.8316069321379302 ) ) ;
#8367=ADVANCED_FACE ( 'NONE', ( #6255 ), #6402, .F. ) ;
#8369=FACE_OUTER_BOUND ( 'NONE', #4002, .T. ) ;
#8371=EDGE_CURVE ( 'NONE', #5472, #14341, #8650, .T. ) ;
#8373=ORIENTED_EDGE ( 'NONE', *, *, #2304, .F. ) ;
#8374=EDGE_CURVE ( 'NONE', #5152, #4454, #6931, .T. ) ;
#8375=CARTESIAN_POINT ( 'NONE',  ( -3.294555838625194077, 14.99999999999918643, -108.9576586821702620 ) ) ;
#8380=CARTESIAN_POINT ( 'NONE',  ( -24.60401395879240738, 4.143790226087491035, -208.9577473736382842 ) ) ;
#8387=AXIS2_PLACEMENT_3D ( 'NONE', #7114, #8519, #10606 ) ;
#8394=CARTESIAN_POINT ( 'NONE',  ( 10.75998892872498658, 2.667360448133907713, -106.5950482656118794 ) ) ;
#8400=ORIENTED_EDGE ( 'NONE', *, *, #7717, .T. ) ;
#8401=CARTESIAN_POINT ( 'NONE',  ( 6.795064564604292201, 0.7174242581283463149, 3.395653431975275804 ) ) ;
#8407=VERTEX_POINT ( 'NONE', #3379 ) ;
#8417=DIRECTION ( 'NONE',  ( -1.000000000000000000, 0.000000000000000000, 0.000000000000000000 ) ) ;
#8418=CARTESIAN_POINT ( 'NONE',  ( 8.895558325401111688, 15.00000000000000000, -141.4560052469132643 ) ) ;
#8420=CARTESIAN_POINT ( 'NONE',  ( -8.765507753109435640, 1.591638444933427977E-16, -148.3002607745583816 ) ) ;
#8422=CARTESIAN_POINT ( 'NONE',  ( 5.021457302209542561, 0.1001282284926883204, -1.279387354551734024 ) ) ;
#8423=CARTESIAN_POINT ( 'NONE',  ( 6.122889832264990062, 9.999999999999998224, 5.281130614573720905 ) ) ;
#8429=CARTESIAN_POINT ( 'NONE',  ( -22.96235718882280707, 8.673617379884035472E-16, -203.4902939858489788 ) ) ;
#8436=EDGE_CURVE ( 'NONE', #5913, #1934, #7222, .T. ) ;
#8439=DIRECTION ( 'NONE',  ( 0.000000000000000000, 1.000000000000000000, 0.000000000000000000 ) ) ;
#8440=EDGE_CURVE ( 'NONE', #191, #14278, #2153, .T. ) ;
#8444=CARTESIAN_POINT ( 'NONE',  ( -0.1621610429705883094, -1.190394676226177737E-12, -136.1940307089123507 ) ) ;
#8445=CARTESIAN_POINT ( 'NONE',  ( 15.55587903155823248, 5.000000000000000888, -128.0070267003170272 ) ) ;
#8447=DIRECTION ( 'NONE',  ( -0.9997619372588932851, 0.000000000000000000, -0.02181900108494707474 ) ) ;
#8453=CIRCLE ( 'NONE', #1837, 5.000000000000000000 ) ;
#8460=EDGE_CURVE ( 'NONE', #933, #7952, #583, .T. ) ;
#8463=AXIS2_PLACEMENT_3D ( 'NONE', #1922, #6789, #12660 ) ;
#8464=ADVANCED_FACE ( 'NONE', ( #5697 ), #9180, .F. ) ;
#8466=CARTESIAN_POINT ( 'NONE',  ( 14.32267195561841433, 12.49999999999999822, -126.6197849905234278 ) ) ;
#8467=ORIENTED_EDGE ( 'NONE', *, *, #7527, .T. ) ;
#8476=CARTESIAN_POINT ( 'NONE',  ( 7.504172156237145508, 0.1516696207292601850, -105.5034272634598977 ) ) ;
#8477=EDGE_CURVE ( 'NONE', #5038, #13240, #9014, .T. ) ;
#8479=CARTESIAN_POINT ( 'NONE',  ( -0.9850606648477213678, 15.00000000000000000, -125.5681744140592144 ) ) ;
#8485=CARTESIAN_POINT ( 'NONE',  ( 8.196277028564448841, 2.365617111222970692, 2.402449729030273762 ) ) ;
#8493=CIRCLE ( 'NONE', #12696, 4.999999999999992895 ) ;
#8501=CARTESIAN_POINT ( 'NONE',  ( 1.123966981038241109, 8.673617379884035472E-16, -145.3508939974056773 ) ) ;
#8502=FACE_OUTER_BOUND ( 'NONE', #7929, .T. ) ;
#8503=CARTESIAN_POINT ( 'NONE',  ( -22.33245550614446984, 8.673617379884035472E-16, -176.1180941298629818 ) ) ;
#8519=DIRECTION ( 'NONE',  ( -0.000000000000000000, 1.000000000000000000, -0.000000000000000000 ) ) ;
#8522=CARTESIAN_POINT ( 'NONE',  ( 0.5277094098148726875, 5.000000000000800249, -137.0293413729473571 ) ) ;
#8523=CARTESIAN_POINT ( 'NONE',  ( 8.346107330767033261, -2.159485683299472295E-13, -114.8449120968014796 ) ) ;
#8525=DIRECTION ( 'NONE',  ( 0.000000000000000000, 0.000000000000000000, 1.000000000000000000 ) ) ;
#8528=VERTEX_POINT ( 'NONE', #3308 ) ;
#8529=CARTESIAN_POINT ( 'NONE',  ( 23.72559141557340112, 0.5631470407087223462, -138.6353840888844502 ) ) ;
#8535=CARTESIAN_POINT ( 'NONE',  ( -3.504378794273236508, 14.99999999999999822, -116.8541096786202331 ) ) ;
#8537=CARTESIAN_POINT ( 'NONE',  ( -7.950184983571356945, 9.999999999999994671, -122.1589960244479016 ) ) ;
#8538=CARTESIAN_POINT ( 'NONE',  ( 9.304453467381463838, 4.110933237340877717E-16, -163.3650005149288233 ) ) ;
#8541=CARTESIAN_POINT ( 'NONE',  ( 17.50071171097425804, 8.749999999999998224, -91.70093451412481045 ) ) ;
#8542=ORIENTED_EDGE ( 'NONE', *, *, #3374, .T. ) ;
#8545=EDGE_CURVE ( 'NONE', #273, #9933, #6986, .T. ) ;
#8546=DIRECTION ( 'NONE',  ( 0.000000000000000000, 0.000000000000000000, 1.000000000000000000 ) ) ;
#8549=DIRECTION ( 'NONE',  ( 8.764770998266002131E-18, -0.000000000000000000, 1.000000000000000000 ) ) ;
#8551=CARTESIAN_POINT ( 'NONE',  ( 10.79363737070329776, 14.04001088496077543, -106.2926778297471060 ) ) ;
#8555=LINE ( 'NONE', #14142, #4704 ) ;
#8556=ORIENTED_EDGE ( 'NONE', *, *, #3673, .T. ) ;
#8557=CARTESIAN_POINT ( 'NONE',  ( 5.630997345025299694, 2.457945380941962465, 4.493121576497173919 ) ) ;
#8563=CARTESIAN_POINT ( 'NONE',  ( -0.9850606648477213678, 15.00000000000000000, -125.5681744140592144 ) ) ;
#8564=CLOSED_SHELL ( 'NONE', ( #5471, #15100, #9992, #3352, #1257, #12816, #15077, #11401, #10263, #2144, #14148, #12451, #3832, #12509, #7546, #5002, #12711, #1647, #6962, #10188, #11834, #14702, #8464, #10186, #7804, #2973, #5886, #15215, #11210, #3741, #606, #279, #8367, #5633, #5617, #9102, #11969, #14144, #1965, #12599, #1966, #3527, #14725, #12889, #6676, #10837, #13962, #12734, #9192, #13834, #342, #11778, #9407, #6922, #9340, #2608, #12536, #6376, #14654, #1883, #9042, #5725, #8774, #8854, #137, #7862, #11963, #11317, #4986, #4325, #3431, #4692, #11734, #2072, #10953 ) ) ;
#8568=CARTESIAN_POINT ( 'NONE',  ( 9.985652091690132792, 14.71651756310949999, -106.3014141697038042 ) ) ;
#8575=CARTESIAN_POINT ( 'NONE',  ( 10.72774301836061639, 0.4980643078076283370, -164.7196873471209244 ) ) ;
#8576=CARTESIAN_POINT ( 'NONE',  ( 24.11812047241811285, 4.000000000000000000, -143.1328717288817813 ) ) ;
#8579=CARTESIAN_POINT ( 'NONE',  ( 1.401654536806489659, 8.673617379884035472E-16, -145.1626543382392924 ) ) ;
#8583=ORIENTED_EDGE ( 'NONE', *, *, #14635, .F. ) ;
#8588=CARTESIAN_POINT ( 'NONE',  ( 9.044950117654433797, 0.000000000000000000, -144.9826476090360643 ) ) ;
#8590=CARTESIAN_POINT ( 'NONE',  ( -9.486278975404857761, 3.140033110049585741, -115.8846352400757240 ) ) ;
#8598=CARTESIAN_POINT ( 'NONE',  ( -3.672164062207812218, -6.326810776413004444E-12, -131.0905698957661514 ) ) ;
#8599=CARTESIAN_POINT ( 'NONE',  ( 6.285553548860313811, 8.673617379884035472E-16, -104.9603685434299649 ) ) ;
#8602=CARTESIAN_POINT ( 'NONE',  ( 26.15341798802279527, 4.000000000000000000, -138.7600702976168066 ) ) ;
#8604=ORIENTED_EDGE ( 'NONE', *, *, #5370, .T. ) ;
#8610=ORIENTED_EDGE ( 'NONE', *, *, #6941, .T. ) ;
#8611=LINE ( 'NONE', #13268, #12179 ) ;
#8615=CARTESIAN_POINT ( 'NONE',  ( 8.673617379884035472E-16, 5.000000000000000888, -1.663700395152567513 ) ) ;
#8617=DIRECTION ( 'NONE',  ( 0.02181900108494707474, 0.000000000000000000, -0.9997619372588931741 ) ) ;
#8622=CIRCLE ( 'NONE', #10858, 2.000000000000001776 ) ;
#8627=EDGE_CURVE ( 'NONE', #8296, #13571, #7329, .T. ) ;
#8628=CARTESIAN_POINT ( 'NONE',  ( 11.32016196459919399, 5.000000000000001776, -106.4092894470421271 ) ) ;
#8631=EDGE_CURVE ( 'NONE', #14015, #1063, #13202, .T. ) ;
#8633=DIRECTION ( 'NONE',  ( 0.000000000000000000, 1.000000000000000000, 0.000000000000000000 ) ) ;
#8634=CIRCLE ( 'NONE', #4928, 3.500000000000003109 ) ;
#8636=CARTESIAN_POINT ( 'NONE',  ( 6.415040636403542607, 0.6340196072765523772, 1.032023330731489219 ) ) ;
#8641=CARTESIAN_POINT ( 'NONE',  ( 9.044950117654433797, 4.000000000000000000, -144.9826476090360643 ) ) ;
#8648=AXIS2_PLACEMENT_3D ( 'NONE', #12197, #10107, #1685 ) ;
#8650=B_SPLINE_CURVE_WITH_KNOTS ( 'NONE', 3,
 ( #13378, #13607, #11197, #7486, #1620, #4172, #13458, #14700, #7562, #3010, #11423, #987, #15152, #5619, #11649, #12582, #14851, #1996 ),
 .UNSPECIFIED., .F., .F.,
 ( 4, 2, 2, 2, 2, 2, 2, 2, 4 ),
 ( 0.000000000000000000, 0.002234240643988127332, 0.003351360965982170398, 0.004468481287976213898, 0.006702721931964300030, 0.008936962575952387897, 0.01117120321994047663, 0.01340544386392856363, 0.01787392515190473763 ),
 .UNSPECIFIED. ) ;
#8656=EDGE_CURVE ( 'NONE', #10108, #8528, #10497, .T. ) ;
#8659=CARTESIAN_POINT ( 'NONE',  ( -7.585720900221621932, 8.673617379884034486E-16, -147.1779900946870896 ) ) ;
#8660=CARTESIAN_POINT ( 'NONE',  ( 5.940997791171045428, 0.02470368953922983876, -139.8438714080451462 ) ) ;
#8662=AXIS2_PLACEMENT_3D ( 'NONE', #10587, #6024, #2561 ) ;
#8663=CARTESIAN_POINT ( 'NONE',  ( -25.01903476313728447, 8.673617379884033500E-16, -185.3139711507751599 ) ) ;
#8664=ORIENTED_EDGE ( 'NONE', *, *, #4956, .T. ) ;
#8668=CARTESIAN_POINT ( 'NONE',  ( -15.87132822948224486, -8.950197302265710935E-13, -192.3250264793432507 ) ) ;
#8677=DIRECTION ( 'NONE',  ( -0.000000000000000000, 1.000000000000000000, 0.000000000000000000 ) ) ;
#8680=EDGE_CURVE ( 'NONE', #11140, #13718, #13039, .T. ) ;
#8681=CARTESIAN_POINT ( 'NONE',  ( -9.210337242589636375, 10.00000000000081535, -118.3325445942146246 ) ) ;
#8682=CARTESIAN_POINT ( 'NONE',  ( -3.903074397104974391, 8.673617379884035472E-16, -118.5654830222526499 ) ) ;
#8683=CARTESIAN_POINT ( 'NONE',  ( 8.518838221584619674, 8.673617379884035472E-16, -111.8377054444463141 ) ) ;
#8686=CARTESIAN_POINT ( 'NONE',  ( 4.999884908348398049, 0.09438068890155060231, -1.653151978968578462 ) ) ;
#8687=AXIS2_PLACEMENT_3D ( 'NONE', #10794, #208, #10959 ) ;
#8703=CARTESIAN_POINT ( 'NONE',  ( -25.01864811757476303, 1.587607347591324158, -206.7381864276124190 ) ) ;
#8704=ORIENTED_EDGE ( 'NONE', *, *, #6474, .F. ) ;
#8710=TOROIDAL_SURFACE ( 'NONE', #9710, 4.000000000000001776, 1.000000000000000000 ) ;
#8711=DIRECTION ( 'NONE',  ( -0.000000000000000000, 1.000000000000000000, -0.000000000000000000 ) ) ;
#8712=CARTESIAN_POINT ( 'NONE',  ( -9.385448347264265578, 5.000000000000000888, -115.3551636530117150 ) ) ;
#8717=ORIENTED_EDGE ( 'NONE', *, *, #4680, .F. ) ;
#8721=AXIS2_PLACEMENT_3D ( 'NONE', #8298, #11707, #12875 ) ;
#8725=( BOUNDED_SURFACE ( )  B_SPLINE_SURFACE ( 3, 2, ( 
 ( #14470, #14155, #1462 ),
 ( #2703, #1229, #78 ),
 ( #2394, #13223, #10893 ),
 ( #9429, #3866, #309 ),
 ( #4862, #8568, #7403 ),
 ( #12127, #9504, #10738 ),
 ( #3701, #13142, #14701 ),
 ( #465, #4023, #7637 ),
 ( #10973, #5100, #5399 ),
 ( #1544, #6559, #11271 ),
 ( #12353, #10113, #693 ),
 ( #621, #391, #4252 ),
 ( #6403, #1854, #9814 ),
 ( #5178, #7563, #14853 ) ),
 .UNSPECIFIED., .F., .F., .T. ) 
 B_SPLINE_SURFACE_WITH_KNOTS ( ( 4, 2, 2, 2, 2, 2, 4 ),
 ( 3, 3 ),
 ( -9.470303715793572266E-06, 0.0005986386120071484880, 0.0009026930698686195555, 0.001206747527730090514, 0.001510801985591561473, 0.001814856443453032649, 0.002422965359175974567 ),
 ( 0.000000000000000000, 1.000000000000000000 ),
 .UNSPECIFIED. ) 
 GEOMETRIC_REPRESENTATION_ITEM ( )  RATIONAL_B_SPLINE_SURFACE ( (
 ( 1.000000000000000000, 1.000000000000000000, 1.000000000000000000),
 ( 1.000000000000000000, 1.000023086200706457, 1.000000000000000000),
 ( 1.000000000000000000, 0.9968203200712785206, 1.000000000000000000),
 ( 1.000000000000000000, 0.9876439521679505340, 1.000000000000000000),
 ( 1.000000000000000000, 0.9839375215982008038, 1.000000000000000000),
 ( 1.000000000000000000, 0.9755509977066852967, 1.000000000000000000),
 ( 1.000000000000000000, 0.9708179905542198007, 1.000000000000000000),
 ( 1.000000000000000000, 0.9610203602157827429, 1.000000000000000000),
 ( 1.000000000000000000, 0.9560186120561716683, 1.000000000000000000),
 ( 1.000000000000000000, 0.9464213852071460265, 1.000000000000000000),
 ( 1.000000000000000000, 0.9417776319690466247, 1.000000000000000000),
 ( 1.000000000000000000, 0.9300548202764272743, 1.000000000000000000),
 ( 1.000000000000000000, 0.9250790184741459754, 1.000000000000000000),
 ( 1.000000000000000000, 0.9251337988227811282, 1.000000000000000000) ) ) 
 REPRESENTATION_ITEM ( '' )  SURFACE ( )  );
#8736=LINE ( 'NONE', #7802, #5994 ) ;
#8738=CARTESIAN_POINT ( 'NONE',  ( 11.49434807426983340, 0.9346580912065771685, -164.9697452992295155 ) ) ;
#8740=CARTESIAN_POINT ( 'NONE',  ( -25.59366506200112212, 8.673617379884035472E-16, -196.2657947609912696 ) ) ;
#8742=CARTESIAN_POINT ( 'NONE',  ( 5.578155699418820390, 0.2507831308262787329, 0.07728901913012563296 ) ) ;
#8744=VERTEX_POINT ( 'NONE', #4621 ) ;
#8745=DIRECTION ( 'NONE',  ( 0.000000000000000000, 0.000000000000000000, -1.000000000000000000 ) ) ;
#8748=CIRCLE ( 'NONE', #13941, 1.000000000000042633 ) ;
#8753=CARTESIAN_POINT ( 'NONE',  ( -8.611029641430635095, 2.324435220029751559, -115.7034661592633995 ) ) ;
#8761=AXIS2_PLACEMENT_3D ( 'NONE', #2108, #235, #1324 ) ;
#8763=CARTESIAN_POINT ( 'NONE',  ( 0.5277094143303744378, -8.082121701904429344E-13, -137.0293413685615462 ) ) ;
#8764=CARTESIAN_POINT ( 'NONE',  ( 9.719609032732419607, 5.000000000000000888, -108.8314952391709767 ) ) ;
#8766=CARTESIAN_POINT ( 'NONE',  ( 11.03716979879487425, 8.773889247172311556, -47.61077750239103779 ) ) ;
#8768=CARTESIAN_POINT ( 'NONE',  ( 9.991517632468019272, 4.874398275619288512, -45.52987401239477805 ) ) ;
#8769=CARTESIAN_POINT ( 'NONE',  ( 24.68832053908537461, 1.068321173883799435, -138.5167654850991141 ) ) ;
#8774=ADVANCED_FACE ( 'NONE', ( #6237 ), #8710, .F. ) ;
#8778=FACE_OUTER_BOUND ( 'NONE', #1193, .T. ) ;
#8780=CARTESIAN_POINT ( 'NONE',  ( 1.041485463413605039, 5.000000000000000888, -139.4527924098652534 ) ) ;
#8781=CARTESIAN_POINT ( 'NONE',  ( 6.122889832264996279, 4.584371499408331552, 5.281130614573727122 ) ) ;
#8782=CARTESIAN_POINT ( 'NONE',  ( -4.234402844927157794, 15.00000000000000000, -117.4888040839639558 ) ) ;
#8784=CARTESIAN_POINT ( 'NONE',  ( -25.22236287666808607, 7.173903195122934007E-14, -199.9119606112305689 ) ) ;
#8792=CARTESIAN_POINT ( 'NONE',  ( 13.47730208875211844, 6.000000000000000000, -127.1728814958210876 ) ) ;
#8798=VERTEX_POINT ( 'NONE', #10870 ) ;
#8804=CARTESIAN_POINT ( 'NONE',  ( 1.123679064339592859, 4.590773665857039276, -139.4222662838609210 ) ) ;
#8808=CARTESIAN_POINT ( 'NONE',  ( 10.93997309537930285, 12.49999999999999822, -43.15715636164252089 ) ) ;
#8812=CARTESIAN_POINT ( 'NONE',  ( 10.88783379353840353, 0.4980643078046000372, -164.5252078881505327 ) ) ;
#8814=CARTESIAN_POINT ( 'NONE',  ( 10.40609041963844028, 2.453994274272181197, -106.8025912277847738 ) ) ;
#8815=CARTESIAN_POINT ( 'NONE',  ( -25.78218315853617781, 8.673617379884035472E-16, -191.6593332018818217 ) ) ;
#8818=( BOUNDED_SURFACE ( )  B_SPLINE_SURFACE ( 3, 2, ( 
 ( #13045, #12112, #10876 ),
 ( #4773, #10960, #3854 ),
 ( #295, #1298, #1530 ),
 ( #8476, #9489, #12976 ),
 ( #2455, #5010, #9727 ),
 ( #2537, #379, #5087 ),
 ( #9801, #14457, #11952 ),
 ( #7152, #14531, #8249 ),
 ( #11874, #2380, #7078 ),
 ( #11798, #4849, #1212 ),
 ( #5922, #9640, #10796 ),
 ( #14213, #210, #9560 ),
 ( #10648, #4923, #13210 ),
 ( #3685, #5999, #3615 ),
 ( #14285, #8394, #14373 ),
 ( #13127, #3772, #2613 ),
 ( #2771, #12340, #10185 ),
 ( #454, #9875, #14767 ),
 ( #7475, #6322, #5316 ),
 ( #13595, #3929, #8628 ) ),
 .UNSPECIFIED., .F., .F., .F. ) 
 B_SPLINE_SURFACE_WITH_KNOTS ( ( 4, 2, 2, 2, 2, 2, 2, 2, 2, 4 ),
 ( 3, 3 ),
 ( -1.605708952745050187E-05, 0.0007915698365215041894, 0.001599196762570458813, 0.002406823688619413436, 0.002810637151643890531, 0.003214450614668368060, 0.004022077540717322250, 0.004829704466766277307, 0.005637331392815232364, 0.006444958318864186554 ),
 ( 0.000000000000000000, 1.000000000000000000 ),
 .UNSPECIFIED. ) 
 GEOMETRIC_REPRESENTATION_ITEM ( )  RATIONAL_B_SPLINE_SURFACE ( (
 ( 1.000000000000000000, 1.000000000000000000, 1.000000000000000000),
 ( 1.000000000000000000, 1.000000004030991319, 1.000000000000000000),
 ( 1.000000000000000000, 0.9993280885290816151, 1.000000000000000000),
 ( 1.000000000000000000, 0.9965616808472221866, 1.000000000000000000),
 ( 1.000000000000000000, 0.9944483308498629492, 1.000000000000000000),
 ( 1.000000000000000000, 0.9887906551701354241, 1.000000000000000000),
 ( 1.000000000000000000, 0.9853034643475333532, 1.000000000000000000),
 ( 1.000000000000000000, 0.9792464072626098082, 1.000000000000000000),
 ( 1.000000000000000000, 0.9770901656133914592, 1.000000000000000000),
 ( 1.000000000000000000, 0.9725405627970424849, 1.000000000000000000),
 ( 1.000000000000000000, 0.9701365459986746043, 1.000000000000000000),
 ( 1.000000000000000000, 0.9628092176376522593, 1.000000000000000000),
 ( 1.000000000000000000, 0.9577259713103128957, 1.000000000000000000),
 ( 1.000000000000000000, 0.9478123764691049891, 1.000000000000000000),
 ( 1.000000000000000000, 0.9429374510257780839, 1.000000000000000000),
 ( 1.000000000000000000, 0.9346631652659601608, 1.000000000000000000),
 ( 1.000000000000000000, 0.9312238446806561099, 1.000000000000000000),
 ( 1.000000000000000000, 0.9264379836092896392, 1.000000000000000000),
 ( 1.000000000000000000, 0.9251151247725492022, 1.000000000000000000),
 ( 1.000000000000000000, 0.9251337988227200659, 1.000000000000000000) ) ) 
 REPRESENTATION_ITEM ( '' )  SURFACE ( )  );
#8835=CARTESIAN_POINT ( 'NONE',  ( 8.592224267316021624, 5.000000000000000888, -111.5170830772279515 ) ) ;
#8839=CARTESIAN_POINT ( 'NONE',  ( 8.942896775526056885, 11.26065431988117638, 2.518669333141213773 ) ) ;
#8840=CARTESIAN_POINT ( 'NONE',  ( 1.624578347342659157, 15.00000000000000178, -110.6108487083152596 ) ) ;
#8850=CARTESIAN_POINT ( 'NONE',  ( -5.534063745946611768, 14.90222776335429700, -117.1292924427878575 ) ) ;
#8853=CARTESIAN_POINT ( 'NONE',  ( 9.875992363739401370, 12.49999999999999822, -120.1725736630937007 ) ) ;
#8854=ADVANCED_FACE ( 'NONE', ( #7618 ), #13167, .F. ) ;
#8856=ORIENTED_EDGE ( 'NONE', *, *, #4054, .T. ) ;
#8860=ORIENTED_EDGE ( 'NONE', *, *, #839, .T. ) ;
#8868=PLANE ( 'NONE',  #98 ) ;
#8882=CARTESIAN_POINT ( 'NONE',  ( -4.887975900231388060, 0.02948499366869817423, -117.2415000213202774 ) ) ;
#8887=CIRCLE ( 'NONE', #754, 2.000000000000007994 ) ;
#8888=CARTESIAN_POINT ( 'NONE',  ( 6.577825583858426306, 0.000000000000000000, -139.0000488628143103 ) ) ;
#8890=CARTESIAN_POINT ( 'NONE',  ( -23.30526566008802902, 8.673617379884035472E-16, -178.8465041759440055 ) ) ;
#8896=FACE_OUTER_BOUND ( 'NONE', #5616, .T. ) ;
#8913=CARTESIAN_POINT ( 'NONE',  ( 10.99170155471432686, 11.63675136861741244, -45.52739065948508568 ) ) ;
#8916=CARTESIAN_POINT ( 'NONE',  ( -20.28323750239604806, 4.000000000000000000, -200.3886341823752844 ) ) ;
#8920=VERTEX_POINT ( 'NONE', #13588 ) ;
#8923=EDGE_CURVE ( 'NONE', #14015, #2518, #12661, .T. ) ;
#8924=CARTESIAN_POINT ( 'NONE',  ( 10.02810328368141768, 11.68469885172349798, -45.38224167655878460 ) ) ;
#8925=CARTESIAN_POINT ( 'NONE',  ( 9.945392800007761380, 12.56622419557329096, -43.41640182928829006 ) ) ;
#8926=CARTESIAN_POINT ( 'NONE',  ( 5.595249735037589822, 2.348479801108206200, 4.434930130517638069 ) ) ;
#8927=CARTESIAN_POINT ( 'NONE',  ( -8.888107754931663607, 12.67556477985378116, -116.5586263778010903 ) ) ;
#8930=CARTESIAN_POINT ( 'NONE',  ( 9.218878510548623950, 15.00000000000000000, -124.0543039030355601 ) ) ;
#8932=CARTESIAN_POINT ( 'NONE',  ( 27.11959404819519293, 3.246087323616470233, -137.4897650963793296 ) ) ;
#8935=CARTESIAN_POINT ( 'NONE',  ( -22.38716924508033657, 4.000000000000000000, -164.7809911966533889 ) ) ;
#8941=EDGE_CURVE ( 'NONE', #8920, #1352, #2545, .T. ) ;
#8946=CARTESIAN_POINT ( 'NONE',  ( 13.52340959288768651, 5.000000000000000888, -125.7424794682274438 ) ) ;
#8949=CARTESIAN_POINT ( 'NONE',  ( 8.990769910733003911, 12.49999999999999822, 0.3250886916252374026 ) ) ;
#8956=CARTESIAN_POINT ( 'NONE',  ( -4.561986575600236016, 1.189234257945038070E-15, -117.3660065143490812 ) ) ;
#8957=CARTESIAN_POINT ( 'NONE',  ( -5.928758847211441640, 0.2324570288725731071, -117.1828119328369695 ) ) ;
#8962=CIRCLE ( 'NONE', #2303, 5.000000000000000000 ) ;
#8964=VERTEX_POINT ( 'NONE', #6623 ) ;
#8965=CARTESIAN_POINT ( 'NONE',  ( -13.94227320128385017, 1.734723475976807094E-15, -160.5206178152066343 ) ) ;
#8970=DIRECTION ( 'NONE',  ( -0.000000000000000000, -1.000000000000000000, -0.000000000000000000 ) ) ;
#8975=CARTESIAN_POINT ( 'NONE',  ( -3.768042520877054269, 1.734723475976807094E-15, -109.5986228335332129 ) ) ;
#8989=CARTESIAN_POINT ( 'NONE',  ( -9.721966606378851239, 5.000000000000000888, -116.3614657639809309 ) ) ;
#8991=CARTESIAN_POINT ( 'NONE',  ( 8.954409718278865782, 11.89299648869835835, 1.991138219077579041 ) ) ;
#8992=CARTESIAN_POINT ( 'NONE',  ( 12.76858567064540217, 3.999999999993260502, -166.6103056774037441 ) ) ;
#8998=VECTOR ( 'NONE', #11302, 1000.000000000000114 ) ;
#9004=EDGE_CURVE ( 'NONE', #14341, #13571, #6607, .T. ) ;
#9005=CARTESIAN_POINT ( 'NONE',  ( 11.07647859176971039, 15.00000000000000000, -126.6612394307274911 ) ) ;
#9006=DIRECTION ( 'NONE',  ( -0.000000000000000000, 1.000000000000000000, -0.000000000000000000 ) ) ;
#9007=CARTESIAN_POINT ( 'NONE',  ( 23.17896007687009075, 0.3998921152608300722, -138.1654099684218409 ) ) ;
#9013=ORIENTED_EDGE ( 'NONE', *, *, #7717, .F. ) ;
#9014=B_SPLINE_CURVE_WITH_KNOTS ( 'NONE', 3,
 ( #4393, #11570, #14928, #10418, #5397, #7941, #4324, #9028, #12815, #8089, #2222, #6711, #10112, #5548, #13910, #12504 ),
 .UNSPECIFIED., .F., .F.,
 ( 4, 2, 2, 2, 2, 2, 2, 4 ),
 ( 3.469446951953614189E-18, 0.0005010218446280251129, 0.001002043689256046756, 0.001503065533884068291, 0.002004087378512090043, 0.002505109223140111578, 0.003006131067768133113, 0.004008174757024192229 ),
 .UNSPECIFIED. ) ;
#9015=CARTESIAN_POINT ( 'NONE',  ( -6.738069272571859614, 14.39261927056258372, -116.5044176451309852 ) ) ;
#9022=CARTESIAN_POINT ( 'NONE',  ( 24.07280085736360675, 5.000000000000000888, -135.1358744081167913 ) ) ;
#9028=CARTESIAN_POINT ( 'NONE',  ( 10.58382518318612320, 14.03954883485831751, -106.8470192801346030 ) ) ;
#9032=CARTESIAN_POINT ( 'NONE',  ( -4.234402844927150689, 0.000000000000000000, -117.4888040839639558 ) ) ;
#9033=ORIENTED_EDGE ( 'NONE', *, *, #4363, .F. ) ;
#9034=CARTESIAN_POINT ( 'NONE',  ( -9.721966606378851239, 5.000000000000000888, -116.3614657639809309 ) ) ;
#9039=CARTESIAN_POINT ( 'NONE',  ( 8.236624398825258098, 15.00000000000000000, -106.5667377758158523 ) ) ;
#9040=FACE_OUTER_BOUND ( 'NONE', #2718, .T. ) ;
#9042=ADVANCED_FACE ( 'NONE', ( #6774 ), #11913, .T. ) ;
#9043=CARTESIAN_POINT ( 'NONE',  ( -28.70971482902378114, 3.999999999999513278, -179.7031761687850349 ) ) ;
#9044=CARTESIAN_POINT ( 'NONE',  ( 11.77099615976924163, 1.493628967302184973, -165.6844967162601279 ) ) ;
#9049=ORIENTED_EDGE ( 'NONE', *, *, #2836, .T. ) ;
#9050=DIRECTION ( 'NONE',  ( -0.000000000000000000, 1.000000000000000000, 0.000000000000000000 ) ) ;
#9052=CARTESIAN_POINT ( 'NONE',  ( -25.14123021401396940, 8.651900396264618934E-15, -199.0874206847575749 ) ) ;
#9053=CARTESIAN_POINT ( 'NONE',  ( 6.410864412206024987, 14.96873749810645826, 0.9153280175020522824 ) ) ;
#9054=CARTESIAN_POINT ( 'NONE',  ( 4.246495378557483491, 8.673617379884035472E-16, -105.2373590921493758 ) ) ;
#9056=CARTESIAN_POINT ( 'NONE',  ( 24.53888684075532467, 2.337595819977410685E-12, -142.6514391812058591 ) ) ;
#9059=CARTESIAN_POINT ( 'NONE',  ( 17.50071171097425804, 8.749999999999998224, -91.70093451412481045 ) ) ;
#9067=CARTESIAN_POINT ( 'NONE',  ( 9.980434402550784512, 5.834507182123311431, -43.94877651782068995 ) ) ;
#9068=B_SPLINE_CURVE_WITH_KNOTS ( 'NONE', 3,
 ( #11247, #5374, #819, #14673, #14822, #12557, #13510, #10016, #11398, #4221 ),
 .UNSPECIFIED., .F., .F.,
 ( 4, 2, 2, 2, 4 ),
 ( 0.000000000000000000, 0.0002464242564425689190, 0.0004928485128851378379, 0.0007392727693277068111, 0.0009856970257702756758 ),
 .UNSPECIFIED. ) ;
#9069=CARTESIAN_POINT ( 'NONE',  ( 8.571367539318496043, 12.50000000000000000, -116.3909463212235806 ) ) ;
#9078=CARTESIAN_POINT ( 'NONE',  ( -8.208951728224976208, 13.46737988720133750, -116.7121244410452334 ) ) ;
#9080=CARTESIAN_POINT ( 'NONE',  ( 8.852045268163109881, 12.49999999999999822, -117.5747611282338596 ) ) ;
#9081=CARTESIAN_POINT ( 'NONE',  ( -9.721966606378851239, 10.00000000000000000, -116.3614657639809309 ) ) ;
#9083=CARTESIAN_POINT ( 'NONE',  ( 25.53732853817565740, 1.428021340339478584, -137.8769250524031804 ) ) ;
#9087=CARTESIAN_POINT ( 'NONE',  ( -4.452859729112454978, 4.000000000000000888, -143.4037473448349829 ) ) ;
#9090=CARTESIAN_POINT ( 'NONE',  ( -7.289398910521209807, 14.05303354678142824, -116.2745874757426918 ) ) ;
#9093=CARTESIAN_POINT ( 'NONE',  ( -25.32353976185253330, 1.355199924532299205, -206.8830429655051830 ) ) ;
#9096=CARTESIAN_POINT ( 'NONE',  ( 11.04730217088350663, 5.000000000000000888, -107.1178495010082941 ) ) ;
#9097=PLANE ( 'NONE',  #9643 ) ;
#9101=AXIS2_PLACEMENT_3D ( 'NONE', #8418, #12137, #3710 ) ;
#9102=ADVANCED_FACE ( 'NONE', ( #13739 ), #5017, .T. ) ;
#9105=EDGE_CURVE ( 'NONE', #5472, #4732, #8962, .T. ) ;
#9107=CARTESIAN_POINT ( 'NONE',  ( -8.265142125449676413, 1.586851510356210415, -116.6996609440855934 ) ) ;
#9109=CARTESIAN_POINT ( 'NONE',  ( 11.32016196459919755, 12.66760504685707822, -106.4092894470422124 ) ) ;
#9112=CARTESIAN_POINT ( 'NONE',  ( -24.40461474964762090, 2.124593680485182396E-15, -208.9486585025150873 ) ) ;
#9119=CARTESIAN_POINT ( 'NONE',  ( -25.55679448025485812, 2.417363203818269302, -207.9855790150824362 ) ) ;
#9121=CARTESIAN_POINT ( 'NONE',  ( 8.935548306764875548, 10.16392762569079800, 2.855381327240379630 ) ) ;
#9122=CARTESIAN_POINT ( 'NONE',  ( -0.06526978513835804407, 5.000000000000000888, -101.7940732946829598 ) ) ;
#9124=AXIS2_PLACEMENT_3D ( 'NONE', #1758, #11182, #4542 ) ;
#9126=DIRECTION ( 'NONE',  ( 0.000000000000000000, 0.000000000000000000, 1.000000000000000000 ) ) ;
#9131=CARTESIAN_POINT ( 'NONE',  ( -6.269035454201815405, 12.12141402271314305, -125.0025068202018019 ) ) ;
#9135=CARTESIAN_POINT ( 'NONE',  ( 8.990525241558630754, 12.49999999999999822, 0.3362996048474836686 ) ) ;
#9141=EDGE_LOOP ( 'NONE', ( #949, #8139, #6199, #6543 ) ) ;
#9148=AXIS2_PLACEMENT_3D ( 'NONE', #11078, #2823, #8525 ) ;
#9149=CARTESIAN_POINT ( 'NONE',  ( 9.948146083160592568, 11.56847231179307300, -43.54255919497041560 ) ) ;
#9151=EDGE_CURVE ( 'NONE', #3245, #9933, #4955, .T. ) ;
#9154=CARTESIAN_POINT ( 'NONE',  ( -4.873637833193480873, 15.00000000000000000, -117.2491930705805885 ) ) ;
#9156=CARTESIAN_POINT ( 'NONE',  ( 10.12352296778766814, 15.00000000000000000, -125.3801087895597135 ) ) ;
#9157=CARTESIAN_POINT ( 'NONE',  ( -7.472766077161554499, 14.05285657010038847, -116.8715385114339824 ) ) ;
#9159=CARTESIAN_POINT ( 'NONE',  ( 25.18430511132843108, 1.421781986552433485, -138.4549000095262272 ) ) ;
#9161=AXIS2_PLACEMENT_3D ( 'NONE', #11024, #512, #3839 ) ;
#9165=CARTESIAN_POINT ( 'NONE',  ( 8.861879677533035959, 12.49999999999999822, -108.3481013197220619 ) ) ;
#9168=VERTEX_POINT ( 'NONE', #10779 ) ;
#9169=DIRECTION ( 'NONE',  ( 0.000000000000000000, 0.000000000000000000, -1.000000000000000000 ) ) ;
#9172=AXIS2_PLACEMENT_3D ( 'NONE', #9475, #15223, #12654 ) ;
#9173=CARTESIAN_POINT ( 'NONE',  ( -24.79172285805294251, 2.627299923518312763, -208.0710315741841043 ) ) ;
#9176=CARTESIAN_POINT ( 'NONE',  ( 8.305394803915289614, 5.000000000000000888, -114.0089953534778004 ) ) ;
#9177=ORIENTED_EDGE ( 'NONE', *, *, #7217, .F. ) ;
#9180=PLANE ( 'NONE',  #4525 ) ;
#9188=CARTESIAN_POINT ( 'NONE',  ( 9.958563954548985464, 4.811570552143352941, -44.18269933957010664 ) ) ;
#9189=ORIENTED_EDGE ( 'NONE', *, *, #13876, .F. ) ;
#9190=CARTESIAN_POINT ( 'NONE',  ( -27.59894172905100973, 3.999999999999963585, -206.0619156399042993 ) ) ;
#9192=ADVANCED_FACE ( 'NONE', ( #3367 ), #11297, .T. ) ;
#9195=EDGE_CURVE ( 'NONE', #4732, #273, #8611, .T. ) ;
#9197=ORIENTED_EDGE ( 'NONE', *, *, #8680, .F. ) ;
#9199=DIRECTION ( 'NONE',  ( 0.02181900108494737658, 0.000000000000000000, -0.9997619372588931741 ) ) ;
#9200=CARTESIAN_POINT ( 'NONE',  ( 6.130230623468325035, 11.30611287585377589, 5.118568765223321826 ) ) ;
#9201=CARTESIAN_POINT ( 'NONE',  ( -8.199037228203923888, -3.875321772615099985E-11, -114.3845095685870490 ) ) ;
#9208=CARTESIAN_POINT ( 'NONE',  ( 21.22030245073296228, 8.195043764685355780E-16, -138.8546042205708773 ) ) ;
#9213=ORIENTED_EDGE ( 'NONE', *, *, #2154, .F. ) ;
#9215=CARTESIAN_POINT ( 'NONE',  ( -13.51590403952440234, 1.734723475976807094E-15, -183.0154514670591936 ) ) ;
#9219=EDGE_CURVE ( 'NONE', #881, #1120, #1876, .T. ) ;
#9222=( BOUNDED_SURFACE ( )  B_SPLINE_SURFACE ( 3, 2, ( 
 ( #13929, #15175, #10217 ),
 ( #9121, #3170, #10285 ),
 ( #11444, #3400, #867 ),
 ( #5570, #12607, #9200 ),
 ( #1087, #15097, #14951 ),
 ( #2172, #11521, #4491 ),
 ( #4346, #9277, #8109 ),
 ( #12913, #6876, #8037 ),
 ( #12836, #5718, #14074 ),
 ( #937, #2326, #7025 ),
 ( #10437, #6952, #4412 ),
 ( #13775, #11739, #4568 ),
 ( #11670, #2098, #7961 ),
 ( #10514, #5794, #6732 ),
 ( #15021, #3249, #15250 ),
 ( #6805, #10356, #9053 ),
 ( #4640, #9350, #7882 ),
 ( #2022, #2628, #3554 ) ),
 .UNSPECIFIED., .F., .F., .T. ) 
 B_SPLINE_SURFACE_WITH_KNOTS ( ( 4, 2, 2, 2, 2, 2, 2, 2, 4 ),
 ( 3, 3 ),
 ( 0.01045536940180365887, 0.01094738860842426123, 0.01143940781504486186, 0.01193142702166546248, 0.01242344622828606485, 0.01291546543490666547, 0.01340748464152726610, 0.01389950384814786846, 0.01439152305476846909 ),
 ( 0.000000000000000000, 1.000000000000000000 ),
 .UNSPECIFIED. ) 
 GEOMETRIC_REPRESENTATION_ITEM ( )  RATIONAL_B_SPLINE_SURFACE ( (
 ( 1.000000000000000000, 0.6694682279269850156, 1.000000000000000000),
 ( 1.000000000000000000, 0.6694691252012310301, 1.000000000000000000),
 ( 1.000000000000000000, 0.6695768079868921197, 1.000000000000000000),
 ( 1.000000000000000000, 0.6700344632551947788, 1.000000000000000000),
 ( 1.000000000000000000, 0.6703764894997463752, 1.000000000000000000),
 ( 1.000000000000000000, 0.6713200582808653838, 1.000000000000000000),
 ( 1.000000000000000000, 0.6719288413528142767, 1.000000000000000000),
 ( 1.000000000000000000, 0.6734679306280143551, 1.000000000000000000),
 ( 1.000000000000000000, 0.6743949249898886222, 1.000000000000000000),
 ( 1.000000000000000000, 0.6766890287557600914, 1.000000000000000000),
 ( 1.000000000000000000, 0.6780280999877503767, 1.000000000000000000),
 ( 1.000000000000000000, 0.6812929544910970581, 1.000000000000000000),
 ( 1.000000000000000000, 0.6832424793221053561, 1.000000000000000000),
 ( 1.000000000000000000, 0.6879706062521270260, 1.000000000000000000),
 ( 1.000000000000000000, 0.6907332617435087974, 1.000000000000000000),
 ( 1.000000000000000000, 0.6976599582870975924, 1.000000000000000000),
 ( 1.000000000000000000, 0.7018653012264122193, 1.000000000000000000),
 ( 1.000000000000000000, 0.7071067811865473507, 1.000000000000000000) ) ) 
 REPRESENTATION_ITEM ( '' )  SURFACE ( )  );
#9226=DIRECTION ( 'NONE',  ( 0.000000000000000000, 0.000000000000000000, 1.000000000000000000 ) ) ;
#9233=CARTESIAN_POINT ( 'NONE',  ( -4.924212822021372560, 14.97043413793575972, -117.3690025739556404 ) ) ;
#9235=CARTESIAN_POINT ( 'NONE',  ( 25.92117664022351420, 2.488669359944063242, -137.1713175122655173 ) ) ;
#9241=DIRECTION ( 'NONE',  ( 0.000000000000000000, 0.000000000000000000, -1.000000000000000000 ) ) ;
#9246=EDGE_CURVE ( 'NONE', #12872, #2589, #357, .T. ) ;
#9247=CARTESIAN_POINT ( 'NONE',  ( -6.442579204135082449, 14.53778547989058723, -116.6257450304697585 ) ) ;
#9248=CIRCLE ( 'NONE', #6532, 2.500000000000000000 ) ;
#9251=CARTESIAN_POINT ( 'NONE',  ( -25.43638953643460354, 0.8166224425976650325, -205.4887980176190752 ) ) ;
#9254=CARTESIAN_POINT ( 'NONE',  ( 10.77011162811585265, 5.000000000000002665, -107.4112503379939056 ) ) ;
#9269=EDGE_LOOP ( 'NONE', ( #8860, #5854, #579, #8583 ) ) ;
#9270=CARTESIAN_POINT ( 'NONE',  ( 8.640721352953065093, 3.280814622354975452, 2.680269431086986121 ) ) ;
#9277=CARTESIAN_POINT ( 'NONE',  ( 8.890868772111733875, 12.65371242469951341, 4.902628950838662014 ) ) ;
#9278=CARTESIAN_POINT ( 'NONE',  ( -0.5126277339370232111, 5.000000000000000888, -103.6859198938564646 ) ) ;
#9280=DIRECTION ( 'NONE',  ( 0.9997619372588932851, 0.000000000000000000, 0.02181900108494707127 ) ) ;
#9291=ORIENTED_EDGE ( 'NONE', *, *, #14807, .T. ) ;
#9307=EDGE_LOOP ( 'NONE', ( #3287, #8610, #2190, #264 ) ) ;
#9313=CARTESIAN_POINT ( 'NONE',  ( -27.47952516445719695, 4.000000000000000888, -206.2928504520293131 ) ) ;
#9316=AXIS2_PLACEMENT_3D ( 'NONE', #4820, #10767, #14335 ) ;
#9319=CARTESIAN_POINT ( 'NONE',  ( -0.8896971555397489295, 9.999999999999998224, -104.6801027822219936 ) ) ;
#9322=CARTESIAN_POINT ( 'NONE',  ( -25.12160904166909958, 2.323552219295974108, -208.4222310589716471 ) ) ;
#9323=EDGE_CURVE ( 'NONE', #2594, #7276, #3295, .T. ) ;
#9329=FACE_OUTER_BOUND ( 'NONE', #11256, .T. ) ;
#9331=ORIENTED_EDGE ( 'NONE', *, *, #4783, .F. ) ;
#9340=ADVANCED_FACE ( 'NONE', ( #14002 ), #9222, .T. ) ;
#9342=CARTESIAN_POINT ( 'NONE',  ( 9.943023108890811201, 5.000000000000000888, -43.30782091980646697 ) ) ;
#9350=CARTESIAN_POINT ( 'NONE',  ( 8.983776437537306592, 15.03735113318141714, 0.6455345399050246291 ) ) ;
#9352=CARTESIAN_POINT ( 'NONE',  ( 8.536856906383286869, 0.000000000000000000, -164.4613227688425354 ) ) ;
#9356=CARTESIAN_POINT ( 'NONE',  ( 25.98238260393377175, 2.581044006060433382, -137.1487496856579753 ) ) ;
#9361=EDGE_LOOP ( 'NONE', ( #11754, #6148, #11823 ) ) ;
#9362=ORIENTED_EDGE ( 'NONE', *, *, #2194, .F. ) ;
#9363=CARTESIAN_POINT ( 'NONE',  ( 9.653464198873995983, 12.50000000000000000, -108.9308074128229862 ) ) ;
#9372=( NAMED_UNIT ( * ) PLANE_ANGLE_UNIT ( ) SI_UNIT ( $, .RADIAN. ) );
#9374=AXIS2_PLACEMENT_3D ( 'NONE', #2051, #9006, #10246 ) ;
#9377=CARTESIAN_POINT ( 'NONE',  ( 13.35507181691441225, 0.000000000000000000, -132.8670847673578805 ) ) ;
#9379=CARTESIAN_POINT ( 'NONE',  ( 11.32016196459912649, 15.00000000000000000, -106.4092894470390291 ) ) ;
#9381=ORIENTED_EDGE ( 'NONE', *, *, #10609, .T. ) ;
#9382=EDGE_CURVE ( 'NONE', #9763, #13945, #832, .T. ) ;
#9385=CARTESIAN_POINT ( 'NONE',  ( -28.63722085524334204, 3.999999999999999112, -204.0000079243689868 ) ) ;
#9391=CARTESIAN_POINT ( 'NONE',  ( -3.899357168004182002E-10, 15.00000000000247624, -101.1952717268974311 ) ) ;
#9397=CARTESIAN_POINT ( 'NONE',  ( -25.33200545782566238, 0.2453806451254461896, -202.6873302614697252 ) ) ;
#9398=CARTESIAN_POINT ( 'NONE',  ( 4.950900406836922230, 0.000000000000000000, -134.4284351762048573 ) ) ;
#9401=CIRCLE ( 'NONE', #7416, 2.000000000000001776 ) ;
#9407=ADVANCED_FACE ( 'NONE', ( #3785 ), #8725, .T. ) ;
#9410=CARTESIAN_POINT ( 'NONE',  ( -5.794432043291358525, 6.000000000000000000, -125.0404107129116085 ) ) ;
#9414=DIRECTION ( 'NONE',  ( 0.9989498407774362043, 0.000000000000000000, 0.04581719776170026237 ) ) ;
#9419=AXIS2_PLACEMENT_3D ( 'NONE', #15272, #9226, #12943 ) ;
#9420=ORIENTED_EDGE ( 'NONE', *, *, #6390, .F. ) ;
#9421=CARTESIAN_POINT ( 'NONE',  ( 8.875022499991118252, 5.000000000000000888, 5.628716256677545715 ) ) ;
#9425=ORIENTED_EDGE ( 'NONE', *, *, #4053, .F. ) ;
#9429=CARTESIAN_POINT ( 'NONE',  ( 9.891575892914513446, 14.76107634086678644, -106.0971120608575120 ) ) ;
#9433=CARTESIAN_POINT ( 'NONE',  ( 13.15367060044211556, 0.000000000000000000, -166.3809663071982641 ) ) ;
#9437=DIRECTION ( 'NONE',  ( -0.000000000000000000, 1.000000000000000000, -0.000000000000000000 ) ) ;
#9450=CARTESIAN_POINT ( 'NONE',  ( -7.490165920340420946, 1.096071398114234263, -116.1895725676946682 ) ) ;
#9451=ADVANCED_BREP_SHAPE_REPRESENTATION ( '', ( #2140, #9419 ), #3238 ) ;
#9452=VECTOR ( 'NONE', #2530, 1000.000000000000000 ) ;
#9454=CYLINDRICAL_SURFACE ( 'NONE', #3716, 1.000000000000000888 ) ;
#9455=DIRECTION ( 'NONE',  ( 0.000000000000000000, 0.000000000000000000, 1.000000000000000000 ) ) ;
#9459=CARTESIAN_POINT ( 'NONE',  ( 10.02128254425321607, 15.00000000000000000, -108.3753986617072371 ) ) ;
#9460=CARTESIAN_POINT ( 'NONE',  ( 5.853739503561296686, 8.673617379884035472E-16, -123.2563334432540785 ) ) ;
#9465=ORIENTED_EDGE ( 'NONE', *, *, #5175, .T. ) ;
#9466=ORIENTED_EDGE ( 'NONE', *, *, #5550, .F. ) ;
#9471=CARTESIAN_POINT ( 'NONE',  ( 4.892302586673455522, 15.00000000000000000, -102.5092683516998875 ) ) ;
#9475=CARTESIAN_POINT ( 'NONE',  ( 29.21736815051484015, 8.773889247172311556, -44.21329492081407153 ) ) ;
#9484=CARTESIAN_POINT ( 'NONE',  ( 1.041036260628787957, 5.000000000000000888, -139.4530670678226443 ) ) ;
#9489=CARTESIAN_POINT ( 'NONE',  ( 7.533261943714915532, 0.1450191290813469813, -105.4228757050405960 ) ) ;
#9495=CARTESIAN_POINT ( 'NONE',  ( 5.149405770047748021, 1.500743523323658346, 3.597836686962641917 ) ) ;
#9497=VECTOR ( 'NONE', #13764, 1000.000000000000000 ) ;
#9503=CARTESIAN_POINT ( 'NONE',  ( 26.64925767285982161, 4.000000000000000000, -138.6957041034480653 ) ) ;
#9504=CARTESIAN_POINT ( 'NONE',  ( 10.25363971656158668, 14.55503923202592098, -106.4026536807294718 ) ) ;
#9521=ORIENTED_EDGE ( 'NONE', *, *, #9246, .F. ) ;
#9531=CARTESIAN_POINT ( 'NONE',  ( 4.074537004179775046, 8.673617379884034486E-16, -119.0111424115291356 ) ) ;
#9533=CARTESIAN_POINT ( 'NONE',  ( -4.876757625501888072, 15.00000000000000355, -115.1249378319107421 ) ) ;
#9536=CARTESIAN_POINT ( 'NONE',  ( 6.586989535938814200, 1.734723475976807094E-15, -124.5540024164598378 ) ) ;
#9539=CARTESIAN_POINT ( 'NONE',  ( -25.11906781955738310, 0.000000000000000000, -198.9681998140721078 ) ) ;
#9542=CARTESIAN_POINT ( 'NONE',  ( -25.99849160774861900, 4.000000000000000000, -208.3968943305774815 ) ) ;
#9546=CARTESIAN_POINT ( 'NONE',  ( 2.299001413603840138, 15.00000000000000000, -109.5170782816550030 ) ) ;
#9549=CARTESIAN_POINT ( 'NONE',  ( 12.84147110302715511, 2.904872082602520944, -165.9573549719088135 ) ) ;
#9556=CARTESIAN_POINT ( 'NONE',  ( 26.71007981443199952, 5.000000000000000888, -136.8791680534710054 ) ) ;
#9558=CARTESIAN_POINT ( 'NONE',  ( 3.434326385468031368E-15, 5.000000000000000000, -105.0258972447171857 ) ) ;
#9560=CARTESIAN_POINT ( 'NONE',  ( 10.02700419641868557, 1.638247714484150519, -106.0252156366010610 ) ) ;
#9565=CARTESIAN_POINT ( 'NONE',  ( 4.078835579805053513, 0.1704923352145251980, -0.08935591895255695638 ) ) ;
#9570=ORIENTED_EDGE ( 'NONE', *, *, #534, .T. ) ;
#9581=FACE_OUTER_BOUND ( 'NONE', #4233, .T. ) ;
#9584=CARTESIAN_POINT ( 'NONE',  ( -1.224736468745108775, 5.434031181108818783E-13, -142.0096238726336821 ) ) ;
#9586=CARTESIAN_POINT ( 'NONE',  ( 8.390458931657674313, 2.708951583600975876, 2.526057450858589792 ) ) ;
#9592=CARTESIAN_POINT ( 'NONE',  ( -24.75251826597561333, 8.673617379884035472E-16, -198.2590867002109576 ) ) ;
#9598=CARTESIAN_POINT ( 'NONE',  ( -5.534063745943522683, 0.09777223664412376669, -117.1292924427800415 ) ) ;
#9600=EDGE_CURVE ( 'NONE', #12872, #13945, #1820, .T. ) ;
#9602=CARTESIAN_POINT ( 'NONE',  ( 3.460515205134051975, 8.673617379884035472E-16, -111.7394307393016391 ) ) ;
#9605=PLANE ( 'NONE',  #14766 ) ;
#9607=CARTESIAN_POINT ( 'NONE',  ( -7.251835631655214165, 5.000000000000797584, -123.8995801872340223 ) ) ;
#9614=CARTESIAN_POINT ( 'NONE',  ( 26.78844938926727437, 3.550418194419153739, -138.2511778740417299 ) ) ;
#9624=CARTESIAN_POINT ( 'NONE',  ( 12.34479200262613396, 1.921688117712943011, -165.5931851613482593 ) ) ;
#9627=B_SPLINE_CURVE_WITH_KNOTS ( 'NONE', 3,
 ( #1701, #13620, #9974, #2795, #14713, #781, #4112, #3022, #3090, #11282, #12517, #8814, #10050, #7498, #13543, #7649, #10123, #5487 ),
 .UNSPECIFIED., .F., .F.,
 ( 4, 2, 2, 2, 2, 2, 2, 2, 4 ),
 ( -1.730026862698029293E-05, 0.002001214906283857280, 0.003010472493739274440, 0.003515101287466980418, 0.004019730081194686395, 0.005028987668650091412, 0.006038245256105494695, 0.007047502843560897977, 0.008056760431016302126 ),
 .UNSPECIFIED. ) ;
#9633=CARTESIAN_POINT ( 'NONE',  ( -2.237745678288944440, 15.00000000000000711, -122.9455479326446437 ) ) ;
#9635=CIRCLE ( 'NONE', #25, 3.000000000000011990 ) ;
#9637=CARTESIAN_POINT ( 'NONE',  ( 0.000000000000000000, 9.999999999999998224, -100.6237003951525537 ) ) ;
#9639=AXIS2_PLACEMENT_3D ( 'NONE', #4950, #2638, #12138 ) ;
#9640=CARTESIAN_POINT ( 'NONE',  ( 9.627700091802285698, 1.251235758015203592, -106.1653571646377259 ) ) ;
#9643=AXIS2_PLACEMENT_3D ( 'NONE', #6853, #13818, #3145 ) ;
#9644=FACE_OUTER_BOUND ( 'NONE', #1591, .T. ) ;
#9647=CARTESIAN_POINT ( 'NONE',  ( 4.510303310612941097, 0.6340196074359315537, 2.016023895169278379 ) ) ;
#9655=CARTESIAN_POINT ( 'NONE',  ( 3.717577911061872520, 5.000000000000000888, -143.6771719914432595 ) ) ;
#9663=CARTESIAN_POINT ( 'NONE',  ( 9.068716941525980957, 1.734723475976807094E-15, -163.1923081219560174 ) ) ;
#9665=DIRECTION ( 'NONE',  ( -0.000000000000000000, -1.000000000000000000, -0.000000000000000000 ) ) ;
#9666=EDGE_CURVE ( 'NONE', #2133, #10636, #11232, .T. ) ;
#9668=CARTESIAN_POINT ( 'NONE',  ( -15.50355452676521040, 8.673617379884035472E-16, -162.8135211086045899 ) ) ;
#9673=ORIENTED_EDGE ( 'NONE', *, *, #8163, .T. ) ;
#9675=CARTESIAN_POINT ( 'NONE',  ( -23.43478651890449171, 8.673617379884035472E-16, -196.1076013386743853 ) ) ;
#9681=CARTESIAN_POINT ( 'NONE',  ( -6.822452048366741018, 0.5769591942652574357, -117.0063474466234084 ) ) ;
#9685=CARTESIAN_POINT ( 'NONE',  ( 5.760783416743275431, -1.035187345108135067E-30, -105.7086590657731904 ) ) ;
#9687=DIRECTION ( 'NONE',  ( 0.000000000000000000, -0.000000000000000000, 1.000000000000000000 ) ) ;
#9691=CARTESIAN_POINT ( 'NONE',  ( 4.950900406836953316, -4.336808689942017736E-15, -134.4284351762049141 ) ) ;
#9692=CARTESIAN_POINT ( 'NONE',  ( 23.85593715806772153, 5.000000000000000888, -134.9913929663534873 ) ) ;
#9698=CARTESIAN_POINT ( 'NONE',  ( 21.23839455451635061, 4.156108327861118244E-16, -138.9326824654702648 ) ) ;
#9700=CIRCLE ( 'NONE', #11937, 0.9999999999999988898 ) ;
#9703=ORIENTED_EDGE ( 'NONE', *, *, #9600, .F. ) ;
#9710=AXIS2_PLACEMENT_3D ( 'NONE', #13443, #12023, #1675 ) ;
#9713=CARTESIAN_POINT ( 'NONE',  ( -9.385448347264267355, 15.00000000000000000, -115.3551636530117150 ) ) ;
#9715=EDGE_CURVE ( 'NONE', #5674, #13215, #10105, .T. ) ;
#9719=CARTESIAN_POINT ( 'NONE',  ( 9.044950117654433797, 6.000000000000000000, -141.4826476090360643 ) ) ;
#9720=AXIS2_PLACEMENT_3D ( 'NONE', #14724, #13402, #9913 ) ;
#9721=VECTOR ( 'NONE', #15181, 1000.000000000000000 ) ;
#9727=CARTESIAN_POINT ( 'NONE',  ( 7.868841884385653351, 0.2423173772081719524, -105.4238801664120047 ) ) ;
#9733=ORIENTED_EDGE ( 'NONE', *, *, #12014, .F. ) ;
#9734=CARTESIAN_POINT ( 'NONE',  ( 4.402343282610404529, 0.5131405436234475204, 1.653012093462698617 ) ) ;
#9743=AXIS2_PLACEMENT_3D ( 'NONE', #5747, #14261, #10611 ) ;
#9749=CARTESIAN_POINT ( 'NONE',  ( 11.27996230380671605, 0.9346580912078079617, -165.2299598695886971 ) ) ;
#9750=CARTESIAN_POINT ( 'NONE',  ( 26.64925767285982161, 4.000000000000000000, -138.6957041034480653 ) ) ;
#9751=CARTESIAN_POINT ( 'NONE',  ( 5.228075279701640099, 4.000000000000000000, -165.7939279834373849 ) ) ;
#9753=CARTESIAN_POINT ( 'NONE',  ( 5.228075279701640099, 1.000000000000000000, -167.7939279834373849 ) ) ;
#9754=CARTESIAN_POINT ( 'NONE',  ( 11.44399236068192849, 4.000000000000000000, -138.9341978221715976 ) ) ;
#9755=AXIS2_PLACEMENT_3D ( 'NONE', #6928, #913, #2149 ) ;
#9758=EDGE_LOOP ( 'NONE', ( #14092, #3907, #93, #14719, #10845 ) ) ;
#9763=VERTEX_POINT ( 'NONE', #21 ) ;
#9770=CARTESIAN_POINT ( 'NONE',  ( 0.6300320263538776722, -4.336808689942017736E-15, -128.5410338263872632 ) ) ;
#9786=B_SPLINE_CURVE_WITH_KNOTS ( 'NONE', 3,
 ( #2828, #9698, #7529, #192, #13340, #14431, #8529, #12314, #8769, #13501, #12083, #4902, #1507, #13184, #13263, #269, #9614, #12004, #14583, #2748 ),
 .UNSPECIFIED., .F., .F.,
 ( 4, 2, 2, 2, 2, 2, 2, 2, 2, 4 ),
 ( -1.419797821985954122E-05, 0.001094435061963930454, 0.002203068102147720704, 0.003311701142331510955, 0.004420334182515300338, 0.005528967222699090155, 0.006083283742790985930, 0.006637600262882880839, 0.007746233303066660247, 0.008854866343250441391 ),
 .UNSPECIFIED. ) ;
#9792=ORIENTED_EDGE ( 'NONE', *, *, #14897, .T. ) ;
#9800=DIRECTION ( 'NONE',  ( -0.02181900108494737658, 0.000000000000000000, 0.9997619372588931741 ) ) ;
#9801=CARTESIAN_POINT ( 'NONE',  ( 8.641297968024963083, 0.6305609033237062899, -105.9901394978445097 ) ) ;
#9805=VERTEX_POINT ( 'NONE', #12065 ) ;
#9806=CARTESIAN_POINT ( 'NONE',  ( 4.999884908349637946, 0.09438068890030250346, -1.653151978968653957 ) ) ;
#9811=DIRECTION ( 'NONE',  ( 0.9939692226109179130, 0.000000000000000000, -0.1096594022519158801 ) ) ;
#9814=CARTESIAN_POINT ( 'NONE',  ( 11.04730216892670569, 12.84598696159166487, -107.1178495030794693 ) ) ;
#9822=CARTESIAN_POINT ( 'NONE',  ( 12.90827548330815766, 3.452651285030396977, -166.3555584590855858 ) ) ;
#9824=CARTESIAN_POINT ( 'NONE',  ( -1.331179381611672374, 8.673617379884035472E-16, -147.1845506124080032 ) ) ;
#9826=CARTESIAN_POINT ( 'NONE',  ( 8.306309981135230558, 2.550729144823657979, 2.473100317603431186 ) ) ;
#9842=CARTESIAN_POINT ( 'NONE',  ( -3.846760974179296966, 15.00000000000000355, -118.7367476769033345 ) ) ;
#9843=CARTESIAN_POINT ( 'NONE',  ( -7.626890066815782632, 5.000000000000794032, -122.9684017742212632 ) ) ;
#9849=ORIENTED_EDGE ( 'NONE', *, *, #7231, .F. ) ;
#9859=CARTESIAN_POINT ( 'NONE',  ( 13.34352170149614025, 13.85492800443912387, -126.0862001755899371 ) ) ;
#9871=AXIS2_PLACEMENT_3D ( 'NONE', #8792, #13522, #13742 ) ;
#9875=CARTESIAN_POINT ( 'NONE',  ( 11.29096412601620258, 4.293855562754802513, -106.8042879785164274 ) ) ;
#9886=DIRECTION ( 'NONE',  ( 0.000000000000000000, 1.000000000000000000, 0.000000000000000000 ) ) ;
#9896=CARTESIAN_POINT ( 'NONE',  ( 1.078231930479278899, 6.000000000000000000, -139.4303258909232852 ) ) ;
#9900=DIRECTION ( 'NONE',  ( 0.000000000000000000, 0.000000000000000000, 1.000000000000000000 ) ) ;
#9913=DIRECTION ( 'NONE',  ( -0.02181900108494679719, 0.000000000000000000, 0.9997619372588931741 ) ) ;
#9914=ORIENTED_EDGE ( 'NONE', *, *, #7214, .T. ) ;
#9923=CARTESIAN_POINT ( 'NONE',  ( -3.149239014469442210, 5.000000000000002665, -131.9551168572792790 ) ) ;
#9924=CARTESIAN_POINT ( 'NONE',  ( 9.247146435752135574, 5.000000000000000888, -109.6962599557244715 ) ) ;
#9928=CARTESIAN_POINT ( 'NONE',  ( 8.935548306746156300, 9.999999999999998224, 2.855381328098127725 ) ) ;
#9933=VERTEX_POINT ( 'NONE', #10682 ) ;
#9935=CARTESIAN_POINT ( 'NONE',  ( -6.288157641191917335, 13.40945642053105225, -124.9981450708252595 ) ) ;
#9937=CARTESIAN_POINT ( 'NONE',  ( 9.998507851868444263, 12.56623780283944924, -45.85017076944640735 ) ) ;
#9938=CARTESIAN_POINT ( 'NONE',  ( 6.085378087782216561, 4.179870625069618484, 5.225355098807171750 ) ) ;
#9942=ORIENTED_EDGE ( 'NONE', *, *, #1644, .T. ) ;
#9949=FACE_OUTER_BOUND ( 'NONE', #14192, .T. ) ;
#9968=CARTESIAN_POINT ( 'NONE',  ( -9.385448347264267355, 5.000000000000000888, -115.3551636530117150 ) ) ;
#9971=AXIS2_PLACEMENT_3D ( 'NONE', #10798, #6001, #14375 ) ;
#9973=CARTESIAN_POINT ( 'NONE',  ( 12.41730312957572302, 2.668544226152360643, -166.2839238872912233 ) ) ;
#9974=CARTESIAN_POINT ( 'NONE',  ( 7.534811383515542360, 0.1271246988106354836, -105.5137719823530205 ) ) ;
#9975=CARTESIAN_POINT ( 'NONE',  ( -26.36649137993302361, 3.822280693179559147E-12, -175.2408862124428310 ) ) ;
#9981=DIRECTION ( 'NONE',  ( 0.000000000000000000, 1.000000000000000000, 0.000000000000000000 ) ) ;
#9987=CARTESIAN_POINT ( 'NONE',  ( -9.721966606022585111, 4.636404319106432581, -116.3614657654590587 ) ) ;
#9992=ADVANCED_FACE ( 'NONE', ( #6117 ), #332, .T. ) ;
#10000=CARTESIAN_POINT ( 'NONE',  ( 10.27157762081180969, -3.902699979233760293E-12, -107.9972514637445329 ) ) ;
#10002=CARTESIAN_POINT ( 'NONE',  ( 26.15341798802279527, 6.000000000000000000, -138.7600702976168066 ) ) ;
#10005=CARTESIAN_POINT ( 'NONE',  ( 9.997152224788115049, 5.773884043947351330, -44.28753052795517675 ) ) ;
#10007=CARTESIAN_POINT ( 'NONE',  ( 4.917302814907795749, 15.00000000000000178, -102.2758535390863273 ) ) ;
#10016=CARTESIAN_POINT ( 'NONE',  ( -24.69661280395743574, 4.000000000000000888, -209.0572573213358396 ) ) ;
#10018=CARTESIAN_POINT ( 'NONE',  ( 26.58801926426209405, 6.000000000000000000, -139.0072983920785532 ) ) ;
#10020=CARTESIAN_POINT ( 'NONE',  ( 8.930279828349792837, 15.00000000000000000, -123.5978143988205318 ) ) ;
#10024=ORIENTED_EDGE ( 'NONE', *, *, #8058, .F. ) ;
#10025=DIRECTION ( 'NONE',  ( -0.02181900108494707127, 0.000000000000000000, 0.9997619372588930631 ) ) ;
#10033=ORIENTED_EDGE ( 'NONE', *, *, #1844, .T. ) ;
#10043=VECTOR ( 'NONE', #163, 1000.000000000000000 ) ;
#10045=VERTEX_POINT ( 'NONE', #8588 ) ;
#10050=CARTESIAN_POINT ( 'NONE',  ( 10.55744226398496188, 2.749053926740207210, -106.8760807525077610 ) ) ;
#10051=CARTESIAN_POINT ( 'NONE',  ( -9.605448531522425171, 8.673617379884035472E-16, -155.1394882739618311 ) ) ;
#10059=CARTESIAN_POINT ( 'NONE',  ( 0.000000000000000000, 5.000000000000000888, -100.6237003951525679 ) ) ;
#10060=CARTESIAN_POINT ( 'NONE',  ( 8.495120055765772449, 0.4951638288707319036, -105.5936704557864800 ) ) ;
#10063=CARTESIAN_POINT ( 'NONE',  ( 26.73766085848597740, 5.000000000000000888, -138.7442440334353080 ) ) ;
#10067=CARTESIAN_POINT ( 'NONE',  ( -9.385448347264267355, 5.000000000000000888, -115.3551636530117150 ) ) ;
#10073=CARTESIAN_POINT ( 'NONE',  ( 4.165694389856393620, 1.734723475976807094E-15, -108.8942237923054250 ) ) ;
#10078=CARTESIAN_POINT ( 'NONE',  ( 8.990769910733003911, 12.49999999999999822, 0.3250886916252374026 ) ) ;
#10079=CARTESIAN_POINT ( 'NONE',  ( 10.51703944396922275, 12.50000000000000000, -121.3897425166904469 ) ) ;
#10086=CARTESIAN_POINT ( 'NONE',  ( 9.998602840258165259, 12.56502379761173671, -45.85452320410524862 ) ) ;
#10089=CARTESIAN_POINT ( 'NONE',  ( -8.611029641428904924, 12.67556477996888553, -115.7034661592606710 ) ) ;
#10091=CARTESIAN_POINT ( 'NONE',  ( 8.852045267489970115, 15.00000000000000178, -117.5747611283908043 ) ) ;
#10092=CARTESIAN_POINT ( 'NONE',  ( 23.49624735387704533, 0.5263503646385538914, -138.0521088526025153 ) ) ;
#10095=CARTESIAN_POINT ( 'NONE',  ( -18.35446420518660560, 3.999999999999999112, -158.2547620175516272 ) ) ;
#10101=CARTESIAN_POINT ( 'NONE',  ( 26.13050938914192756, 4.000000000000000000, -138.2605953772281566 ) ) ;
#10105=B_SPLINE_CURVE_WITH_KNOTS ( 'NONE', 3,
 ( #8205, #6754, #12937, #2117 ),
 .UNSPECIFIED., .F., .F.,
 ( 4, 4 ),
 ( 0.000000000000000000, 0.0005767408338914856592 ),
 .UNSPECIFIED. ) ;
#10106=CARTESIAN_POINT ( 'NONE',  ( 11.65935602426492146, 5.000000000000001776, -123.2257483849739828 ) ) ;
#10107=DIRECTION ( 'NONE',  ( 0.000000000000000000, 1.000000000000000000, 0.000000000000000000 ) ) ;
#10108=VERTEX_POINT ( 'NONE', #7661 ) ;
#10109=DIRECTION ( 'NONE',  ( 0.000000000000000000, 0.000000000000000000, 1.000000000000000000 ) ) ;
#10112=CARTESIAN_POINT ( 'NONE',  ( 9.798257320807429949, 14.75244170371860797, -106.4031996619075073 ) ) ;
#10113=CARTESIAN_POINT ( 'NONE',  ( 11.02703746864928469, 13.70076941827196393, -106.7007979685955661 ) ) ;
#10116=PRODUCT_DEFINITION_FORMATION_WITH_SPECIFIED_SOURCE ( 'ANY', '', #1532, .NOT_KNOWN. ) ;
#10117=CARTESIAN_POINT ( 'NONE',  ( 10.99340860758277927, 5.943472311793079221, -45.60560901953395785 ) ) ;
#10122=CARTESIAN_POINT ( 'NONE',  ( 6.509216192753445540, 15.00000000000000178, -109.6918098674199911 ) ) ;
#10123=CARTESIAN_POINT ( 'NONE',  ( 11.04730217088347466, 4.663186150664629714, -107.1178495010082514 ) ) ;
#10125=CARTESIAN_POINT ( 'NONE',  ( -13.29322798955594465, 4.000000000000054179, -151.9140868489417642 ) ) ;
#10130=DIRECTION ( 'NONE',  ( 8.764770998266003672E-18, -0.000000000000000000, 1.000000000000000000 ) ) ;
#10132=AXIS2_PLACEMENT_3D ( 'NONE', #3972, #8677, #13412 ) ;
#10135=B_SPLINE_CURVE_WITH_KNOTS ( 'NONE', 3,
 ( #4343, #561, #4191, #10060, #7580, #3167, #5272, #14796, #3029, #4269, #12374, #15018, #1791, #13629, #7736, #12456, #1873, #6578 ),
 .UNSPECIFIED., .F., .F.,
 ( 4, 2, 2, 2, 2, 2, 2, 2, 4 ),
 ( -1.729984944104041706E-05, 0.002003810841594060033, 0.003014366187111617960, 0.003519643859870403863, 0.004024921532629188899, 0.005035476878146755500, 0.006046032223664322101, 0.007056587569181887835, 0.008067142914699454437 ),
 .UNSPECIFIED. ) ;
#10136=B_SPLINE_CURVE_WITH_KNOTS ( 'NONE', 3,
 ( #1092, #8190, #12917, #12840, #3331, #7094, #7172, #2331, #7029, #11893, #2175, #11742, #1235, #5943, #83, #4795, #3634, #1316 ),
 .UNSPECIFIED., .F., .F.,
 ( 4, 2, 2, 2, 2, 2, 2, 2, 4 ),
 ( 0.000000000000000000, 0.002451912426773313405, 0.004903824853546626811, 0.006129781066933302595, 0.007355737280319980115, 0.009807649707093331684, 0.01225956213386668325, 0.01471147456064003829, 0.01961529941418670847 ),
 .UNSPECIFIED. ) ;
#10143=CARTESIAN_POINT ( 'NONE',  ( -6.756410658677025616, 10.62990111995887865, -124.9665698180028670 ) ) ;
#10145=VECTOR ( 'NONE', #11136, 1000.000000000000000 ) ;
#10152=CARTESIAN_POINT ( 'NONE',  ( -7.751437813422534795, 10.00000000000000000, -124.5369783794910319 ) ) ;
#10153=ORIENTED_EDGE ( 'NONE', *, *, #12794, .T. ) ;
#10154=CARTESIAN_POINT ( 'NONE',  ( 8.963174318014939246, 12.17502284788009170, 1.589538110194233855 ) ) ;
#10155=CARTESIAN_POINT ( 'NONE',  ( 1.171458888995337899, 15.00000000000000355, -111.2928373221764815 ) ) ;
#10163=CARTESIAN_POINT ( 'NONE',  ( 10.95283577138780728, 11.77391770468068088, -44.23857723416275434 ) ) ;
#10166=CARTESIAN_POINT ( 'NONE',  ( 4.606088890118262391, 0.7456749647984134421, 2.303154267099985830 ) ) ;
#10167=CARTESIAN_POINT ( 'NONE',  ( -9.385448346789152296, 10.36359568087253535, -115.3551636526205044 ) ) ;
#10171=CARTESIAN_POINT ( 'NONE',  ( 8.347943498143836294, 12.49999999999999822, -114.9028610997572457 ) ) ;
#10172=CARTESIAN_POINT ( 'NONE',  ( -5.928758847211410554, 14.76754297112742798, -117.1828119328369553 ) ) ;
#10175=CARTESIAN_POINT ( 'NONE',  ( -30.40484592373450212, 4.000000000000000888, -187.9928767041745061 ) ) ;
#10183=EDGE_CURVE ( 'NONE', #8015, #2663, #1076, .T. ) ;
#10185=CARTESIAN_POINT ( 'NONE',  ( 11.14636119983888385, 3.654497975985243841, -106.3565569454754041 ) ) ;
#10186=ADVANCED_FACE ( 'NONE', ( #7511 ), #12229, .T. ) ;
#10188=ADVANCED_FACE ( 'NONE', ( #641 ), #3394, .F. ) ;
#10189=CARTESIAN_POINT ( 'NONE',  ( 8.563244450085640835, 5.000000000000000000, -111.6252051639990981 ) ) ;
#10190=DIRECTION ( 'NONE',  ( -0.000000000000000000, 1.000000000000000000, -0.000000000000000000 ) ) ;
#10194=CARTESIAN_POINT ( 'NONE',  ( 4.516549078349731516, 2.547190344450775967, -1.663700395152574396 ) ) ;
#10204=CARTESIAN_POINT ( 'NONE',  ( 6.843830495165342143, 15.00000000000000000, -108.8700626460535261 ) ) ;
#10206=DIRECTION ( 'NONE',  ( -0.000000000000000000, -1.000000000000000000, -0.000000000000000000 ) ) ;
#10207=VERTEX_POINT ( 'NONE', #1794 ) ;
#10208=CARTESIAN_POINT ( 'NONE',  ( -23.09901293210274886, 3.999999999999755307, -165.9319877299972461 ) ) ;
#10212=ORIENTED_EDGE ( 'NONE', *, *, #6310, .T. ) ;
#10215=CARTESIAN_POINT ( 'NONE',  ( -25.68413237157757933, 0.4228586813406581824, -203.6825093939540920 ) ) ;
#10217=CARTESIAN_POINT ( 'NONE',  ( 6.122889832264990062, 9.999999999999761968, 5.281130614573721793 ) ) ;
#10218=AXIS2_PLACEMENT_3D ( 'NONE', #6355, #7583, #6427 ) ;
#10220=CIRCLE ( 'NONE', #11448, 5.000000000000000888 ) ;
#10226=DIRECTION ( 'NONE',  ( -0.000000000000000000, 1.000000000000000000, -0.000000000000000000 ) ) ;
#10230=CARTESIAN_POINT ( 'NONE',  ( 27.03835354040193195, 5.000000000000000888, -138.2189567750509980 ) ) ;
#10233=CARTESIAN_POINT ( 'NONE',  ( -5.309262520577839872, 6.000000000000000000, -125.0911079416483176 ) ) ;
#10234=CARTESIAN_POINT ( 'NONE',  ( 3.391286578035700217, 15.00000000000000000, -107.3770126362747419 ) ) ;
#10241=CARTESIAN_POINT ( 'NONE',  ( 10.00293577155236235, 11.69603995595522505, -43.86820082419217925 ) ) ;
#10243=CARTESIAN_POINT ( 'NONE',  ( -6.679542461294499134, 14.42304080565615543, -116.5285319886262414 ) ) ;
#10245=CARTESIAN_POINT ( 'NONE',  ( 9.146012981092644267, 12.49999999999999822, -118.4481327388941025 ) ) ;
#10246=DIRECTION ( 'NONE',  ( 0.000000000000000000, 0.000000000000000000, 1.000000000000000000 ) ) ;
#10247=CARTESIAN_POINT ( 'NONE',  ( 25.70480266353256482, 2.194422113504707283, -137.2509578016119463 ) ) ;
#10250=DIRECTION ( 'NONE',  ( 0.000000000000000000, -1.000000000000000000, 0.000000000000000000 ) ) ;
#10254=CARTESIAN_POINT ( 'NONE',  ( -5.525175898872149105, 14.85443352937157790, -116.9935625178452057 ) ) ;
#10255=DIRECTION ( 'NONE',  ( 0.02181900108494707474, 0.000000000000000000, -0.9997619372588932851 ) ) ;
#10257=CARTESIAN_POINT ( 'NONE',  ( -25.68068971291294744, 0.4053893758593278274, -203.6019930943793383 ) ) ;
#10260=CARTESIAN_POINT ( 'NONE',  ( 19.68155780323316151, 5.000000000000001776, -131.7762816226957057 ) ) ;
#10263=ADVANCED_FACE ( 'NONE', ( #1874 ), #6579, .F. ) ;
#10276=CARTESIAN_POINT ( 'NONE',  ( -26.45842032310348202, 3.999999999998672617, -207.8493744993166672 ) ) ;
#10277=CARTESIAN_POINT ( 'NONE',  ( 12.50482138048521641, 2.904909039721687236, -166.3652064813286700 ) ) ;
#10284=CARTESIAN_POINT ( 'NONE',  ( 1.320501113854931408, 15.00000000000000000, -137.8664870916819893 ) ) ;
#10285=CARTESIAN_POINT ( 'NONE',  ( 6.122889832127041743, 10.32785525203418509, 5.281130614556315273 ) ) ;
#10286=CARTESIAN_POINT ( 'NONE',  ( -6.310237929021329961, 1.734723475976807094E-15, -119.2996315833885035 ) ) ;
#10294=CARTESIAN_POINT ( 'NONE',  ( 8.895558325401111688, 6.000000000000000000, -125.4560052468458906 ) ) ;
#10297=ORIENTED_EDGE ( 'NONE', *, *, #4344, .F. ) ;
#10299=CARTESIAN_POINT ( 'NONE',  ( -3.025102703132700022, 15.00000000000000000, -116.3639557890653577 ) ) ;
#10303=ORIENTED_EDGE ( 'NONE', *, *, #11927, .F. ) ;
#10304=( BOUNDED_SURFACE ( )  B_SPLINE_SURFACE ( 3, 2, ( 
 ( #3547, #9421, #3468 ),
 ( #12905, #3320, #8030 ),
 ( #8254, #12755, #2318 ),
 ( #10429, #15166, #11803 ),
 ( #1219, #15010, #4561 ),
 ( #4403, #11731, #9270 ),
 ( #13994, #8102, #2618 ),
 ( #14379, #12199, #14537 ),
 ( #11881, #1455, #10655 ),
 ( #8557, #302, #7159 ),
 ( #6249, #13133, #8485 ),
 ( #144, #7321, #14291 ),
 ( #4930, #13050, #5929 ),
 ( #384, #8401, #4854 ),
 ( #9495, #3777, #13216 ),
 ( #5015, #7245, #14220 ),
 ( #6162, #12118, #12034 ),
 ( #10730, #3934, #10882 ),
 ( #9647, #69, #8636 ),
 ( #9734, #3692, #2543 ),
 ( #2462, #4781, #14463 ),
 ( #11958, #2777, #1382 ),
 ( #1303, #6084, #10801 ),
 ( #9565, #3859, #215 ),
 ( #1535, #13292, #7481 ),
 ( #13372, #2696, #3621 ),
 ( #8324, #7395, #10966 ),
 ( #6006, #5093, #9806 ) ),
 .UNSPECIFIED., .F., .F., .T. ) 
 B_SPLINE_SURFACE_WITH_KNOTS ( ( 4, 2, 2, 2, 2, 2, 2, 2, 2, 2, 2, 2, 2, 4 ),
 ( 3, 3 ),
 ( 0.000000000000000000, 0.0003820775045722776039, 0.0007641550091445552077, 0.001146232513716832812, 0.001337271266002971505, 0.001528310018289110415, 0.001910387522861388019, 0.002292465027433665623, 0.003056620036578220831, 0.003438697541150498652, 0.003820775045722776039, 0.004584930054867331246, 0.005349085064011886020, 0.006113240073156441662 ),
 ( 0.000000000000000000, 1.000000000000000000 ),
 .UNSPECIFIED. ) 
 GEOMETRIC_REPRESENTATION_ITEM ( )  RATIONAL_B_SPLINE_SURFACE ( (
 ( 1.000000000000000000, 0.6694682279269816849, 1.000000000000000000),
 ( 1.000000000000000000, 0.6694688976805022174, 1.000000000000000000),
 ( 1.000000000000000000, 0.6718652449342649158, 1.000000000000000000),
 ( 1.000000000000000000, 0.6808533733821083844, 1.000000000000000000),
 ( 1.000000000000000000, 0.6875604826314558604, 1.000000000000000000),
 ( 1.000000000000000000, 0.7038992507919969999, 1.000000000000000000),
 ( 1.000000000000000000, 0.7134862437630616894, 1.000000000000000000),
 ( 1.000000000000000000, 0.7292503528835072579, 1.000000000000000000),
 ( 1.000000000000000000, 0.7347607280474764968, 1.000000000000000000),
 ( 1.000000000000000000, 0.7459493779136278091, 1.000000000000000000),
 ( 1.000000000000000000, 0.7516437210088404708, 1.000000000000000000),
 ( 1.000000000000000000, 0.7688860810062153606, 1.000000000000000000),
 ( 1.000000000000000000, 0.7805878518874648231, 1.000000000000000000),
 ( 1.000000000000000000, 0.8038470659974755739, 1.000000000000000000),
 ( 1.000000000000000000, 0.8154457322603761993, 1.000000000000000000),
 ( 1.000000000000000000, 0.8485885531796709680, 1.000000000000000000),
 ( 1.000000000000000000, 0.8687647592111614747, 1.000000000000000000),
 ( 1.000000000000000000, 0.8953432496372137894, 1.000000000000000000),
 ( 1.000000000000000000, 0.9036225306460309303, 1.000000000000000000),
 ( 1.000000000000000000, 0.9186755269451735151, 1.000000000000000000),
 ( 1.000000000000000000, 0.9254787334919890585, 1.000000000000000000),
 ( 1.000000000000000000, 0.9438496984080199104, 1.000000000000000000),
 ( 1.000000000000000000, 0.9533694582932917827, 1.000000000000000000),
 ( 1.000000000000000000, 0.9678894448523732708, 1.000000000000000000),
 ( 1.000000000000000000, 0.9728964749375748067, 1.000000000000000000),
 ( 1.000000000000000000, 0.9793693877884432908, 1.000000000000000000),
 ( 1.000000000000000000, 0.9809066217507083074, 1.000000000000000000),
 ( 1.000000000000000000, 0.9811261306835751261, 1.000000000000000000) ) ) 
 REPRESENTATION_ITEM ( '' )  SURFACE ( )  );
#10310=CARTESIAN_POINT ( 'NONE',  ( 6.453443679602843375, 15.00000000000000000, -109.8021161339212455 ) ) ;
#10312=ORIENTED_EDGE ( 'NONE', *, *, #5175, .F. ) ;
#10313=CARTESIAN_POINT ( 'NONE',  ( 24.10521022763708743, 0.8297099929889686365, -137.8334368346246492 ) ) ;
#10322=DIRECTION ( 'NONE',  ( -1.000000000000000000, 0.000000000000000000, 0.000000000000000000 ) ) ;
#10325=CARTESIAN_POINT ( 'NONE',  ( -25.22140796077621872, 1.064333479732355909E-15, -199.9032618446891547 ) ) ;
#10331=ORIENTED_EDGE ( 'NONE', *, *, #1963, .T. ) ;
#10333=DIRECTION ( 'NONE',  ( 0.02181900108494707127, 0.000000000000000000, -0.9997619372588931741 ) ) ;
#10344=B_SPLINE_CURVE_WITH_KNOTS ( 'NONE', 3,
 ( #775, #1858, #5402, #6409, #13687, #10117 ),
 .UNSPECIFIED., .F., .F.,
 ( 4, 2, 4 ),
 ( 0.000000000000000000, 0.001008764465307790880, 0.002017528930615581761 ),
 .UNSPECIFIED. ) ;
#10347=CARTESIAN_POINT ( 'NONE',  ( -27.36259546841008827, 1.380486956869476911E-13, -204.7781919227250853 ) ) ;
#10356=CARTESIAN_POINT ( 'NONE',  ( 8.976478810040582346, 15.03641560954238088, 0.9799169515470964598 ) ) ;
#10357=CARTESIAN_POINT ( 'NONE',  ( -2.027137927904086201, 5.000000000000000888, -107.0032022124503044 ) ) ;
#10364=CARTESIAN_POINT ( 'NONE',  ( -6.790153584124030139, 10.31788924015992137, -124.9643354754709748 ) ) ;
#10366=EDGE_CURVE ( 'NONE', #40, #2594, #133, .T. ) ;
#10368=EDGE_CURVE ( 'NONE', #13477, #4330, #5568, .T. ) ;
#10373=CARTESIAN_POINT ( 'NONE',  ( 26.88776758612647200, 5.000000000000000888, -138.4814716795148684 ) ) ;
#10375=VERTEX_POINT ( 'NONE', #4409 ) ;
#10376=ORIENTED_EDGE ( 'NONE', *, *, #8477, .F. ) ;
#10377=CARTESIAN_POINT ( 'NONE',  ( 10.56600390958041302, 8.673617379884035472E-16, -167.0813103633617231 ) ) ;
#10384=B_SPLINE_CURVE_WITH_KNOTS ( 'NONE', 3,
 ( #2839, #8780, #439, #1666 ),
 .UNSPECIFIED., .F., .F.,
 ( 4, 4 ),
 ( 0.08237334560920292481, 0.08250179899282622520 ),
 .UNSPECIFIED. ) ;
#10387=CIRCLE ( 'NONE', #10877, 0.9999999999999987788 ) ;
#10388=AXIS2_PLACEMENT_3D ( 'NONE', #13370, #6552, #7708 ) ;
#10393=CARTESIAN_POINT ( 'NONE',  ( 26.71007981443199952, 6.000000000000000000, -136.8791680534710054 ) ) ;
#10396=CARTESIAN_POINT ( 'NONE',  ( 1.299830696487494386, 4.000000000000000000, -139.3994634862947635 ) ) ;
#10411=CARTESIAN_POINT ( 'NONE',  ( -25.21522606501703834, 1.851995413243205713, -207.7825160301809149 ) ) ;
#10414=CARTESIAN_POINT ( 'NONE',  ( 26.71007981443199952, 5.000000000000000888, -136.8791680534710054 ) ) ;
#10415=ORIENTED_EDGE ( 'NONE', *, *, #6650, .T. ) ;
#10418=CARTESIAN_POINT ( 'NONE',  ( 10.97402408521754857, 13.16001484901744334, -107.0745672077283785 ) ) ;
#10428=EDGE_LOOP ( 'NONE', ( #2844, #7004, #9849, #12518, #6836 ) ) ;
#10429=CARTESIAN_POINT ( 'NONE',  ( 6.052559506676158385, 3.990476221019045866, 5.174528079217774135 ) ) ;
#10434=ORIENTED_EDGE ( 'NONE', *, *, #3371, .T. ) ;
#10437=CARTESIAN_POINT ( 'NONE',  ( 8.957191258107528142, 11.99542373187157018, 1.863686112684491025 ) ) ;
#10439=CARTESIAN_POINT ( 'NONE',  ( 5.000000000000000000, 8.673617379884035472E-16, -100.6237003951525537 ) ) ;
#10445=DIRECTION ( 'NONE',  ( -0.9997619372588932851, -0.000000000000000000, -0.02181900108494707474 ) ) ;
#10451=VERTEX_POINT ( 'NONE', #1008 ) ;
#10453=CARTESIAN_POINT ( 'NONE',  ( 10.73212172315381885, 12.50000000000000533, -107.4514619188133082 ) ) ;
#10458=CARTESIAN_POINT ( 'NONE',  ( 26.64011553632023066, 4.666487833696466581, -138.9157185642569914 ) ) ;
#10462=EDGE_CURVE ( 'NONE', #7347, #14600, #842, .T. ) ;
#10464=CARTESIAN_POINT ( 'NONE',  ( -2.397620167341370845, 5.000000000000000888, -107.6176329143618062 ) ) ;
#10476=ORIENTED_EDGE ( 'NONE', *, *, #3712, .T. ) ;
#10483=CARTESIAN_POINT ( 'NONE',  ( 6.153839613028314837, 12.51224853425506289, 4.615052189839248697 ) ) ;
#10490=CARTESIAN_POINT ( 'NONE',  ( -25.70029544500438590, 0.7328807590276666950, -204.7564699162097099 ) ) ;
#10497=LINE ( 'NONE', #15229, #1305 ) ;
#10501=CARTESIAN_POINT ( 'NONE',  ( -6.371526220232841098, 5.000000000000000888, -125.9870988568622465 ) ) ;
#10505=CARTESIAN_POINT ( 'NONE',  ( 11.06771612204629207, 8.749999999999998224, -94.84204383295364948 ) ) ;
#10507=CARTESIAN_POINT ( 'NONE',  ( -25.49544145210780499, 8.673617379884035472E-16, -197.0346082499829095 ) ) ;
#10511=ORIENTED_EDGE ( 'NONE', *, *, #11272, .T. ) ;
#10513=CARTESIAN_POINT ( 'NONE',  ( -25.64914917419623208, 1.594688008273111635, -206.8106692875541910 ) ) ;
#10514=CARTESIAN_POINT ( 'NONE',  ( 8.973073561997775727, 12.37582002200307585, 1.135947805892676410 ) ) ;
#10517=CARTESIAN_POINT ( 'NONE',  ( 26.15341798802279527, 4.000000000000000000, -138.2600702976168350 ) ) ;
#10530=CARTESIAN_POINT ( 'NONE',  ( 14.22910372453204353, 6.000000000000000000, -126.5134921567817941 ) ) ;
#10536=CARTESIAN_POINT ( 'NONE',  ( -5.082498805844318568, 5.000000000000001776, -111.2070015758558696 ) ) ;
#10542=CARTESIAN_POINT ( 'NONE',  ( 25.37357285188495837, -5.098721647816789303E-12, -136.0302139099745773 ) ) ;
#10553=CARTESIAN_POINT ( 'NONE',  ( 8.673617379884035472E-16, 14.99999999999999645, -100.6237003951525679 ) ) ;
#10556=CARTESIAN_POINT ( 'NONE',  ( -25.49686867869201023, 0.3475987381038808111, -203.6525958643808281 ) ) ;
#10557=FACE_OUTER_BOUND ( 'NONE', #5623, .T. ) ;
#10560=CARTESIAN_POINT ( 'NONE',  ( 3.717577911061872520, 5.000000000000000888, -143.6771719914432595 ) ) ;
#10565=CARTESIAN_POINT ( 'NONE',  ( 9.044950117654433797, -4.000000000000000000, -141.4826476090360643 ) ) ;
#10572=CARTESIAN_POINT ( 'NONE',  ( 1.081679185590002756, 4.727159810604965706, -139.4347531963001643 ) ) ;
#10574=CARTESIAN_POINT ( 'NONE',  ( -25.15829320847776529, -1.662059052993006175E-12, -208.1809449273558528 ) ) ;
#10587=CARTESIAN_POINT ( 'NONE',  ( 16.45731177154546998, 8.749999999999998224, -89.72322964069195450 ) ) ;
#10588=CARTESIAN_POINT ( 'NONE',  ( 1.004809442601929836, 5.666666666666666963, -139.4752805618705622 ) ) ;
#10597=CARTESIAN_POINT ( 'NONE',  ( 8.364153288505452366, 12.49999999999999645, -112.7786105982117419 ) ) ;
#10606=DIRECTION ( 'NONE',  ( 0.000000000000000000, 0.000000000000000000, 1.000000000000000000 ) ) ;
#10609=EDGE_CURVE ( 'NONE', #7526, #11904, #13390, .T. ) ;
#10611=DIRECTION ( 'NONE',  ( 0.000000000000000000, 0.000000000000000000, -1.000000000000000000 ) ) ;
#10612=CARTESIAN_POINT ( 'NONE',  ( 12.21230042287087691, 5.000000000000000888, -124.0782217030330656 ) ) ;
#10614=DIRECTION ( 'NONE',  ( -8.764770998266002131E-18, 0.000000000000000000, -1.000000000000000000 ) ) ;
#10621=ORIENTED_EDGE ( 'NONE', *, *, #317, .F. ) ;
#10623=CARTESIAN_POINT ( 'NONE',  ( 6.321864114638128918, 14.74656758735381779, 1.877230377063963784 ) ) ;
#10626=VECTOR ( 'NONE', #4852, 1000.000000000000114 ) ;
#10632=VECTOR ( 'NONE', #7595, 1000.000000000000000 ) ;
#10636=VERTEX_POINT ( 'NONE', #9503 ) ;
#10646=DIRECTION ( 'NONE',  ( 0.000000000000000000, 0.000000000000000000, 1.000000000000000000 ) ) ;
#10648=CARTESIAN_POINT ( 'NONE',  ( 10.03945249976937859, 1.886766667216011495, -106.6275678995573060 ) ) ;
#10655=CARTESIAN_POINT ( 'NONE',  ( 8.358184211585273360, 2.650800484095609200, 2.505650865491267254 ) ) ;
#10671=CARTESIAN_POINT ( 'NONE',  ( 15.09707649861359613, 4.000000000000000000, -161.4544678506381388 ) ) ;
#10679=CARTESIAN_POINT ( 'NONE',  ( 11.04730217088350663, 12.49999999999999822, -107.1178495010082941 ) ) ;
#10682=CARTESIAN_POINT ( 'NONE',  ( 6.491365067585774362, 15.00000000000000000, 0.2705411889128706004 ) ) ;
#10687=CARTESIAN_POINT ( 'NONE',  ( 26.15341798802279527, 4.000000000000000000, -138.7600702976168066 ) ) ;
#10689=CARTESIAN_POINT ( 'NONE',  ( -9.739626904459424139, 15.00000000000000178, -116.2879091882953446 ) ) ;
#10691=CARTESIAN_POINT ( 'NONE',  ( 26.15341798802279527, 6.000000000000000000, -138.7600702976168066 ) ) ;
#10692=CARTESIAN_POINT ( 'NONE',  ( 11.09126156230712468, 2.140620105417839675E-13, -122.3351348873811162 ) ) ;
#10695=DIRECTION ( 'NONE',  ( -1.000000000000000000, 0.000000000000000000, 0.000000000000000000 ) ) ;
#10698=ORIENTED_EDGE ( 'NONE', *, *, #9151, .T. ) ;
#10704=CARTESIAN_POINT ( 'NONE',  ( 3.167496085402304207, 15.00000000000000000, -107.8568673623673959 ) ) ;
#10707=AXIS2_PLACEMENT_3D ( 'NONE', #2019, #13927, #8107 ) ;
#10709=CARTESIAN_POINT ( 'NONE',  ( 12.03407860800352047, 1.493611570121361698, -165.3653928882239086 ) ) ;
#10710=( BOUNDED_SURFACE ( )  B_SPLINE_SURFACE ( 3, 1, ( 
 ( #12026, #8712 ),
 ( #7387, #2535 ),
 ( #3770, #9558 ),
 ( #9637, #1296 ) ),
 .UNSPECIFIED., .F., .F., .T. ) 
 B_SPLINE_SURFACE_WITH_KNOTS ( ( 4, 4 ),
 ( 2, 2 ),
 ( 0.000000000000000000, 1.000000000000000000 ),
 ( 0.000000000000000000, 1.000000000000000000 ),
 .UNSPECIFIED. ) 
 GEOMETRIC_REPRESENTATION_ITEM ( )  RATIONAL_B_SPLINE_SURFACE ( (
 ( 1.000000000000000000, 1.000000000000000000),
 ( 0.8974116706346633165, 0.8974116706346633165),
 ( 0.8974116706346633165, 0.8974116706346633165),
 ( 1.000000000000000000, 1.000000000000000000) ) ) 
 REPRESENTATION_ITEM ( '' )  SURFACE ( )  );
#10711=CARTESIAN_POINT ( 'NONE',  ( 6.293934161496127722, 14.99999999999999822, -117.6207956168515807 ) ) ;
#10713=DIRECTION ( 'NONE',  ( -0.9997619372588931741, -0.000000000000000000, -0.02181900108494707821 ) ) ;
#10719=CARTESIAN_POINT ( 'NONE',  ( 4.351822957764132305, 0.03155975272378051116, -16.26963315870613869 ) ) ;
#10724=CARTESIAN_POINT ( 'NONE',  ( 8.807773658247754156, 15.00000000000000000, -105.8689255569352667 ) ) ;
#10726=CARTESIAN_POINT ( 'NONE',  ( -4.706582913227679299, 13.87736884190558406, -125.1575984163914086 ) ) ;
#10728=ORIENTED_EDGE ( 'NONE', *, *, #12052, .T. ) ;
#10729=EDGE_CURVE ( 'NONE', #13718, #5770, #13690, .T. ) ;
#10730=CARTESIAN_POINT ( 'NONE',  ( 4.570349143970012129, 0.7032832823769218367, 2.199267984206088489 ) ) ;
#10738=CARTESIAN_POINT ( 'NONE',  ( 10.14988979988700457, 14.51423292646842889, -106.5995613745913602 ) ) ;
#10750=CARTESIAN_POINT ( 'NONE',  ( 6.023654006863524479, 0.4287155192450040064, 0.6418499716679767486 ) ) ;
#10754=ORIENTED_EDGE ( 'NONE', *, *, #10368, .T. ) ;
#10756=CARTESIAN_POINT ( 'NONE',  ( -26.57518893882630096, 8.673617379884035472E-16, -201.5880480395080951 ) ) ;
#10760=ORIENTED_EDGE ( 'NONE', *, *, #4309, .F. ) ;
#10764=CARTESIAN_POINT ( 'NONE',  ( 15.45423724370449214, 8.673617379884033500E-16, -134.7453193863913157 ) ) ;
#10767=DIRECTION ( 'NONE',  ( 0.02058562339462769938, 0.3314513491899343522, -0.9432477061883729474 ) ) ;
#10768=DIRECTION ( 'NONE',  ( 0.9939692226109180240, -0.000000000000000000, -0.1096594022519158940 ) ) ;
#10769=CARTESIAN_POINT ( 'NONE',  ( 17.83675209366140280, 8.673617379884035472E-16, -136.7184283642698404 ) ) ;
#10772=CARTESIAN_POINT ( 'NONE',  ( 1.243260443319662123, 6.000000000000000000, -139.4020581015306846 ) ) ;
#10773=EDGE_LOOP ( 'NONE', ( #8400, #10434 ) ) ;
#10779=CARTESIAN_POINT ( 'NONE',  ( 10.22352057816269699, 15.00000000000000000, -125.5112093480189657 ) ) ;
#10787=ORIENTED_EDGE ( 'NONE', *, *, #7323, .T. ) ;
#10794=CARTESIAN_POINT ( 'NONE',  ( 29.21736815051483660, 8.773889247172311556, -44.21329492081407153 ) ) ;
#10796=CARTESIAN_POINT ( 'NONE',  ( 9.673258414158063090, 1.297355693541400345, -105.9236831072048375 ) ) ;
#10798=CARTESIAN_POINT ( 'NONE',  ( 9.044950117654433797, -4.000000000000000000, -141.4826476090360643 ) ) ;
#10801=CARTESIAN_POINT ( 'NONE',  ( 5.602568457641995181, 0.2629148106111021677, 0.1074933644148804157 ) ) ;
#10817=CARTESIAN_POINT ( 'NONE',  ( 13.13192191588670887, 4.000000000000000000, -166.1703390355876877 ) ) ;
#10818=DIRECTION ( 'NONE',  ( 0.000000000000000000, 1.000000000000000000, 0.000000000000000000 ) ) ;
#10820=CARTESIAN_POINT ( 'NONE',  ( -12.30607691012835403, 8.673617379884034486E-16, -158.4081044807556111 ) ) ;
#10825=ORIENTED_EDGE ( 'NONE', *, *, #12216, .T. ) ;
#10837=ADVANCED_FACE ( 'NONE', ( #2784 ), #1621, .T. ) ;
#10844=CARTESIAN_POINT ( 'NONE',  ( 10.46664703690589349, 5.000000000000000888, -121.2724779346276875 ) ) ;
#10845=ORIENTED_EDGE ( 'NONE', *, *, #9246, .T. ) ;
#10848=ORIENTED_EDGE ( 'NONE', *, *, #4845, .T. ) ;
#10858=AXIS2_PLACEMENT_3D ( 'NONE', #11547, #3202, #15129 ) ;
#10859=CARTESIAN_POINT ( 'NONE',  ( -6.790153584124027475, 9.999999999999998224, -124.9643354754709748 ) ) ;
#10864=LINE ( 'NONE', #9713, #2582 ) ;
#10870=CARTESIAN_POINT ( 'NONE',  ( 13.78275167297412906, 13.34157715675068623, -126.2206732457524794 ) ) ;
#10876=CARTESIAN_POINT ( 'NONE',  ( 6.288457687478774538, 8.673617379884035472E-16, -105.0111312234652985 ) ) ;
#10877=AXIS2_PLACEMENT_3D ( 'NONE', #8808, #13465, #3153 ) ;
#10880=CARTESIAN_POINT ( 'NONE',  ( 1.123679064339592859, 4.590773665857039276, -139.4222662838609210 ) ) ;
#10882=CARTESIAN_POINT ( 'NONE',  ( 6.533497844638413987, 0.7032832832067333895, 1.143078642481199614 ) ) ;
#10893=CARTESIAN_POINT ( 'NONE',  ( 9.379784756826319736, 14.94013921591925076, -106.1734080947524319 ) ) ;
#10900=CARTESIAN_POINT ( 'NONE',  ( 11.77584962622735887, 1.499941477809432211, -165.6889925597199351 ) ) ;
#10904=CARTESIAN_POINT ( 'NONE',  ( 4.999884422966211162, 0.09518442032929252949, -1.466239102699074870 ) ) ;
#10906=EDGE_LOOP ( 'NONE', ( #7523, #427, #9197, #1218 ) ) ;
#10909=EDGE_LOOP ( 'NONE', ( #13073, #4652, #15086, #1511 ) ) ;
#10911=CARTESIAN_POINT ( 'NONE',  ( -16.79479163992151669, 8.673617379884035472E-16, -186.8953034624466909 ) ) ;
#10915=ORIENTED_EDGE ( 'NONE', *, *, #9195, .F. ) ;
#10917=CARTESIAN_POINT ( 'NONE',  ( -7.687033461059511019, 1.096071398028247046, -116.8257989789358220 ) ) ;
#10926=CARTESIAN_POINT ( 'NONE',  ( -6.027592497978528918, 4.999999999999210409, -126.6584150166564768 ) ) ;
#10934=DIRECTION ( 'NONE',  ( 0.000000000000000000, 0.000000000000000000, 1.000000000000000000 ) ) ;
#10939=ORIENTED_EDGE ( 'NONE', *, *, #2304, .T. ) ;
#10941=CARTESIAN_POINT ( 'NONE',  ( -8.199037228204968386, 15.00000000003875478, -114.3845095685942255 ) ) ;
#10943=CARTESIAN_POINT ( 'NONE',  ( -9.721966606378851239, 10.00000000000000000, -116.3614657639809309 ) ) ;
#10944=CARTESIAN_POINT ( 'NONE',  ( 4.025564746441875563, 0.09586553063150847487, -1.251268110428811697 ) ) ;
#10948=CARTESIAN_POINT ( 'NONE',  ( -24.61436772009224327, 4.000000000000000000, -208.9121151917288728 ) ) ;
#10953=ADVANCED_FACE ( 'NONE', ( #9644 ), #11800, .F. ) ;
#10956=CIRCLE ( 'NONE', #14926, 16.00000000006737721 ) ;
#10959=DIRECTION ( 'NONE',  ( 0.02181900108494737658, 0.000000000000000000, -0.9997619372588931741 ) ) ;
#10960=CARTESIAN_POINT ( 'NONE',  ( 6.605878363002800846, 8.242932226922413110E-11, -105.1138548165823607 ) ) ;
#10966=CARTESIAN_POINT ( 'NONE',  ( 4.999884244121599153, 0.09548446344527571072, -1.396462267504845922 ) ) ;
#10971=DIRECTION ( 'NONE',  ( 0.1096594022519158801, 0.000000000000000000, 0.9939692226109179130 ) ) ;
#10973=CARTESIAN_POINT ( 'NONE',  ( 10.77692171413472977, 14.06121913176011162, -106.2890056980015743 ) ) ;
#10975=AXIS2_PLACEMENT_3D ( 'NONE', #14277, #1286, #5989 ) ;
#10981=CARTESIAN_POINT ( 'NONE',  ( 11.93152510496921792, 1.468982674681399425, -165.5488479599881657 ) ) ;
#10982=CARTESIAN_POINT ( 'NONE',  ( 21.72409770179331545, 4.000000000000000000, -147.6411415183954432 ) ) ;
#10983=CARTESIAN_POINT ( 'NONE',  ( -8.141143895042660006, 3.999999999999993783, -146.5791559415450536 ) ) ;
#10984=CARTESIAN_POINT ( 'NONE',  ( 5.538592533983068833, 2.409808734938486930E-16, -141.6430817385786725 ) ) ;
#10985=( BOUNDED_SURFACE ( )  B_SPLINE_SURFACE ( 3, 2, ( 
 ( #12948, #11921, #1347 ),
 ( #13092, #10542, #5890 ),
 ( #9692, #6050, #7118 ),
 ( #263, #13020, #1119 ),
 ( #2507, #185, #10769 ),
 ( #15276, #14423, #11841 ),
 ( #13176, #4896, #7285 ),
 ( #110, #6984, #9377 ),
 ( #8445, #5971, #7203 ),
 ( #2279, #4824, #14337 ),
 ( #10612, #34, #1424 ),
 ( #3739, #10692, #11998 ),
 ( #6129, #12867, #9536 ),
 ( #10844, #4974, #3822 ),
 ( #14262, #11701, #9460 ),
 ( #3661, #8362, #5820 ),
 ( #14108, #3510, #8216 ),
 ( #2355, #11769, #1187 ),
 ( #14186, #3591, #8292 ),
 ( #11008, #1723, #11077 ),
 ( #5288, #6518, #14809 ),
 ( #1652, #8523, #495 ),
 ( #2742, #654, #13417 ),
 ( #4060, #14502, #3979 ),
 ( #1577, #5213, #2662 ),
 ( #7445, #8683, #344 ),
 ( #8835, #7594, #422 ),
 ( #13257, #6365, #5132 ),
 ( #2820, #11156, #10073 ),
 ( #14735, #13562, #4134 ),
 ( #9924, #2962, #6439 ),
 ( #14657, #5358, #12162 ),
 ( #8764, #7363, #7674 ),
 ( #13494, #10000, #8599 ),
 ( #12077, #2893, #12309 ),
 ( #576, #7522, #12387 ) ),
 .UNSPECIFIED., .F., .F., .F. ) 
 B_SPLINE_SURFACE_WITH_KNOTS ( ( 4, 2, 2, 2, 2, 2, 2, 2, 2, 2, 2, 2, 2, 2, 2, 2, 2, 4 ),
 ( 3, 3 ),
 ( 0.04342216404570826971, 0.04926220847718112278, 0.05218223069291755278, 0.05510225290865397585, 0.06094229734012682892, 0.06678234177159968199, 0.06824235287946789352, 0.06970236398733611893, 0.07262238620307254200, 0.07554240841880896506, 0.07700241952667717660, 0.07846243063454538813, 0.08138245285028181120, 0.08284246395815002273, 0.08430247506601823426, 0.08576248617388644579, 0.08722249728175465733, 0.09014251949749109427 ),
 ( 0.000000000000000000, 1.000000000000000000 ),
 .UNSPECIFIED. ) 
 GEOMETRIC_REPRESENTATION_ITEM ( )  RATIONAL_B_SPLINE_SURFACE ( (
 ( 1.000000000000000000, 0.7071067811865475727, 1.000000000000000000),
 ( 1.000000000000000000, 0.7071067811865475727, 1.000000000000000000),
 ( 1.000000000000000000, 0.7071067811865475727, 1.000000000000000000),
 ( 1.000000000000000000, 0.7071067811865475727, 1.000000000000000000),
 ( 1.000000000000000000, 0.7071067811865475727, 1.000000000000000000),
 ( 1.000000000000000000, 0.7071067811865475727, 1.000000000000000000),
 ( 1.000000000000000000, 0.7071067811865475727, 1.000000000000000000),
 ( 1.000000000000000000, 0.7071067811865475727, 1.000000000000000000),
 ( 1.000000000000000000, 0.7071067811865474617, 1.000000000000000000),
 ( 1.000000000000000000, 0.7071067811865474617, 1.000000000000000000),
 ( 1.000000000000000000, 0.7071067811865475727, 1.000000000000000000),
 ( 1.000000000000000000, 0.7071067811865475727, 1.000000000000000000),
 ( 1.000000000000000000, 0.7071067811865475727, 1.000000000000000000),
 ( 1.000000000000000000, 0.7071067811865475727, 1.000000000000000000),
 ( 1.000000000000000000, 0.7071067811865475727, 1.000000000000000000),
 ( 1.000000000000000000, 0.7071067811865475727, 1.000000000000000000),
 ( 1.000000000000000000, 0.7071067811865475727, 1.000000000000000000),
 ( 1.000000000000000000, 0.7071067811865475727, 1.000000000000000000),
 ( 1.000000000000000000, 0.7071067811865474617, 1.000000000000000000),
 ( 1.000000000000000000, 0.7071067811865474617, 1.000000000000000000),
 ( 1.000000000000000000, 0.7071067811865474617, 1.000000000000000000),
 ( 1.000000000000000000, 0.7071067811865474617, 1.000000000000000000),
 ( 1.000000000000000000, 0.7071067811865474617, 1.000000000000000000),
 ( 1.000000000000000000, 0.7071067811865474617, 1.000000000000000000),
 ( 1.000000000000000000, 0.7071067811865475727, 1.000000000000000000),
 ( 1.000000000000000000, 0.7071067811865475727, 1.000000000000000000),
 ( 1.000000000000000000, 0.7071067811865475727, 1.000000000000000000),
 ( 1.000000000000000000, 0.7071067811865475727, 1.000000000000000000),
 ( 1.000000000000000000, 0.7071067811865475727, 1.000000000000000000),
 ( 1.000000000000000000, 0.7071067811865475727, 1.000000000000000000),
 ( 1.000000000000000000, 0.7071067811865475727, 1.000000000000000000),
 ( 1.000000000000000000, 0.7071067811865475727, 1.000000000000000000),
 ( 1.000000000000000000, 0.7071067811865475727, 1.000000000000000000),
 ( 1.000000000000000000, 0.7071067811865475727, 1.000000000000000000),
 ( 1.000000000000000000, 0.7071067811865482389, 1.000000000000000000),
 ( 1.000000000000000000, 0.7071067811865482389, 1.000000000000000000) ) ) 
 REPRESENTATION_ITEM ( '' )  SURFACE ( )  );
#10986=CARTESIAN_POINT ( 'NONE',  ( 5.101173563692228186, 0.1187549523756990522, -0.9191412569148569300 ) ) ;
#10995=ORIENTED_EDGE ( 'NONE', *, *, #6671, .T. ) ;
#11002=EDGE_CURVE ( 'NONE', #14278, #8296, #13326, .T. ) ;
#11007=CARTESIAN_POINT ( 'NONE',  ( -9.247150027671290573, -2.758321981116462875E-12, -118.2023151953508773 ) ) ;
#11008=CARTESIAN_POINT ( 'NONE',  ( 8.481465556139287543, 5.000000000000000888, -115.9036014638648453 ) ) ;
#11009=ORIENTED_EDGE ( 'NONE', *, *, #8440, .F. ) ;
#11010=CARTESIAN_POINT ( 'NONE',  ( 4.999999999999997335, 0.000000000000000000, -108.9020125831789727 ) ) ;
#11024=CARTESIAN_POINT ( 'NONE',  ( 1.266169042200451900, 6.000000000000000000, -139.9015330219193913 ) ) ;
#11035=CARTESIAN_POINT ( 'NONE',  ( 13.95473576866137755, 13.06343050236333170, -126.2896892777352633 ) ) ;
#11036=CIRCLE ( 'NONE', #4146, 16.00000000006737721 ) ;
#11040=CARTESIAN_POINT ( 'NONE',  ( 8.673617379884035472E-16, 9.999999999999998224, -1.663700395152567513 ) ) ;
#11055=CARTESIAN_POINT ( 'NONE',  ( 5.000000000000001776, 1.301042606982605321E-15, -45.97309604003013561 ) ) ;
#11056=CARTESIAN_POINT ( 'NONE',  ( 11.86629858958631978, 1.298284280918086342, -165.2423957076782131 ) ) ;
#11058=CARTESIAN_POINT ( 'NONE',  ( -10.47572155697075402, 1.591638444933427977E-16, -150.0444545769670412 ) ) ;
#11059=CARTESIAN_POINT ( 'NONE',  ( 0.5944212552585367293, 5.000000000000000888, -138.5540974747773930 ) ) ;
#11060=CARTESIAN_POINT ( 'NONE',  ( -24.73733098891339210, 8.673617379884034486E-16, -183.9739661531728245 ) ) ;
#11061=ORIENTED_EDGE ( 'NONE', *, *, #8440, .T. ) ;
#11068=DIRECTION ( 'NONE',  ( 0.000000000000000000, 0.000000000000000000, -1.000000000000000000 ) ) ;
#11069=ORIENTED_EDGE ( 'NONE', *, *, #6310, .F. ) ;
#11077=CARTESIAN_POINT ( 'NONE',  ( 3.551824805805253060, 8.673617379884035472E-16, -116.7502625731503656 ) ) ;
#11078=CARTESIAN_POINT ( 'NONE',  ( 7.000000000000000888, 5.000000000000000888, -1.663700395152567513 ) ) ;
#11080=ORIENTED_EDGE ( 'NONE', *, *, #6390, .T. ) ;
#11087=ORIENTED_EDGE ( 'NONE', *, *, #12052, .F. ) ;
#11090=CARTESIAN_POINT ( 'NONE',  ( 13.78275167297412906, 13.34157715675068623, -126.2206732457524794 ) ) ;
#11098=ORIENTED_EDGE ( 'NONE', *, *, #9004, .T. ) ;
#11120=AXIS2_PLACEMENT_3D ( 'NONE', #11843, #10614, #10695 ) ;
#11128=CARTESIAN_POINT ( 'NONE',  ( 11.04730217088350663, 15.00000000000000000, -107.1178495010082941 ) ) ;
#11132=CARTESIAN_POINT ( 'NONE',  ( 12.06072315356882996, 1.933739209393280589, -165.9530378701809923 ) ) ;
#11135=CARTESIAN_POINT ( 'NONE',  ( -24.39793690352481548, 0.000000000000000000, -182.5284601783003495 ) ) ;
#11136=DIRECTION ( 'NONE',  ( 0.000000000000000000, 1.000000000000000000, 0.000000000000000000 ) ) ;
#11140=VERTEX_POINT ( 'NONE', #11040 ) ;
#11147=CARTESIAN_POINT ( 'NONE',  ( -9.625715240929041627, 3.489827457201579275, -115.8367759348243595 ) ) ;
#11156=CARTESIAN_POINT ( 'NONE',  ( 8.873074003806229015, 1.073784846296689040E-12, -110.5883967389756748 ) ) ;
#11160=FACE_OUTER_BOUND ( 'NONE', #3620, .T. ) ;
#11161=CARTESIAN_POINT ( 'NONE',  ( 4.413686865555820127, 15.00000000000000178, -104.6754972201258482 ) ) ;
#11165=ORIENTED_EDGE ( 'NONE', *, *, #1678, .F. ) ;
#11169=CARTESIAN_POINT ( 'NONE',  ( 9.969654309237004242, 12.69562645089776964, -44.87941232917236789 ) ) ;
#11171=CARTESIAN_POINT ( 'NONE',  ( 17.50071171097425804, 8.749999999999998224, -91.70093451412481045 ) ) ;
#11182=DIRECTION ( 'NONE',  ( 0.000000000000000000, 1.000000000000000000, 0.000000000000000000 ) ) ;
#11190=EDGE_LOOP ( 'NONE', ( #14031, #6530, #8128, #4958 ) ) ;
#11193=CARTESIAN_POINT ( 'NONE',  ( -4.234402844927150689, 15.00000000000000000, -117.4888040839639558 ) ) ;
#11197=CARTESIAN_POINT ( 'NONE',  ( -0.1117941955214300648, 10.00000000000000000, -102.1231258608400907 ) ) ;
#11204=VERTEX_POINT ( 'NONE', #4166 ) ;
#11205=CARTESIAN_POINT ( 'NONE',  ( -9.385448347264267355, 9.999999999999998224, -115.3551636530117150 ) ) ;
#11210=ADVANCED_FACE ( 'NONE', ( #7628 ), #8868, .F. ) ;
#11213=CARTESIAN_POINT ( 'NONE',  ( -20.78318744499695470, 8.673617379884035472E-16, -172.3918248695773059 ) ) ;
#11218=FACE_OUTER_BOUND ( 'NONE', #5361, .T. ) ;
#11223=CARTESIAN_POINT ( 'NONE',  ( -8.455319114079472342, 1.782382842817059165, -116.6570696633463911 ) ) ;
#11230=EDGE_CURVE ( 'NONE', #3740, #5461, #13121, .T. ) ;
#11232=B_SPLINE_CURVE_WITH_KNOTS ( 'NONE', 3,
 ( #7903, #10458, #11539, #954 ),
 .UNSPECIFIED., .F., .F.,
 ( 4, 4 ),
 ( -1.414214726962510347E-05, 0.001035133531573338228 ),
 .UNSPECIFIED. ) ;
#11235=DIRECTION ( 'NONE',  ( 0.02181900108494732801, 0.000000000000000000, -0.9997619372588931741 ) ) ;
#11237=VERTEX_POINT ( 'NONE', #7788 ) ;
#11238=CARTESIAN_POINT ( 'NONE',  ( 9.952382861741629227, 4.874414676631592336, -43.73669136194838813 ) ) ;
#11239=CARTESIAN_POINT ( 'NONE',  ( 11.46158717457445242, 12.50000000000000355, -122.9370801587496231 ) ) ;
#11247=CARTESIAN_POINT ( 'NONE',  ( -25.42939282183900573, 4.000000000000000000, -209.0516719515502473 ) ) ;
#11248=CARTESIAN_POINT ( 'NONE',  ( -9.131312970615338642, 12.51400246205168010, -116.0049100415184569 ) ) ;
#11250=CARTESIAN_POINT ( 'NONE',  ( 12.15266112769998053, 15.00000000000000000, -123.9192486815589263 ) ) ;
#11251=CARTESIAN_POINT ( 'NONE',  ( 27.51230736755065109, 4.535074869370507855, -137.3927180564188006 ) ) ;
#11254=CARTESIAN_POINT ( 'NONE',  ( -29.11373319368141921, 4.000000000000000000, -181.2633039353972322 ) ) ;
#11256=EDGE_LOOP ( 'NONE', ( #458, #1102, #10995, #9049, #10825, #14021 ) ) ;
#11259=CARTESIAN_POINT ( 'NONE',  ( 9.971950858281140029, 8.773889247172311556, -44.63331069169930032 ) ) ;
#11263=CARTESIAN_POINT ( 'NONE',  ( 11.02460460396801345, 5.000000000000000888, -122.2267226321878866 ) ) ;
#11264=CARTESIAN_POINT ( 'NONE',  ( 0.5944212552585367293, 0.000000000000000000, -138.5540974747773930 ) ) ;
#11271=CARTESIAN_POINT ( 'NONE',  ( 10.73540465342505357, 13.79079921804019548, -106.9347929316625425 ) ) ;
#11272=EDGE_CURVE ( 'NONE', #788, #13477, #6002, .T. ) ;
#11280=CARTESIAN_POINT ( 'NONE',  ( 4.673610763312950667, 0.0002987076048428271343, -16.05876724900730679 ) ) ;
#11282=CARTESIAN_POINT ( 'NONE',  ( 9.861753912003623057, 1.663174471683243949, -106.5437946333974679 ) ) ;
#11284=CARTESIAN_POINT ( 'NONE',  ( -22.38002629026897594, -1.081729916803953434E-12, -166.3206558604766201 ) ) ;
#11292=DIRECTION ( 'NONE',  ( -0.000000000000000000, -1.000000000000000000, -0.000000000000000000 ) ) ;
#11297=( BOUNDED_SURFACE ( )  B_SPLINE_SURFACE ( 3, 2, ( 
 ( #3520, #10553, #12803 ),
 ( #7215, #9391, #13030 ),
 ( #9471, #14197, #12958 ),
 ( #46, #14119, #11711 ),
 ( #4755, #11782, #2208 ),
 ( #8302, #11852, #9319 ),
 ( #8228, #1277, #6916 ),
 ( #10704, #11636, #120 ),
 ( #1054, #3439, #4834 ),
 ( #9546, #8150, #2365 ),
 ( #15219, #7062, #14272 ),
 ( #2291, #8375, #6995 ),
 ( #1129, #14437, #14351 ),
 ( #13430, #13188, #1942 ),
 ( #3914, #3751, #14875 ),
 ( #8535, #6581, #7373 ),
 ( #6302, #10941, #6656 ),
 ( #2754, #11369, #14515 ) ),
 .UNSPECIFIED., .F., .F., .T. ) 
 B_SPLINE_SURFACE_WITH_KNOTS ( ( 4, 2, 2, 2, 2, 2, 2, 2, 4 ),
 ( 3, 3 ),
 ( -2.168404344971008868E-19, 0.002802366342598247659, 0.005604732685196495319, 0.007005915856495618932, 0.008407099027794743412, 0.01120946537039299064, 0.01401183171299123786, 0.01681419805558948682, 0.02241893074078598128 ),
 ( 0.000000000000000000, 1.000000000000000000 ),
 .UNSPECIFIED. ) 
 GEOMETRIC_REPRESENTATION_ITEM ( )  RATIONAL_B_SPLINE_SURFACE ( (
 ( 1.000000000000000000, 0.7071067811865475727, 1.000000000000000000),
 ( 1.000000000000000000, 0.7071067811865475727, 1.000000000000000000),
 ( 1.000000000000000000, 0.7071067811865475727, 1.000000000000000000),
 ( 1.000000000000000000, 0.7071067811865475727, 1.000000000000000000),
 ( 1.000000000000000000, 0.7071067811865475727, 1.000000000000000000),
 ( 1.000000000000000000, 0.7071067811865475727, 1.000000000000000000),
 ( 1.000000000000000000, 0.7071067811865474617, 1.000000000000000000),
 ( 1.000000000000000000, 0.7071067811865474617, 1.000000000000000000),
 ( 1.000000000000000000, 0.7071067811865475727, 1.000000000000000000),
 ( 1.000000000000000000, 0.7071067811865475727, 1.000000000000000000),
 ( 1.000000000000000000, 0.7071067811865475727, 1.000000000000000000),
 ( 1.000000000000000000, 0.7071067811865475727, 1.000000000000000000),
 ( 1.000000000000000000, 0.7071067811865475727, 1.000000000000000000),
 ( 1.000000000000000000, 0.7071067811865475727, 1.000000000000000000),
 ( 1.000000000000000000, 0.7071067811865475727, 1.000000000000000000),
 ( 1.000000000000000000, 0.7071067811865475727, 1.000000000000000000),
 ( 1.000000000000000000, 0.7071067811865474617, 1.000000000000000000),
 ( 1.000000000000000000, 0.7071067811865474617, 1.000000000000000000) ) ) 
 REPRESENTATION_ITEM ( '' )  SURFACE ( )  );
#11302=DIRECTION ( 'NONE',  ( -0.02181900108494707127, -0.000000000000000000, 0.9997619372588931741 ) ) ;
#11307=ORIENTED_EDGE ( 'NONE', *, *, #11565, .T. ) ;
#11309=CARTESIAN_POINT ( 'NONE',  ( -5.613243360039387397, 3.999999999999999112, -181.6031318735493869 ) ) ;
#11316=EDGE_CURVE ( 'NONE', #8744, #3728, #7241, .T. ) ;
#11317=ADVANCED_FACE ( 'NONE', ( #12656 ), #2071, .F. ) ;
#11318=FACE_OUTER_BOUND ( 'NONE', #14171, .T. ) ;
#11320=CARTESIAN_POINT ( 'NONE',  ( -4.890501715614027134, 14.99999999916422233, -117.3116236002413899 ) ) ;
#11322=CARTESIAN_POINT ( 'NONE',  ( 8.507048280578556998, 15.00000000000000000, -111.8750672986241881 ) ) ;
#11323=CARTESIAN_POINT ( 'NONE',  ( -9.681086997240701209, 10.70057783228466519, -116.3713800322179850 ) ) ;
#11328=CARTESIAN_POINT ( 'NONE',  ( -29.51097267919375611, 4.000000000000000888, -182.9257734226692378 ) ) ;
#11330=ORIENTED_EDGE ( 'NONE', *, *, #3374, .F. ) ;
#11331=CARTESIAN_POINT ( 'NONE',  ( -8.648486276335452416, 12.61601666265212529, -115.6868502166757224 ) ) ;
#11339=ORIENTED_EDGE ( 'NONE', *, *, #412, .F. ) ;
#11352=AXIS2_PLACEMENT_3D ( 'NONE', #8602, #1726, #14505 ) ;
#11356=CARTESIAN_POINT ( 'NONE',  ( -18.78509308054654170, 8.673617379884035472E-16, -168.2639965131413931 ) ) ;
#11357=CARTESIAN_POINT ( 'NONE',  ( 11.61481609544922655, 1.294168654864739310, -165.5398345278520651 ) ) ;
#11361=EDGE_LOOP ( 'NONE', ( #5733, #3264, #9177, #704, #14325, #5955 ) ) ;
#11366=CARTESIAN_POINT ( 'NONE',  ( 26.73766085848597740, 6.000000000000000000, -138.7442440334353080 ) ) ;
#11369=CARTESIAN_POINT ( 'NONE',  ( -9.476787056091273698, 15.00000000000000000, -115.4301398046334839 ) ) ;
#11370=CARTESIAN_POINT ( 'NONE',  ( -6.992168204854784186, 5.000000000000000888, -113.2636094675863063 ) ) ;
#11377=AXIS2_PLACEMENT_3D ( 'NONE', #6441, #349, #5062 ) ;
#11379=CIRCLE ( 'NONE', #520, 0.9999999999999731326 ) ;
#11381=EDGE_CURVE ( 'NONE', #673, #10375, #8493, .T. ) ;
#11386=EDGE_LOOP ( 'NONE', ( #4178, #10331 ) ) ;
#11387=CARTESIAN_POINT ( 'NONE',  ( 8.949251933909494028, 11.66085798210991697, 2.227471517426460768 ) ) ;
#11398=CARTESIAN_POINT ( 'NONE',  ( -24.64653759749926465, 4.000000000000000000, -208.9889250379274301 ) ) ;
#11399=DIRECTION ( 'NONE',  ( 0.9997619372588931741, 0.000000000000000000, 0.02181900108494707474 ) ) ;
#11401=ADVANCED_FACE ( 'NONE', ( #9329 ), #13114, .T. ) ;
#11402=CARTESIAN_POINT ( 'NONE',  ( 9.875992363362541937, 15.00000000000000000, -120.1725736632532318 ) ) ;
#11405=FACE_OUTER_BOUND ( 'NONE', #1328, .T. ) ;
#11408=CARTESIAN_POINT ( 'NONE',  ( -21.09070732192979492, 4.000000000000000000, -162.5659300234576676 ) ) ;
#11415=CARTESIAN_POINT ( 'NONE',  ( -25.45939401113465550, 0.6794050853239335108, -205.0195236891385377 ) ) ;
#11420=EDGE_CURVE ( 'NONE', #14600, #2663, #6926, .T. ) ;
#11423=CARTESIAN_POINT ( 'NONE',  ( -2.802205527622656955, 9.999999999999996447, -108.2424688405072288 ) ) ;
#11427=CARTESIAN_POINT ( 'NONE',  ( -9.347739544678665524, 4.300886386704505959, -115.3723878648253844 ) ) ;
#11428=CARTESIAN_POINT ( 'NONE',  ( -9.525540565743067845, 3.627568584023658005, -116.4087343257889131 ) ) ;
#11435=CARTESIAN_POINT ( 'NONE',  ( 13.78275167297412906, 6.000000000000000000, -126.2206732457524794 ) ) ;
#11437=CARTESIAN_POINT ( 'NONE',  ( -25.68866767343566693, 0.000000000000000000, -190.1221061183514962 ) ) ;
#11441=ORIENTED_EDGE ( 'NONE', *, *, #5172, .T. ) ;
#11444=CARTESIAN_POINT ( 'NONE',  ( 8.935898484867617952, 10.32733530284803436, 2.839335920898358623 ) ) ;
#11445=CARTESIAN_POINT ( 'NONE',  ( -0.8896971555284219901, 1.636639605872992197E-12, -104.6801027822252053 ) ) ;
#11448=AXIS2_PLACEMENT_3D ( 'NONE', #2668, #5219, #14344 ) ;
#11449=B_SPLINE_CURVE_WITH_KNOTS ( 'NONE', 3,
 ( #2565, #6107, #8579, #2876, #14400, #1473, #7576, #3955, #13313, #10820, #12139, #9668, #2798, #237, #2717, #3798, #8503, #13238, #2639, #7343, #12056, #11060, #8663, #5036, #1556, #14482, #7501, #12221, #1632, #477, #6347, #12370 ),
 .UNSPECIFIED., .F., .F.,
 ( 4, 2, 2, 2, 2, 2, 2, 2, 2, 2, 2, 2, 2, 2, 2, 4 ),
 ( 8.673617379884033931E-18, 0.004084815278923605887, 0.008169630557847203101, 0.01633926111569434375, 0.02042407639461791755, 0.02450889167354148787, 0.03267852223138869444, 0.04084815278923590448, 0.04289056042869772434, 0.04493296806815954419, 0.04901778334708325330, 0.05310259862600696934, 0.05718741390493067844, 0.06127222918385440142, 0.06331463682331625598, 0.06535704446277812441 ),
 .UNSPECIFIED. ) ;
#11450=CARTESIAN_POINT ( 'NONE',  ( 22.05157068915105611, -2.335861096501437513E-12, -147.3126055969182460 ) ) ;
#11463=CARTESIAN_POINT ( 'NONE',  ( -19.02652486928245068, 4.000000000000000000, -198.3523810112471040 ) ) ;
#11470=CIRCLE ( 'NONE', #4802, 2.000000000000001776 ) ;
#11474=CARTESIAN_POINT ( 'NONE',  ( -7.369174163213084938, 14.17702046568131635, -116.5771123024624103 ) ) ;
#11476=CARTESIAN_POINT ( 'NONE',  ( 9.667889503862193479, 15.00000000000093614, -108.9228968456952344 ) ) ;
#11480=CARTESIAN_POINT ( 'NONE',  ( 26.39556552446789794, 2.215704797542763949, -137.6676921094336876 ) ) ;
#11487=( BOUNDED_SURFACE ( )  B_SPLINE_SURFACE ( 3, 2, ( 
 ( #14173, #3646, #8349 ),
 ( #8278, #10377, #18 ),
 ( #4734, #2114, #3414 ),
 ( #6820, #3576, #6890 ),
 ( #951, #5656, #3343 ),
 ( #4654, #11610, #8202 ),
 ( #11827, #4507, #8124 ),
 ( #9215, #13006, #2266 ),
 ( #8051, #12779, #6971 ),
 ( #1029, #5735, #3962 ),
 ( #10911, #13399, #6276 ),
 ( #3804, #8668, #7507 ),
 ( #4041, #4960, #7185 ),
 ( #9675, #7349, #482 ),
 ( #9592, #3724, #2803 ),
 ( #10756, #8429, #14644 ),
 ( #2723, #13162, #12226 ),
 ( #12145, #14320, #1637 ),
 ( #6352, #1562, #6114 ),
 ( #13075, #5116, #13318 ) ),
 .UNSPECIFIED., .F., .F., .F. ) 
 B_SPLINE_SURFACE_WITH_KNOTS ( ( 4, 2, 2, 2, 2, 2, 2, 2, 2, 4 ),
 ( 3, 3 ),
 ( 0.04111226598309934699, 0.04870987420823701119, 0.05630748243337466846, 0.07150269888364998994, 0.07530150299621882204, 0.07910030710878765414, 0.08669791533392531835, 0.09429552355906298255, 0.09809432767163181466, 0.1018931317842006329 ),
 ( 0.000000000000000000, 0.8628733549542494385 ),
 .UNSPECIFIED. ) 
 GEOMETRIC_REPRESENTATION_ITEM ( )  RATIONAL_B_SPLINE_SURFACE ( (
 ( 1.000000000000000000, 0.7472702456390871717, 0.9306880333625028312),
 ( 1.000000000000000000, 0.7472702456390871717, 0.9306880333625028312),
 ( 1.000000000000000000, 0.7472702456390871717, 0.9306880333625028312),
 ( 1.000000000000000000, 0.7472702456390871717, 0.9306880333625028312),
 ( 1.000000000000000000, 0.7472702456390871717, 0.9306880333625028312),
 ( 1.000000000000000000, 0.7472702456390871717, 0.9306880333625028312),
 ( 1.000000000000000000, 0.7472702456390872827, 0.9306880333625028312),
 ( 1.000000000000000000, 0.7472702456390872827, 0.9306880333625028312),
 ( 1.000000000000000000, 0.7472702456390861725, 0.9306880333625024981),
 ( 1.000000000000000000, 0.7472702456390861725, 0.9306880333625024981),
 ( 1.000000000000000000, 0.7472702456390871717, 0.9306880333625028312),
 ( 1.000000000000000000, 0.7472702456390871717, 0.9306880333625028312),
 ( 1.000000000000000000, 0.7472702456390862835, 0.9306880333625024981),
 ( 1.000000000000000000, 0.7472702456390862835, 0.9306880333625024981),
 ( 1.000000000000000000, 0.7472702456390871717, 0.9306880333625028312),
 ( 1.000000000000000000, 0.7472702456390871717, 0.9306880333625028312),
 ( 1.000000000000000000, 0.7472702456390863945, 0.9306880333625026092),
 ( 1.000000000000000000, 0.7472702456390863945, 0.9306880333625026092),
 ( 1.000000000000000000, 0.7472702456390870607, 0.9306880333625027202),
 ( 1.000000000000000000, 0.7472702456390870607, 0.9306880333625027202) ) ) 
 REPRESENTATION_ITEM ( '' )  SURFACE ( )  );
#11489=ORIENTED_EDGE ( 'NONE', *, *, #534, .F. ) ;
#11494=CARTESIAN_POINT ( 'NONE',  ( -25.25620482601053141, 6.788815924111790495E-10, -199.8982617752898818 ) ) ;
#11497=CARTESIAN_POINT ( 'NONE',  ( 9.381253443180193941, 5.000000000000000888, -119.0445822199432797 ) ) ;
#11510=CARTESIAN_POINT ( 'NONE',  ( 11.18769411126905666, 13.31779969966692789, -106.3797690317953766 ) ) ;
#11512=LINE ( 'NONE', #11435, #9497 ) ;
#11514=CARTESIAN_POINT ( 'NONE',  ( -29.80626542450986349, 3.999999999999753975, -200.5060461161095020 ) ) ;
#11520=CARTESIAN_POINT ( 'NONE',  ( -25.70420084062632426, 0.8205903998713498515, -205.0550399661483993 ) ) ;
#11521=CARTESIAN_POINT ( 'NONE',  ( 8.887137379133079662, 12.34685406312035560, 5.073603994963653996 ) ) ;
#11522=CARTESIAN_POINT ( 'NONE',  ( 0.2132689653687949716, 1.734723475976807094E-15, -112.6263465441575136 ) ) ;
#11530=CYLINDRICAL_SURFACE ( 'NONE', #677, 16.00000000006737721 ) ;
#11533=CARTESIAN_POINT ( 'NONE',  ( 16.50094977371536231, 8.749999999999998224, -91.72275351520976017 ) ) ;
#11539=CARTESIAN_POINT ( 'NONE',  ( 26.66376411343011910, 4.332989673203356595, -138.8074532758291468 ) ) ;
#11542=CARTESIAN_POINT ( 'NONE',  ( -2.802205527622656955, 5.000000000000000888, -108.2424688405072430 ) ) ;
#11546=CARTESIAN_POINT ( 'NONE',  ( 8.821381957849935063, 12.49999999999999822, -110.6350233298706485 ) ) ;
#11547=CARTESIAN_POINT ( 'NONE',  ( 5.228075279701640099, 1.000000000000000000, -165.7939279834373849 ) ) ;
#11549=CARTESIAN_POINT ( 'NONE',  ( 26.76147460282112789, 3.476039578919685624, -138.2546491778831239 ) ) ;
#11551=EDGE_LOOP ( 'NONE', ( #13080, #4524, #14429 ) ) ;
#11561=CARTESIAN_POINT ( 'NONE',  ( -25.02281643586231752, 2.918594768585438537, -209.0154590114276232 ) ) ;
#11565=EDGE_CURVE ( 'NONE', #5152, #5770, #9248, .T. ) ;
#11570=CARTESIAN_POINT ( 'NONE',  ( 11.04730217088347999, 12.66744776516167192, -107.1178495010082514 ) ) ;
#11581=EDGE_CURVE ( 'NONE', #7480, #1063, #12196, .T. ) ;
#11582=CARTESIAN_POINT ( 'NONE',  ( -28.31848045150696436, 3.999999999999600320, -204.6799762813750476 ) ) ;
#11584=EDGE_CURVE ( 'NONE', #2594, #6618, #12770, .T. ) ;
#11590=CARTESIAN_POINT ( 'NONE',  ( -25.28306627899824122, 0.01437449745307941250, -199.9124629347120106 ) ) ;
#11592=CARTESIAN_POINT ( 'NONE',  ( 5.612199600609121930, -5.296307347064899472E-31, -165.5340050431785528 ) ) ;
#11595=CARTESIAN_POINT ( 'NONE',  ( 20.84482309861272498, 5.000000000000000888, -149.6621754078162212 ) ) ;
#11606=CARTESIAN_POINT ( 'NONE',  ( 9.044950117654433797, 0.000000000000000000, -141.4826476090360643 ) ) ;
#11607=ORIENTED_EDGE ( 'NONE', *, *, #7064, .T. ) ;
#11610=CARTESIAN_POINT ( 'NONE',  ( -2.831701609851823065, 0.000000000000000000, -177.7686553741204136 ) ) ;
#11616=TOROIDAL_SURFACE ( 'NONE', #12107, 4.000000000000001776, 1.000000000000000000 ) ;
#11623=FACE_OUTER_BOUND ( 'NONE', #9141, .T. ) ;
#11624=CARTESIAN_POINT ( 'NONE',  ( -8.265142125449935762, 13.41314848964355022, -116.6996609440855650 ) ) ;
#11636=CARTESIAN_POINT ( 'NONE',  ( -1.334601435092752419, 15.00000000000000000, -105.6792246796778869 ) ) ;
#11642=CARTESIAN_POINT ( 'NONE',  ( -25.68188187296914293, 1.246347066919430979, -206.1291706975209763 ) ) ;
#11649=CARTESIAN_POINT ( 'NONE',  ( -5.581362024073983186, 9.999999999999998224, -111.7646305296507165 ) ) ;
#11652=EDGE_CURVE ( 'NONE', #14341, #6054, #10864, .T. ) ;
#11661=CARTESIAN_POINT ( 'NONE',  ( -23.71521175673118975, 8.673617379884035472E-16, -202.9409338110467047 ) ) ;
#11670=CARTESIAN_POINT ( 'NONE',  ( 8.966408348210480383, 12.25254480171083671, 1.441352577737632590 ) ) ;
#11671=CARTESIAN_POINT ( 'NONE',  ( -2.424117393066262061, 1.734723475976807094E-15, -107.6599666632789649 ) ) ;
#11673=EDGE_CURVE ( 'NONE', #191, #10108, #2843, .T. ) ;
#11674=CARTESIAN_POINT ( 'NONE',  ( 15.16156648836315490, 5.000000000000000888, -161.5519024490516529 ) ) ;
#11690=VECTOR ( 'NONE', #9414, 1000.000000000000114 ) ;
#11698=AXIS2_PLACEMENT_3D ( 'NONE', #4244, #5615, #12576 ) ;
#11701=CARTESIAN_POINT ( 'NONE',  ( 10.27130088868191038, 1.514087034083648316E-12, -120.9123952260012089 ) ) ;
#11707=DIRECTION ( 'NONE',  ( -0.9997619372588931741, -0.000000000000000000, -0.02181900108494707474 ) ) ;
#11711=CARTESIAN_POINT ( 'NONE',  ( -0.3214635616123167061, 9.999999999999998224, -103.0394908280460271 ) ) ;
#11714=CARTESIAN_POINT ( 'NONE',  ( -24.96153981867218974, 3.396440209233427154, -209.3551883656818404 ) ) ;
#11725=CARTESIAN_POINT ( 'NONE',  ( -7.195211678798691501, 5.000000000000000888, -124.1091578989210547 ) ) ;
#11730=EDGE_LOOP ( 'NONE', ( #8717, #7837, #4673, #12276 ) ) ;
#11731=CARTESIAN_POINT ( 'NONE',  ( 8.274725579668297470, 2.404323337855486908, 5.020935352624569248 ) ) ;
#11734=ADVANCED_FACE ( 'NONE', ( #3841 ), #14361, .T. ) ;
#11739=CARTESIAN_POINT ( 'NONE',  ( 8.934261526981043033, 14.51811739220718422, 2.914342479709274958 ) ) ;
#11742=CARTESIAN_POINT ( 'NONE',  ( 1.624578347342658713, 8.673617379884035472E-16, -110.6108487083152454 ) ) ;
#11745=CARTESIAN_POINT ( 'NONE',  ( 84.71830840217509717, 4.000000000000000000, -172.4480499191751619 ) ) ;
#11751=ORIENTED_EDGE ( 'NONE', *, *, #3062, .F. ) ;
#11754=ORIENTED_EDGE ( 'NONE', *, *, #11967, .F. ) ;
#11762=CARTESIAN_POINT ( 'NONE',  ( -4.122964195042672308, 5.000000000000000888, -110.0534507760547882 ) ) ;
#11764=CARTESIAN_POINT ( 'NONE',  ( 18.09872976117486942, 8.673617379884035472E-16, -136.9430002941252269 ) ) ;
#11768=DIRECTION ( 'NONE',  ( 0.9989498407774362043, 0.000000000000000000, 0.04581719776170026931 ) ) ;
#11769=CARTESIAN_POINT ( 'NONE',  ( 8.895820146902094550, 1.734723475976807094E-15, -117.6809082908677908 ) ) ;
#11770=ORIENTED_EDGE ( 'NONE', *, *, #6874, .F. ) ;
#11778=ADVANCED_FACE ( 'NONE', ( #14678 ), #5078, .T. ) ;
#11782=CARTESIAN_POINT ( 'NONE',  ( -0.5126277339646087006, 15.00000000000246203, -103.6859198938586815 ) ) ;
#11787=CARTESIAN_POINT ( 'NONE',  ( 6.049572344775472565, 15.00000000000000000, -111.4205638705285679 ) ) ;
#11791=B_SPLINE_CURVE_WITH_KNOTS ( 'NONE', 3,
 ( #2611, #13448, #11035, #6153, #14371, #2852 ),
 .UNSPECIFIED., .F., .F.,
 ( 4, 2, 4 ),
 ( 0.000000000000000000, 0.0004983545201280861151, 0.0009967090402561722302 ),
 .UNSPECIFIED. ) ;
#11794=CARTESIAN_POINT ( 'NONE',  ( 1.077968782234968836, 4.793811891163896277, -139.4304863127936471 ) ) ;
#11798=CARTESIAN_POINT ( 'NONE',  ( 9.390800893974766694, 1.188659780534533139, -106.3264951435503036 ) ) ;
#11800=CYLINDRICAL_SURFACE ( 'NONE', #9971, 3.500000000000003109 ) ;
#11801=CARTESIAN_POINT ( 'NONE',  ( 1.004809442601927394, 5.000000000000000888, -139.4752805618705622 ) ) ;
#11803=CARTESIAN_POINT ( 'NONE',  ( 8.840216610704089817, 3.990476221256948453, 2.799461104694893621 ) ) ;
#11815=FACE_OUTER_BOUND ( 'NONE', #12262, .T. ) ;
#11818=CARTESIAN_POINT ( 'NONE',  ( 9.068716941525979180, 1.734723475976807094E-15, -163.1923081219560174 ) ) ;
#11823=ORIENTED_EDGE ( 'NONE', *, *, #6650, .F. ) ;
#11827=CARTESIAN_POINT ( 'NONE',  ( -9.251449178678159413, 1.734723475976807094E-15, -178.3019022727991398 ) ) ;
#11832=VERTEX_POINT ( 'NONE', #33 ) ;
#11834=ADVANCED_FACE ( 'NONE', ( #11623 ), #1118, .F. ) ;
#11837=LINE ( 'NONE', #7358, #3213 ) ;
#11838=EDGE_CURVE ( 'NONE', #13643, #2207, #5535, .T. ) ;
#11840=AXIS2_PLACEMENT_3D ( 'NONE', #12769, #14957, #4419 ) ;
#11841=CARTESIAN_POINT ( 'NONE',  ( 16.30648644992872676, 8.673617379884035472E-16, -135.4745789036516612 ) ) ;
#11843=CARTESIAN_POINT ( 'NONE',  ( 5.000000000000000888, 9.999999999999998224, -108.9020125831789727 ) ) ;
#11846=ORIENTED_EDGE ( 'NONE', *, *, #1019, .F. ) ;
#11852=CARTESIAN_POINT ( 'NONE',  ( -0.8896971555268431420, 14.99999999999876898, -104.6801027822232157 ) ) ;
#11857=CARTESIAN_POINT ( 'NONE',  ( -24.93348466747179870, 3.665517550122363577, -209.5032877194438470 ) ) ;
#11858=CARTESIAN_POINT ( 'NONE',  ( 10.00452473099216988, 0.1207859802015546630, -163.8779166317577278 ) ) ;
#11862=VECTOR ( 'NONE', #8023, 1000.000000000000000 ) ;
#11866=CARTESIAN_POINT ( 'NONE',  ( -1.639428572435056353, 14.99999999999999822, -124.2686519725904333 ) ) ;
#11874=CARTESIAN_POINT ( 'NONE',  ( 9.149651848773698859, 0.9864195427603029698, -106.2170607917651211 ) ) ;
#11881=CARTESIAN_POINT ( 'NONE',  ( 5.705671018141757145, 2.650800484686449909, 4.619709739133793569 ) ) ;
#11893=CARTESIAN_POINT ( 'NONE',  ( 2.860422134859789800, 8.673617379884037444E-16, -108.4900984580837644 ) ) ;
#11898=CARTESIAN_POINT ( 'NONE',  ( -9.721966606378851239, 15.00000000000000000, -116.3614657639809309 ) ) ;
#11900=CARTESIAN_POINT ( 'NONE',  ( -12.74549125309000885, 3.999999999999993783, -151.2947804600756001 ) ) ;
#11904=VERTEX_POINT ( 'NONE', #10393 ) ;
#11912=ORIENTED_EDGE ( 'NONE', *, *, #8436, .F. ) ;
#11913=TOROIDAL_SURFACE ( 'NONE', #15153, 1.250000000000002220, 1.750000000000000000 ) ;
#11920=DIRECTION ( 'NONE',  ( 0.000000000000000000, 0.000000000000000000, 1.000000000000000000 ) ) ;
#11921=CARTESIAN_POINT ( 'NONE',  ( 26.93149290009008823, 8.673617379884035472E-16, -137.0203993314533761 ) ) ;
#11924=PLANE ( 'NONE',  #12859 ) ;
#11927=EDGE_CURVE ( 'NONE', #8744, #6645, #853, .T. ) ;
#11929=CARTESIAN_POINT ( 'NONE',  ( -29.51225541722604007, 4.000000000000000888, -201.5661097356285723 ) ) ;
#11934=CARTESIAN_POINT ( 'NONE',  ( 6.409599520805702610, 14.96732179972273435, 0.9270135685219680344 ) ) ;
#11937=AXIS2_PLACEMENT_3D ( 'NONE', #14795, #6577, #481 ) ;
#11947=CARTESIAN_POINT ( 'NONE',  ( 1.077968782234507428, 5.000000000000000888, -139.4304863127929082 ) ) ;
#11949=CARTESIAN_POINT ( 'NONE',  ( 5.000000000000000000, 5.000000000000000888, -1.663700395152567513 ) ) ;
#11952=CARTESIAN_POINT ( 'NONE',  ( 8.755026559824571564, 0.6305609032749204257, -105.6652816485397040 ) ) ;
#11954=CARTESIAN_POINT ( 'NONE',  ( -4.030963197337185555, 14.27759960331617428, -125.2321359900997209 ) ) ;
#11958=CARTESIAN_POINT ( 'NONE',  ( 4.226910153394439540, 0.3260126676757187369, 0.9376784990094754191 ) ) ;
#11963=ADVANCED_FACE ( 'NONE', ( #2354 ), #13019, .F. ) ;
#11966=( BOUNDED_SURFACE ( )  B_SPLINE_SURFACE ( 3, 2, ( 
 ( #4460, #6778, #6703 ),
 ( #5539, #11494, #10325 ),
 ( #5836, #7934, #13902 ),
 ( #4682, #5686, #9397 ),
 ( #10257, #10556, #2211 ),
 ( #10490, #2294, #14988 ),
 ( #15064, #11415, #3370 ),
 ( #8233, #9251, #15222 ),
 ( #1058, #13975, #8082 ),
 ( #11642, #15289, #12806 ),
 ( #833, #1986, #6920 ),
 ( #5766, #9093, #14046 ),
 ( #4386, #13814, #8155 ),
 ( #4612, #14124, #3215 ),
 ( #6999, #10411, #5612 ),
 ( #15145, #12653, #3301 ),
 ( #2068, #9322, #9173 ),
 ( #977, #8009, #12733 ),
 ( #2145, #11561, #12884 ),
 ( #6848, #11714, #1134 ),
 ( #14517, #11857, #3837 ),
 ( #361, #1360, #8380 ) ),
 .UNSPECIFIED., .F., .F., .T. ) 
 B_SPLINE_SURFACE_WITH_KNOTS ( ( 4, 2, 2, 2, 2, 2, 2, 2, 2, 2, 4 ),
 ( 3, 3 ),
 ( -1.623076171293996825E-05, 0.002723859379327837719, 0.005463949520368615448, 0.006148972055628809663, 0.006833994590889003878, 0.007519017126149198094, 0.008204039661409392309, 0.008889062196669586524, 0.009574084731929780739, 0.01025910726718997495, 0.01094412980245017090 ),
 ( 0.000000000000000000, 1.000000000000000000 ),
 .UNSPECIFIED. ) 
 GEOMETRIC_REPRESENTATION_ITEM ( )  RATIONAL_B_SPLINE_SURFACE ( (
 ( 1.000000000000000000, 1.000000000000000000, 1.000000000000000000),
 ( 1.000000000000000000, 0.9999677357533394151, 1.000000000000000000),
 ( 1.000000000000000000, 0.9926659029119584421, 1.000000000000000000),
 ( 1.000000000000000000, 0.9597381185227591427, 1.000000000000000000),
 ( 1.000000000000000000, 0.9342244066884717313, 1.000000000000000000),
 ( 1.000000000000000000, 0.8868441346594281294, 1.000000000000000000),
 ( 1.000000000000000000, 0.8765818554801813045, 1.000000000000000000),
 ( 1.000000000000000000, 0.8543202666023007597, 1.000000000000000000),
 ( 1.000000000000000000, 0.8422878763855655704, 1.000000000000000000),
 ( 1.000000000000000000, 0.8166978392028928502, 1.000000000000000000),
 ( 1.000000000000000000, 0.8031073211395015621, 1.000000000000000000),
 ( 1.000000000000000000, 0.7743109652644618590, 1.000000000000000000),
 ( 1.000000000000000000, 0.7590349308573662857, 1.000000000000000000),
 ( 1.000000000000000000, 0.7272728521985072359, 1.000000000000000000),
 ( 1.000000000000000000, 0.7108161654301946575, 1.000000000000000000),
 ( 1.000000000000000000, 0.6771951971006066051, 1.000000000000000000),
 ( 1.000000000000000000, 0.6600161975495444366, 1.000000000000000000),
 ( 1.000000000000000000, 0.6258845079443411397, 1.000000000000000000),
 ( 1.000000000000000000, 0.6093097763769845798, 1.000000000000000000),
 ( 1.000000000000000000, 0.5793944113054434464, 1.000000000000000000),
 ( 1.000000000000000000, 0.5659315413484863333, 1.000000000000000000),
 ( 1.000000000000000000, 0.5562760308710636981, 1.000000000000000000) ) ) 
 REPRESENTATION_ITEM ( '' )  SURFACE ( )  );
#11967=EDGE_CURVE ( 'NONE', #5038, #881, #8748, .T. ) ;
#11969=ADVANCED_FACE ( 'NONE', ( #7117 ), #13487, .T. ) ;
#11978=LINE ( 'NONE', #11898, #719 ) ;
#11979=CARTESIAN_POINT ( 'NONE',  ( 1.004809442601847236, 5.000000000000000888, -139.4752805618705906 ) ) ;
#11984=VERTEX_POINT ( 'NONE', #6364 ) ;
#11994=CARTESIAN_POINT ( 'NONE',  ( 3.379596559112451271, 8.673617379884035472E-16, -115.6190070853288034 ) ) ;
#11997=CARTESIAN_POINT ( 'NONE',  ( 1.320501113854922082, -4.336808689942017736E-15, -137.8664870916820178 ) ) ;
#11998=CARTESIAN_POINT ( 'NONE',  ( 6.844193222559625589, 8.673617379884035472E-16, -124.9748991231763000 ) ) ;
#12000=LINE ( 'NONE', #11010, #6431 ) ;
#12004=CARTESIAN_POINT ( 'NONE',  ( 26.98741591943780094, 4.264362126257767116, -138.2255432259009922 ) ) ;
#12009=CARTESIAN_POINT ( 'NONE',  ( -24.07555247732078030, 3.209883240645346926E-32, -197.1572433827812176 ) ) ;
#12014=EDGE_CURVE ( 'NONE', #8296, #8528, #7593, .T. ) ;
#12023=DIRECTION ( 'NONE',  ( -0.9997619372588932851, 0.000000000000000000, -0.02181900108494707474 ) ) ;
#12026=CARTESIAN_POINT ( 'NONE',  ( -9.385448347264265578, 9.999999999999998224, -115.3551636530117150 ) ) ;
#12028=FACE_OUTER_BOUND ( 'NONE', #12831, .T. ) ;
#12032=DIRECTION ( 'NONE',  ( -0.000000000000000000, 1.000000000000000000, -0.000000000000000000 ) ) ;
#12034=CARTESIAN_POINT ( 'NONE',  ( 6.896101684162133871, 0.9384448392688442553, 1.465219231324311977 ) ) ;
#12048=CARTESIAN_POINT ( 'NONE',  ( 10.67218363251896207, 0.3802680776948408337, -164.3671655685305950 ) ) ;
#12052=EDGE_CURVE ( 'NONE', #587, #5152, #1722, .T. ) ;
#12053=CARTESIAN_POINT ( 'NONE',  ( -11.06538882243261135, 3.999999999999993783, -149.4796096102432159 ) ) ;
#12056=CARTESIAN_POINT ( 'NONE',  ( -24.07048164010645408, 8.673617379884033500E-16, -181.3206119412710962 ) ) ;
#12065=CARTESIAN_POINT ( 'NONE',  ( 4.950900406836922230, 0.000000000000000000, -134.4284351762048573 ) ) ;
#12067=CARTESIAN_POINT ( 'NONE',  ( -7.978007822721722597, 1.532620112711841509, -115.9805901612375578 ) ) ;
#12074=CARTESIAN_POINT ( 'NONE',  ( -5.418138540701907147, 10.00000000000000355, -127.8817495432483469 ) ) ;
#12076=CARTESIAN_POINT ( 'NONE',  ( -3.672164062342282875, 4.999999999996045830, -131.0905698958435437 ) ) ;
#12077=CARTESIAN_POINT ( 'NONE',  ( 10.69730027793196747, 5.000000000000000888, -107.4734661196136472 ) ) ;
#12078=ORIENTED_EDGE ( 'NONE', *, *, #665, .F. ) ;
#12082=ORIENTED_EDGE ( 'NONE', *, *, #8941, .T. ) ;
#12083=CARTESIAN_POINT ( 'NONE',  ( 25.55817180536042343, 1.743203967168683866, -138.4078944009487486 ) ) ;
#12087=ORIENTED_EDGE ( 'NONE', *, *, #6609, .T. ) ;
#12103=AXIS2_PLACEMENT_3D ( 'NONE', #3794, #1165, #8417 ) ;
#12107=AXIS2_PLACEMENT_3D ( 'NONE', #265, #8447, #3981 ) ;
#12109=FACE_OUTER_BOUND ( 'NONE', #12245, .T. ) ;
#12112=CARTESIAN_POINT ( 'NONE',  ( 6.288457687480498493, 8.673617379884035472E-16, -105.0111312234657817 ) ) ;
#12118=CARTESIAN_POINT ( 'NONE',  ( 5.960046513698709525, 0.2792070234823527675, 2.322492007399493463 ) ) ;
#12122=CIRCLE ( 'NONE', #5465, 3.500000000000003109 ) ;
#12127=CARTESIAN_POINT ( 'NONE',  ( 10.30451295169211434, 14.51423292640433438, -106.1859832732645117 ) ) ;
#12137=DIRECTION ( 'NONE',  ( 0.000000000000000000, 1.000000000000000000, 0.000000000000000000 ) ) ;
#12138=DIRECTION ( 'NONE',  ( 0.9989498407774362043, 0.000000000000000000, 0.04581719776170026931 ) ) ;
#12139=CARTESIAN_POINT ( 'NONE',  ( -13.13002412793078477, 8.673617379884033500E-16, -159.4945871395674146 ) ) ;
#12142=VERTEX_POINT ( 'NONE', #10294 ) ;
#12144=CYLINDRICAL_SURFACE ( 'NONE', #7753, 0.4999999999999726885 ) ;
#12145=CARTESIAN_POINT ( 'NONE',  ( -28.26194796053519909, 8.673617379884035472E-16, -205.0068360181388130 ) ) ;
#12150=EDGE_CURVE ( 'NONE', #3728, #13676, #14883, .T. ) ;
#12158=CARTESIAN_POINT ( 'NONE',  ( -8.249568998231312733, 10.00000000000325606, -121.3053947661622090 ) ) ;
#12161=CARTESIAN_POINT ( 'NONE',  ( -2.971798371524276394, 8.673617379884035472E-16, -121.1412956273195078 ) ) ;
#12162=CARTESIAN_POINT ( 'NONE',  ( 5.201313589241833846, 0.000000000000000000, -106.6450149762817716 ) ) ;
#12163=ORIENTED_EDGE ( 'NONE', *, *, #839, .F. ) ;
#12170=VECTOR ( 'NONE', #10333, 1000.000000000000114 ) ;
#12173=EDGE_LOOP ( 'NONE', ( #10476, #11069, #383, #11087 ) ) ;
#12176=CARTESIAN_POINT ( 'NONE',  ( 12.51467606204868055, 14.43297906408152542, -125.8675091911941593 ) ) ;
#12179=VECTOR ( 'NONE', #13345, 1000.000000000000000 ) ;
#12187=AXIS2_PLACEMENT_3D ( 'NONE', #5536, #10255, #3138 ) ;
#12196=CIRCLE ( 'NONE', #10975, 3.000000000000011990 ) ;
#12197=CARTESIAN_POINT ( 'NONE',  ( 9.044950117654433797, 4.000000000000000000, -141.4826476090360643 ) ) ;
#12199=CARTESIAN_POINT ( 'NONE',  ( 7.867579639100686251, 1.761783548405282618, 4.595106300331015525 ) ) ;
#12214=CARTESIAN_POINT ( 'NONE',  ( 12.03942984618162626, 1.499941477806701062, -165.3693158247522206 ) ) ;
#12216=EDGE_CURVE ( 'NONE', #6769, #6645, #14198, .T. ) ;
#12219=CARTESIAN_POINT ( 'NONE',  ( -11.03583607032509306, 8.673617379884034486E-16, -150.6360199482514304 ) ) ;
#12221=CARTESIAN_POINT ( 'NONE',  ( -25.66265810730576291, 8.673617379884035472E-16, -195.5605329225483331 ) ) ;
#12226=CARTESIAN_POINT ( 'NONE',  ( -22.78288617575325148, 3.999999999999503064, -204.9228294213145887 ) ) ;
#12229=CYLINDRICAL_SURFACE ( 'NONE', #13192, 6.999999999999999112 ) ;
#12230=ORIENTED_EDGE ( 'NONE', *, *, #10183, .F. ) ;
#12231=CARTESIAN_POINT ( 'NONE',  ( -9.513824166154098094, 3.588159064070329585, -116.4115394435343802 ) ) ;
#12240=CARTESIAN_POINT ( 'NONE',  ( 3.725927156403949780, -8.673617379884035472E-16, -133.0470886511550930 ) ) ;
#12243=FACE_OUTER_BOUND ( 'NONE', #6824, .T. ) ;
#12245=EDGE_LOOP ( 'NONE', ( #7017, #5237, #7037, #7207 ) ) ;
#12252=CARTESIAN_POINT ( 'NONE',  ( -25.11906781955738310, 0.000000000000000000, -198.9681998140721078 ) ) ;
#12256=CARTESIAN_POINT ( 'NONE',  ( -4.234402844927157794, 15.00000000000000000, -117.4888040839639558 ) ) ;
#12259=CARTESIAN_POINT ( 'NONE',  ( -24.65477654877672720, 3.556530958261907127, -208.7318555042168668 ) ) ;
#12262=EDGE_LOOP ( 'NONE', ( #14070, #8556, #11441, #14941 ) ) ;
#12276=ORIENTED_EDGE ( 'NONE', *, *, #1963, .F. ) ;
#12281=CARTESIAN_POINT ( 'NONE',  ( 5.570677809474934072, 7.976916236371252995E-16, -141.9062416701571863 ) ) ;
#12286=CARTESIAN_POINT ( 'NONE',  ( -8.256868333794509240, 1.840915534571258450, -115.8592241392985045 ) ) ;
#12290=CARTESIAN_POINT ( 'NONE',  ( 11.61838904370529235, 1.298284280916856659, -165.5431421116371382 ) ) ;
#12292=CARTESIAN_POINT ( 'NONE',  ( -25.90868989253521448, 3.999999999998550937, -171.8621034424046172 ) ) ;
#12294=LINE ( 'NONE', #9753, #13841 ) ;
#12309=CARTESIAN_POINT ( 'NONE',  ( 6.913513084311236234, 8.673617379884035472E-16, -104.1914153500056841 ) ) ;
#12313=CARTESIAN_POINT ( 'NONE',  ( 10.96001082017541250, 5.773884165125716450, -44.27064591564993634 ) ) ;
#12314=CARTESIAN_POINT ( 'NONE',  ( 24.37641090407976208, 0.8825362985825043749, -138.5554241525009047 ) ) ;
#12322=CARTESIAN_POINT ( 'NONE',  ( 9.976640234167886589, 12.67883206573310062, -45.13187004413220649 ) ) ;
#12325=CARTESIAN_POINT ( 'NONE',  ( -9.721966606232506081, 10.36359568089365979, -116.3614657645881323 ) ) ;
#12327=CARTESIAN_POINT ( 'NONE',  ( 4.544676675852343806, 6.000000000000000000, -126.1782412829290934 ) ) ;
#12329=ORIENTED_EDGE ( 'NONE', *, *, #8163, .F. ) ;
#12340=CARTESIAN_POINT ( 'NONE',  ( 11.14414536921188592, 3.613765879947322013, -106.7459647845625597 ) ) ;
#12343=CARTESIAN_POINT ( 'NONE',  ( -16.51872302133460124, 0.000000000000000000, -108.9020125831789727 ) ) ;
#12346=ORIENTED_EDGE ( 'NONE', *, *, #13384, .F. ) ;
#12348=CARTESIAN_POINT ( 'NONE',  ( 1.320501113854927633, 6.000000000000000000, -137.8664870916819893 ) ) ;
#12352=CIRCLE ( 'NONE', #14608, 0.4999999999999726885 ) ;
#12353=CARTESIAN_POINT ( 'NONE',  ( 11.04869015131055399, 13.64261357365585070, -106.3489331929075519 ) ) ;
#12356=VECTOR ( 'NONE', #5281, 1000.000000000000114 ) ;
#12357=EDGE_CURVE ( 'NONE', #13477, #12980, #8130, .T. ) ;
#12363=CARTESIAN_POINT ( 'NONE',  ( 9.044950117654433797, 0.000000000000000000, -141.4826476090360643 ) ) ;
#12367=CARTESIAN_POINT ( 'NONE',  ( -9.094017300323571362, 8.673617379884035472E-16, -154.5612483065650054 ) ) ;
#12368=CARTESIAN_POINT ( 'NONE',  ( 5.824043469730588285, 0.03107126107963375031, -140.0877662325354436 ) ) ;
#12370=CARTESIAN_POINT ( 'NONE',  ( -25.11906781955738310, 0.000000000000000000, -198.9681998140721078 ) ) ;
#12374=CARTESIAN_POINT ( 'NONE',  ( 10.25880996898554542, 1.911678198002125573, -106.0927282050041640 ) ) ;
#12376=CARTESIAN_POINT ( 'NONE',  ( 26.58801926426210116, 6.000000000000000000, -139.0072983920785532 ) ) ;
#12387=CARTESIAN_POINT ( 'NONE',  ( 7.608837862079233183, 8.673617379884035472E-16, -103.4801572790971846 ) ) ;
#12401=CARTESIAN_POINT ( 'NONE',  ( 13.68910679601487246, 13.48624612131195555, -126.1906338203120157 ) ) ;
#12402=CARTESIAN_POINT ( 'NONE',  ( 5.942951940282705792, 3.392001843152369300, 5.005362280283235599 ) ) ;
#12405=CARTESIAN_POINT ( 'NONE',  ( 8.821381957564753407, 15.00000000000000000, -110.6350233297983436 ) ) ;
#12408=EDGE_CURVE ( 'NONE', #1063, #7480, #2846, .T. ) ;
#12410=CARTESIAN_POINT ( 'NONE',  ( -0.2993152428870710091, 4.000000000000000000, -140.3884260891180418 ) ) ;
#12412=ORIENTED_EDGE ( 'NONE', *, *, #1019, .T. ) ;
#12418=CARTESIAN_POINT ( 'NONE',  ( -6.288157641191917335, 6.000000000000000000, -124.9981450708252595 ) ) ;
#12420=CARTESIAN_POINT ( 'NONE',  ( 9.801515392239481983, 5.000000000000000000, -108.6954945137553494 ) ) ;
#12421=DIRECTION ( 'NONE',  ( -0.02181900108494696719, 0.000000000000000000, 0.9997619372588931741 ) ) ;
#12422=APPLICATION_CONTEXT ( 'configuration controlled 3d designs of mechanical parts and assemblies' ) ;
#12440=AXIS2_PLACEMENT_3D ( 'NONE', #14000, #6951, #9199 ) ;
#12442=AXIS2_PLACEMENT_3D ( 'NONE', #5567, #13772, #7813 ) ;
#12444=LINE ( 'NONE', #14939, #1751 ) ;
#12447=CARTESIAN_POINT ( 'NONE',  ( -26.92103615529513760, -3.820545969703583956E-12, -176.7902989741743625 ) ) ;
#12448=CARTESIAN_POINT ( 'NONE',  ( 12.18103126625983812, 2.151585356863087384, -166.0646392245766663 ) ) ;
#12449=EDGE_CURVE ( 'NONE', #2826, #5201, #11470, .T. ) ;
#12451=ADVANCED_FACE ( 'NONE', ( #6269 ), #12886, .F. ) ;
#12453=EDGE_LOOP ( 'NONE', ( #2972, #10033, #2821, #8856, #11846 ) ) ;
#12456=CARTESIAN_POINT ( 'NONE',  ( 11.28543669177601494, 4.325399326098414043, -106.3987031433302377 ) ) ;
#12460=CARTESIAN_POINT ( 'NONE',  ( 25.81993756863266398, 1.397373862231122054E-11, -140.3392227824482177 ) ) ;
#12469=CARTESIAN_POINT ( 'NONE',  ( 10.95232128968187091, 11.68831177261878373, -43.87656800833052984 ) ) ;
#12470=ORIENTED_EDGE ( 'NONE', *, *, #2236, .T. ) ;
#12472=CARTESIAN_POINT ( 'NONE',  ( -23.68884049351463972, 3.999999999999999112, -206.7022962662250904 ) ) ;
#12479=CARTESIAN_POINT ( 'NONE',  ( 10.04079546391108124, 11.77387431541663076, -44.82333900155087747 ) ) ;
#12480=CARTESIAN_POINT ( 'NONE',  ( 10.56990542994451410, 15.00000000000000355, -125.5400580087990505 ) ) ;
#12482=CARTESIAN_POINT ( 'NONE',  ( -8.786545012121958820, 12.38245414974118930, -115.6253344005690877 ) ) ;
#12484=CARTESIAN_POINT ( 'NONE',  ( 8.308576004177995245, 15.00000000000000000, -113.5907613746703220 ) ) ;
#12485=CARTESIAN_POINT ( 'NONE',  ( 24.26046657763140857, 0.6944454239927166928, -138.1842452301896742 ) ) ;
#12493=DIRECTION ( 'NONE',  ( 0.000000000000000000, 0.000000000000000000, 1.000000000000000000 ) ) ;
#12504=CARTESIAN_POINT ( 'NONE',  ( 8.807773658247754156, 15.00000000000000000, -105.8689255569352667 ) ) ;
#12509=ADVANCED_FACE ( 'NONE', ( #165 ), #6648, .T. ) ;
#12517=CARTESIAN_POINT ( 'NONE',  ( 10.05869691007584521, 1.912799100046207235, -106.6366767720914623 ) ) ;
#12518=ORIENTED_EDGE ( 'NONE', *, *, #7782, .F. ) ;
#12519=CARTESIAN_POINT ( 'NONE',  ( -25.76048682929828004, 8.673617379884035472E-16, -193.9633714502515716 ) ) ;
#12525=CARTESIAN_POINT ( 'NONE',  ( 20.87131526946579285, 0.000000000000000000, -138.9752963459259547 ) ) ;
#12527=CARTESIAN_POINT ( 'NONE',  ( 1.243260443319662123, 4.000000000000000000, -139.4020581015306846 ) ) ;
#12528=CARTESIAN_POINT ( 'NONE',  ( -0.3214635616143260433, 5.000000000000000888, -103.0394908280558042 ) ) ;
#12530=DESIGN_CONTEXT ( 'detailed design', #12731, 'design' ) ;
#12532=CARTESIAN_POINT ( 'NONE',  ( 22.79641070782754042, 8.673617379884035472E-16, -135.5653294067645049 ) ) ;
#12536=ADVANCED_FACE ( 'NONE', ( #4482 ), #10304, .T. ) ;
#12537=DIRECTION ( 'NONE',  ( -0.02181900108494732801, 0.000000000000000000, 0.9997619372588931741 ) ) ;
#12544=B_SPLINE_CURVE_WITH_KNOTS ( 'NONE', 3,
 ( #15004, #9109, #13832, #2084, #11510, #926, #5626, #8551, #7314, #13287, #6155, #2690, #138, #64, #1376, #10724 ),
 .UNSPECIFIED., .F., .F.,
 ( 4, 2, 2, 2, 2, 2, 2, 4 ),
 ( 5.561946577567963334E-17, 0.0005014808200499583889, 0.001002961640099861050, 0.001504442460149763927, 0.002005923280199666588, 0.002507404100249569466, 0.003008884920299472344, 0.004011846560399272461 ),
 .UNSPECIFIED. ) ;
#12546=CARTESIAN_POINT ( 'NONE',  ( 8.966402098224863337, 12.25239120670691761, 1.441638956463255017 ) ) ;
#12547=CARTESIAN_POINT ( 'NONE',  ( 4.018210755790066813, 15.00000000000000178, -105.8455740756232473 ) ) ;
#12555=EDGE_CURVE ( 'NONE', #14224, #12872, #8129, .T. ) ;
#12557=CARTESIAN_POINT ( 'NONE',  ( -24.90112075662176139, 4.000000000000000888, -209.1976611213315493 ) ) ;
#12558=CARTESIAN_POINT ( 'NONE',  ( -6.385995564644680655, 14.56253871825853530, -116.6487767744769712 ) ) ;
#12560=CARTESIAN_POINT ( 'NONE',  ( 8.330271663372849744, 12.49999999999999822, -113.1592731357591788 ) ) ;
#12562=CARTESIAN_POINT ( 'NONE',  ( 22.25559703696422531, 0.08303441296203807609, -138.6572023805229605 ) ) ;
#12566=( BOUNDED_SURFACE ( )  B_SPLINE_SURFACE ( 3, 2, ( 
 ( #3811, #5963, #4886 ),
 ( #5882, #7277, #4814 ),
 ( #8207, #9598, #13081 ),
 ( #2496, #4965, #23 ),
 ( #4738, #14411, #9681 ),
 ( #14326, #2652, #7193 ),
 ( #9450, #7354, #10917 ),
 ( #12067, #6200, #5048 ),
 ( #3582, #13012, #11223 ),
 ( #8753, #14493, #1713 ),
 ( #13484, #1797, #14799 ),
 ( #13405, #8590, #2809 ),
 ( #1567, #11147, #12231 ),
 ( #1642, #7740, #6357 ),
 ( #566, #5276, #9987 ),
 ( #6582, #5497, #4493 ) ),
 .UNSPECIFIED., .F., .F., .F. ) 
 B_SPLINE_SURFACE_WITH_KNOTS ( ( 4, 2, 2, 2, 2, 2, 2, 4 ),
 ( 3, 3 ),
 ( -1.334638064063315278E-05, 0.001685485362004415181, 0.002534901233326939361, 0.003384317104649463542, 0.004233732975971987722, 0.005083148847294511469, 0.005932564718617035215, 0.006781980589939559829 ),
 ( 0.000000000000000000, 1.000000000000000000 ),
 .UNSPECIFIED. ) 
 GEOMETRIC_REPRESENTATION_ITEM ( )  RATIONAL_B_SPLINE_SURFACE ( (
 ( 1.000000000000000000, 1.000000000000000000, 1.000000000000000000),
 ( 1.000000000000000000, 0.9999849372739773035, 1.000000000000000000),
 ( 1.000000000000000000, 0.9937682810189589766, 1.000000000000000000),
 ( 1.000000000000000000, 0.9761755817002144564, 1.000000000000000000),
 ( 1.000000000000000000, 0.9688601978537728643, 1.000000000000000000),
 ( 1.000000000000000000, 0.9524575494629793360, 1.000000000000000000),
 ( 1.000000000000000000, 0.9433181971022835954, 1.000000000000000000),
 ( 1.000000000000000000, 0.9239129119538113111, 1.000000000000000000),
 ( 1.000000000000000000, 0.9135210720623375691, 1.000000000000000000),
 ( 1.000000000000000000, 0.8936014670382675940, 1.000000000000000000),
 ( 1.000000000000000000, 0.8840084896210586018, 1.000000000000000000),
 ( 1.000000000000000000, 0.8670987394481856070, 1.000000000000000000),
 ( 1.000000000000000000, 0.8600561105956274766, 1.000000000000000000),
 ( 1.000000000000000000, 0.8503557397563155096, 1.000000000000000000),
 ( 1.000000000000000000, 0.8476417977138580584, 1.000000000000000000),
 ( 1.000000000000000000, 0.8476602389438061547, 1.000000000000000000) ) ) 
 REPRESENTATION_ITEM ( '' )  SURFACE ( )  );
#12568=ORIENTED_EDGE ( 'NONE', *, *, #140, .T. ) ;
#12569=CARTESIAN_POINT ( 'NONE',  ( -9.347739544678658419, 10.69911361329557486, -115.3723878648253702 ) ) ;
#12572=LINE ( 'NONE', #10101, #15316 ) ;
#12573=CARTESIAN_POINT ( 'NONE',  ( -3.762890103924136032, -1.083335593717819817E-30, -119.0450417366422755 ) ) ;
#12576=DIRECTION ( 'NONE',  ( 0.000000000000000000, 0.000000000000000000, 1.000000000000000000 ) ) ;
#12580=CIRCLE ( 'NONE', #7886, 2.500000000000000000 ) ;
#12582=CARTESIAN_POINT ( 'NONE',  ( -7.128555860240338049, 10.00000000000000000, -113.3867792963409471 ) ) ;
#12586=CARTESIAN_POINT ( 'NONE',  ( -8.031487215395415546, 1.587880349828493465, -115.9574366882091141 ) ) ;
#12595=CARTESIAN_POINT ( 'NONE',  ( -29.76123416327401472, 2.196423649378339976E-12, -189.7991270702629834 ) ) ;
#12599=ADVANCED_FACE ( 'NONE', ( #11405 ), #1221, .T. ) ;
#12601=ORIENTED_EDGE ( 'NONE', *, *, #11927, .T. ) ;
#12607=CARTESIAN_POINT ( 'NONE',  ( 8.878875710790671505, 11.38038423757601691, 5.452159434543733418 ) ) ;
#12608=CARTESIAN_POINT ( 'NONE',  ( 1.814459646442446061, 1.734723475976807094E-15, -110.3167319592340618 ) ) ;
#12610=CARTESIAN_POINT ( 'NONE',  ( 17.61566365793502698, 8.673617379884035472E-16, -145.0049062421806809 ) ) ;
#12617=CARTESIAN_POINT ( 'NONE',  ( 0.5944212552585367293, 4.000000000000000000, -138.5540974747773930 ) ) ;
#12620=CARTESIAN_POINT ( 'NONE',  ( 11.44399236068192671, 6.000000000000000000, -138.9341978221715976 ) ) ;
#12625=CARTESIAN_POINT ( 'NONE',  ( -24.61436772009224327, 4.000000000000000000, -208.9121151917288728 ) ) ;
#12630=ORIENTED_EDGE ( 'NONE', *, *, #3712, .F. ) ;
#12633=CARTESIAN_POINT ( 'NONE',  ( 10.95559245021438599, 11.70596818966908614, -43.87284672483780668 ) ) ;
#12635=CARTESIAN_POINT ( 'NONE',  ( -7.490165920336979255, 13.90392860188294577, -116.1895725676876481 ) ) ;
#12637=CIRCLE ( 'NONE', #8687, 3.000000000000005329 ) ;
#12638=CARTESIAN_POINT ( 'NONE',  ( 6.055984099849963442, 15.00000000000000000, -111.3700911571895347 ) ) ;
#12641=CARTESIAN_POINT ( 'NONE',  ( 25.46731144555170090, 1.659276419459761565, -138.4193424522641180 ) ) ;
#12653=CARTESIAN_POINT ( 'NONE',  ( -25.15392993456217852, 2.155093112943019751, -208.2125851377665242 ) ) ;
#12654=DIRECTION ( 'NONE',  ( 0.02181900108494707821, 0.000000000000000000, -0.9997619372588931741 ) ) ;
#12656=FACE_OUTER_BOUND ( 'NONE', #13439, .T. ) ;
#12660=DIRECTION ( 'NONE',  ( 0.000000000000000000, 0.000000000000000000, 1.000000000000000000 ) ) ;
#12661=CIRCLE ( 'NONE', #5751, 1.000000000000000888 ) ;
#12665=CARTESIAN_POINT ( 'NONE',  ( -5.599106598294000925, 0.1460420930272973150, -117.2453520682029762 ) ) ;
#12670=DIRECTION ( 'NONE',  ( 0.000000000000000000, 0.000000000000000000, 1.000000000000000000 ) ) ;
#12673=CARTESIAN_POINT ( 'NONE',  ( -29.01353551585973634, -1.091297840028627083E-12, -200.3078382963151398 ) ) ;
#12683=CARTESIAN_POINT ( 'NONE',  ( -3.768042520817070251, 5.000000000000000888, -109.5986228335811035 ) ) ;
#12693=CARTESIAN_POINT ( 'NONE',  ( 26.33833810415152143, 3.213311421644162724, -137.0172291339391961 ) ) ;
#12696=AXIS2_PLACEMENT_3D ( 'NONE', #10560, #15296, #3528 ) ;
#12709=CARTESIAN_POINT ( 'NONE',  ( -5.581362024073984962, 5.000000000000000888, -111.7646305296507165 ) ) ;
#12711=ADVANCED_FACE ( 'NONE', ( #2426 ), #11924, .F. ) ;
#12712=( LENGTH_UNIT ( ) NAMED_UNIT ( * ) SI_UNIT ( .MILLI., .METRE. ) );
#12715=CARTESIAN_POINT ( 'NONE',  ( 8.347943498206106483, 15.00000000000093614, -114.9028610997532382 ) ) ;
#12719=CARTESIAN_POINT ( 'NONE',  ( 21.58150087226717417, 1.257146728175858478E-15, -138.8928492084092454 ) ) ;
#12721=EDGE_LOOP ( 'NONE', ( #10303, #7087, #13627, #4713 ) ) ;
#12722=ORIENTED_EDGE ( 'NONE', *, *, #1088, .T. ) ;
#12729=CARTESIAN_POINT ( 'NONE',  ( -9.097645849187712130, 11.69616909788754811, -115.4858344565724906 ) ) ;
#12731=APPLICATION_CONTEXT ( 'configuration controlled 3d designs of mechanical parts and assemblies' ) ;
#12733=CARTESIAN_POINT ( 'NONE',  ( -24.72728013139317227, 3.011500147175719011, -208.3923052574565986 ) ) ;
#12734=ADVANCED_FACE ( 'NONE', ( #7121 ), #7054, .T. ) ;
#12739=CARTESIAN_POINT ( 'NONE',  ( 16.72930956226772992, 5.000000000000001776, -129.1652552991705249 ) ) ;
#12754=ORIENTED_EDGE ( 'NONE', *, *, #9666, .T. ) ;
#12755=CARTESIAN_POINT ( 'NONE',  ( 8.831196406527940468, 4.174746519320978067, 5.585086345355044557 ) ) ;
#12756=CARTESIAN_POINT ( 'NONE',  ( 9.499156868358349826, 0.02433756043618112708, -163.5877548174848357 ) ) ;
#12759=ORIENTED_EDGE ( 'NONE', *, *, #2781, .T. ) ;
#12761=CARTESIAN_POINT ( 'NONE',  ( -25.67126045880329244, 1.369234990023930010, -206.3875020893990211 ) ) ;
#12764=CARTESIAN_POINT ( 'NONE',  ( 0.000000000000000000, 5.000000000000000888, -101.1952717268990369 ) ) ;
#12769=CARTESIAN_POINT ( 'NONE',  ( 29.19009439915865656, 8.773889247172311556, -42.96359249924044832 ) ) ;
#12770=B_SPLINE_CURVE_WITH_KNOTS ( 'NONE', 3,
 ( #5151, #8784, #1522, #13275, #7613, #2603, #7465, #6311, #6233, #8703, #366, #7303, #1670, #285, #1441, #12259, #5077, #10948 ),
 .UNSPECIFIED., .F., .F.,
 ( 4, 2, 2, 2, 2, 2, 2, 2, 4 ),
 ( -1.667338569123524410E-05, 0.002831516953986391253, 0.005679707293664017567, 0.007103802463502830074, 0.007815850048422199464, 0.008527897633341566253, 0.009951992803180237379, 0.01066404038809959896, 0.01137608797301896055 ),
 .UNSPECIFIED. ) ;
#12779=CARTESIAN_POINT ( 'NONE',  ( -11.26695648740382971, 1.032514652406677416E-11, -186.6451589813374881 ) ) ;
#12783=EDGE_LOOP ( 'NONE', ( #2681, #7698, #12163, #9362, #5709, #9703, #6975, #13915, #3959, #3643 ) ) ;
#12789=CARTESIAN_POINT ( 'NONE',  ( 8.961626804292983195, 15.00000000000000000, -105.6777632968436222 ) ) ;
#12790=CARTESIAN_POINT ( 'NONE',  ( -9.108720832937514444, 12.32676068985322715, -116.5073105006875807 ) ) ;
#12794=EDGE_CURVE ( 'NONE', #14561, #12868, #12000, .T. ) ;
#12795=ORIENTED_EDGE ( 'NONE', *, *, #7064, .F. ) ;
#12803=CARTESIAN_POINT ( 'NONE',  ( 8.673617379884035472E-16, 9.999999999999998224, -100.6237003951525537 ) ) ;
#12806=CARTESIAN_POINT ( 'NONE',  ( -25.10588189737052645, 1.246347066797810932, -206.0870911841997497 ) ) ;
#12807=DIRECTION ( 'NONE',  ( 0.9997619372588931741, 0.000000000000000000, 0.02181900108494707474 ) ) ;
#12815=CARTESIAN_POINT ( 'NONE',  ( 10.49113263805003982, 14.16484045804872061, -106.7936367227621730 ) ) ;
#12816=ADVANCED_FACE ( 'NONE', ( #5214 ), #11616, .F. ) ;
#12820=LINE ( 'NONE', #13987, #11862 ) ;
#12827=CARTESIAN_POINT ( 'NONE',  ( -28.49016282317369431, 1.093032563504590562E-12, -202.0976090756554697 ) ) ;
#12831=EDGE_LOOP ( 'NONE', ( #2914, #10024, #15240 ) ) ;
#12836=CARTESIAN_POINT ( 'NONE',  ( 8.949236727333637731, 11.66009932332230647, 2.228168293400664357 ) ) ;
#12837=CARTESIAN_POINT ( 'NONE',  ( -1.586855474365579610, 8.673617379884035472E-16, -114.8059160835070429 ) ) ;
#12840=CARTESIAN_POINT ( 'NONE',  ( 4.624333745513746763, 8.673617379884034486E-16, -103.8844720882033812 ) ) ;
#12844=CARTESIAN_POINT ( 'NONE',  ( 26.47489239128982419, 3.551309734749960256, -136.9665625843822170 ) ) ;
#12850=CARTESIAN_POINT ( 'NONE',  ( -3.545188519422978413, 10.00000000000000000, -132.7285785787237558 ) ) ;
#12853=CARTESIAN_POINT ( 'NONE',  ( 9.899772909143624844, 12.50000000000000355, -108.5406452818202894 ) ) ;
#12859=AXIS2_PLACEMENT_3D ( 'NONE', #9379, #8140, #14032 ) ;
#12860=TOROIDAL_SURFACE ( 'NONE', #1991, 2.000000000000009326, 1.000000000000000000 ) ;
#12866=CARTESIAN_POINT ( 'NONE',  ( 10.54086443169194531, 14.99999999999764988, -107.6778029778606225 ) ) ;
#12867=CARTESIAN_POINT ( 'NONE',  ( 10.87631271606135819, 1.290928924814131768E-12, -121.9832090784181275 ) ) ;
#12868=VERTEX_POINT ( 'NONE', #7524 ) ;
#12871=TOROIDAL_SURFACE ( 'NONE', #6932, 2.000000000000000000, 5.000000000000000000 ) ;
#12872=VERTEX_POINT ( 'NONE', #4976 ) ;
#12875=DIRECTION ( 'NONE',  ( 0.02181900108494732801, 0.000000000000000000, -0.9997619372588931741 ) ) ;
#12884=CARTESIAN_POINT ( 'NONE',  ( -24.69689105420345143, 3.216921006046159270, -208.5365831628258206 ) ) ;
#12885=CARTESIAN_POINT ( 'NONE',  ( 2.869574948089113509, -4.336808689942016947E-15, -131.9358007310388530 ) ) ;
#12886=( BOUNDED_SURFACE ( )  B_SPLINE_SURFACE ( 3, 1, ( 
 ( #3713, #11979 ),
 ( #6345, #13153 ),
 ( #14397, #6026 ),
 ( #3952, #13067 ) ),
 .UNSPECIFIED., .F., .F., .T. ) 
 B_SPLINE_SURFACE_WITH_KNOTS ( ( 4, 4 ),
 ( 2, 2 ),
 ( 0.000000000000000000, 1.000000000000000000 ),
 ( 0.000000000000000000, 1.000000000000000000 ),
 .UNSPECIFIED. ) 
 GEOMETRIC_REPRESENTATION_ITEM ( )  RATIONAL_B_SPLINE_SURFACE ( (
 ( 1.000000000000000000, 1.000000000000000000),
 ( 0.9999990904828330862, 0.9999990904828330862),
 ( 0.9999990904828330862, 0.9999990904828330862),
 ( 1.000000000000000000, 1.000000000000000000) ) ) 
 REPRESENTATION_ITEM ( '' )  SURFACE ( )  );
#12889=ADVANCED_FACE ( 'NONE', ( #12243 ), #1003, .T. ) ;
#12903=CARTESIAN_POINT ( 'NONE',  ( 10.97171279554003043, 8.773889247172311556, -44.61149169061435060 ) ) ;
#12905=CARTESIAN_POINT ( 'NONE',  ( 6.122889822326360587, 4.740853562741660809, 5.281130613318502753 ) ) ;
#12912=CARTESIAN_POINT ( 'NONE',  ( -25.20396192594209595, 0.003535883027464600988, -199.4400073539133871 ) ) ;
#12913=CARTESIAN_POINT ( 'NONE',  ( 8.946924470861457479, 11.53290492750693197, 2.334117507164750638 ) ) ;
#12917=CARTESIAN_POINT ( 'NONE',  ( 4.917302814907795749, 8.673617379884035472E-16, -102.2758535390863273 ) ) ;
#12922=EDGE_CURVE ( 'NONE', #10207, #13643, #12352, .T. ) ;
#12924=CARTESIAN_POINT ( 'NONE',  ( 24.49199709446414275, 1.068333355338896729, -137.6936497164150524 ) ) ;
#12931=EDGE_LOOP ( 'NONE', ( #6708, #12601, #6766, #8604 ) ) ;
#12932=CARTESIAN_POINT ( 'NONE',  ( 26.15341798802279527, 4.000000000000000000, -138.2600702976168350 ) ) ;
#12936=AXIS2_PLACEMENT_3D ( 'NONE', #14115, #116, #9241 ) ;
#12937=CARTESIAN_POINT ( 'NONE',  ( 13.05714099816148277, 4.000000000000000000, -166.3497942184958447 ) ) ;
#12941=CARTESIAN_POINT ( 'NONE',  ( -3.664341105599659976, 5.000000000000000000, -109.4598404583043703 ) ) ;
#12943=DIRECTION ( 'NONE',  ( 1.000000000000000000, 0.000000000000000000, 0.000000000000000000 ) ) ;
#12948=CARTESIAN_POINT ( 'NONE',  ( 26.93149290009008823, 5.000000000000000888, -137.0203993314533761 ) ) ;
#12951=FACE_OUTER_BOUND ( 'NONE', #12173, .T. ) ;
#12953=ORIENTED_EDGE ( 'NONE', *, *, #8680, .T. ) ;
#12958=CARTESIAN_POINT ( 'NONE',  ( -0.06526978514036563261, 9.999999999999998224, -101.7940732946927227 ) ) ;
#12961=CARTESIAN_POINT ( 'NONE',  ( -9.365519517993458720, 9.999999999999998224, -117.8403265034297505 ) ) ;
#12965=B_SPLINE_CURVE_WITH_KNOTS ( 'NONE', 3,
 ( #13575, #8925, #6534, #13654, #510, #11169, #2758, #6306, #9937, #3054 ),
 .UNSPECIFIED., .F., .F.,
 ( 4, 2, 2, 2, 4 ),
 ( 1.430489624538199204E-17, 0.0007393650634207661089, 0.001478730126841517906, 0.002218095190262269704, 0.002957460253683021501 ),
 .UNSPECIFIED. ) ;
#12974=FACE_OUTER_BOUND ( 'NONE', #1633, .T. ) ;
#12976=CARTESIAN_POINT ( 'NONE',  ( 7.558695724227160184, 0.1516696207343164460, -105.3410990411258013 ) ) ;
#12980=VERTEX_POINT ( 'NONE', #577 ) ;
#12981=CARTESIAN_POINT ( 'NONE',  ( -21.49135656595054655, 0.000000000000000000, -206.0886596525522236 ) ) ;
#12988=B_SPLINE_CURVE_WITH_KNOTS ( 'NONE', 1,
 ( #6669, #7897 ),
 .UNSPECIFIED., .F., .F.,
 ( 2, 2 ),
 ( 0.000000000000000000, 1.000000000000000000 ),
 .UNSPECIFIED. ) ;
#12998=LINE ( 'NONE', #2713, #4911 ) ;
#13006=CARTESIAN_POINT ( 'NONE',  ( -10.45827128286561702, 2.442921369471867893E-15, -185.7209244056693649 ) ) ;
#13010=ORIENTED_EDGE ( 'NONE', *, *, #2677, .T. ) ;
#13012=CARTESIAN_POINT ( 'NONE',  ( -8.456080320763129876, 1.656510688599710290, -116.2291922150375001 ) ) ;
#13014=EDGE_CURVE ( 'NONE', #5472, #7799, #14658, .T. ) ;
#13019=PLANE ( 'NONE',  #5301 ) ;
#13020=CARTESIAN_POINT ( 'NONE',  ( 21.65409573407107402, 8.673617379884035472E-16, -133.3516700272784590 ) ) ;
#13030=CARTESIAN_POINT ( 'NONE',  ( 8.673617379884035472E-16, 9.999999999999998224, -101.1952717268916757 ) ) ;
#13035=CARTESIAN_POINT ( 'NONE',  ( 9.200550766085388688, 14.99999999999999822, -124.0431718307209508 ) ) ;
#13039=LINE ( 'NONE', #2449, #9452 ) ;
#13041=DIRECTION ( 'NONE',  ( 0.000000000000000000, 1.000000000000000000, 0.000000000000000000 ) ) ;
#13043=CARTESIAN_POINT ( 'NONE',  ( -4.545909498366142110, 5.000000000000000000, -129.6154209247606843 ) ) ;
#13045=CARTESIAN_POINT ( 'NONE',  ( 6.288457687482224223, 8.673617379884035472E-16, -105.0111312234662506 ) ) ;
#13049=VERTEX_POINT ( 'NONE', #12620 ) ;
#13050=CARTESIAN_POINT ( 'NONE',  ( 7.113352963092393288, 0.9553916634466306235, 3.767908876148229780 ) ) ;
#13061=FACE_BOUND ( 'NONE', #5791, .T. ) ;
#13065=CARTESIAN_POINT ( 'NONE',  ( 17.21360758414088465, 4.000000000000000000, -156.8016104511478090 ) ) ;
#13067=CARTESIAN_POINT ( 'NONE',  ( 1.114947364559086829, 5.000000000000000888, -139.4079432275550232 ) ) ;
#13073=ORIENTED_EDGE ( 'NONE', *, *, #9105, .T. ) ;
#13075=CARTESIAN_POINT ( 'NONE',  ( -29.27234010639886108, 8.673617379884035472E-16, -207.3549529969440357 ) ) ;
#13080=ORIENTED_EDGE ( 'NONE', *, *, #4223, .F. ) ;
#13081=CARTESIAN_POINT ( 'NONE',  ( -5.561182064722144602, 0.1084047942993575236, -117.2542806587631787 ) ) ;
#13089=B_SPLINE_CURVE_WITH_KNOTS ( 'NONE', 3,
 ( #14831, #12410, #4378, #9087, #4230, #13892, #2059, #6771, #10095, #970, #11408, #13736, #8935, #7849, #6541, #14982, #1906, #1832, #11254, #11328, #747, #5458, #10175, #1978, #6694, #826, #14268, #2286, #11929, #14193, #9385, #2431, #9313, #7125, #15136, #9542, #7209, #6991 ),
 .UNSPECIFIED., .F., .F.,
 ( 4, 2, 2, 2, 2, 2, 2, 2, 2, 2, 2, 2, 2, 2, 2, 2, 2, 2, 4 ),
 ( 0.000000000000000000, 0.005132352563142216634, 0.01026470512628443327, 0.02052941025256887000, 0.03079411537885330674, 0.03336029166042438210, 0.03592646794199545746, 0.04105882050513753184, 0.05132352563142168755, 0.05388970191299279067, 0.05645587819456389378, 0.06158823075770617633, 0.06672058332084844501, 0.07185293588399073450, 0.07441911216556192088, 0.07698528844713309338, 0.07955146472870427976, 0.08083455286948990071, 0.08211764101027552165 ),
 .UNSPECIFIED. ) ;
#13091=CARTESIAN_POINT ( 'NONE',  ( 8.610575960386558592, 15.00000000000000000, -106.0856774745618480 ) ) ;
#13092=CARTESIAN_POINT ( 'NONE',  ( 25.37357285196682355, 5.000000000000000888, -136.0302139098317298 ) ) ;
#13102=ORIENTED_EDGE ( 'NONE', *, *, #6697, .T. ) ;
#13113=EDGE_CURVE ( 'NONE', #3224, #2133, #1133, .T. ) ;
#13114=CYLINDRICAL_SURFACE ( 'NONE', #13201, 3.000000000000005329 ) ;
#13116=EDGE_CURVE ( 'NONE', #6908, #14015, #9635, .T. ) ;
#13119=DIRECTION ( 'NONE',  ( -0.000000000000000000, 1.000000000000000000, -0.000000000000000000 ) ) ;
#13121=B_SPLINE_CURVE_WITH_KNOTS ( 'NONE', 3,
 ( #9096, #9254, #3144, #5470, #12420, #4464, #5391, #10189, #1990, #13817, #14843, #9176, #5690, #13979, #7707, #13906, #686, #11497, #8012, #912, #6852, #3304, #11263, #10106, #3219, #8946, #982, #12739, #14922, #10260, #6630, #2148, #4318, #9022, #15149, #10414 ),
 .UNSPECIFIED., .F., .F.,
 ( 4, 2, 2, 2, 2, 2, 2, 2, 2, 2, 2, 2, 2, 2, 2, 2, 2, 4 ),
 ( 1.734723475976807094E-18, 0.001204836556977712577, 0.002409673113955423419, 0.004819346227910881533, 0.006024182784888610157, 0.007229019341866339647, 0.008433855898844067403, 0.009638692455821797761, 0.01204836556977721164, 0.01445803868373262899, 0.01566287524071035414, 0.01686771179768807583, 0.01927738491164353307, 0.02409673113955440593, 0.02891607736746527879, 0.03132575048142070828, 0.03373542359537614471, 0.03855476982328707308 ),
 .UNSPECIFIED. ) ;
#13123=CARTESIAN_POINT ( 'NONE',  ( 1.123784099566545791, 4.588323854676484181, -139.4224385785465188 ) ) ;
#13125=DIRECTION ( 'NONE',  ( 1.000000000000000000, 0.000000000000000000, 0.000000000000000000 ) ) ;
#13127=CARTESIAN_POINT ( 'NONE',  ( 10.79182909825924419, 3.336188342113987293, -106.9908110512689063 ) ) ;
#13129=CARTESIAN_POINT ( 'NONE',  ( -5.020274906786214686, 13.64026223784254022, -125.1229904268055293 ) ) ;
#13133=CARTESIAN_POINT ( 'NONE',  ( 7.528205663287619309, 1.351247849200009732, 4.229918499259564868 ) ) ;
#13142=CARTESIAN_POINT ( 'NONE',  ( 10.38363273743979498, 14.45937571482893524, -106.4521696696246522 ) ) ;
#13152=DIRECTION ( 'NONE',  ( -0.9997619372588931741, -0.000000000000000000, -0.02181900108494707821 ) ) ;
#13153=CARTESIAN_POINT ( 'NONE',  ( 1.041519256436020280, 5.000000000000000888, -139.4527716894433240 ) ) ;
#13156=CARTESIAN_POINT ( 'NONE',  ( -9.721966606378851239, 5.000000000000000888, -116.3614657639809309 ) ) ;
#13162=CARTESIAN_POINT ( 'NONE',  ( -23.51189632655365003, -2.261592833039957532E-12, -204.5548166363960547 ) ) ;
#13167=TOROIDAL_SURFACE ( 'NONE', #6251, 4.000000000000001776, 1.000000000000000000 ) ;
#13170=CARTESIAN_POINT ( 'NONE',  ( 11.73205471245423048, 8.673617379884034486E-16, -131.2319155360884793 ) ) ;
#13175=CARTESIAN_POINT ( 'NONE',  ( -1.511057375649833556, 6.071532165918824830E-15, -124.5116290068135640 ) ) ;
#13176=CARTESIAN_POINT ( 'NONE',  ( 18.82489474308959032, 5.000000000000000888, -131.0518286717021397 ) ) ;
#13183=ORIENTED_EDGE ( 'NONE', *, *, #5262, .T. ) ;
#13184=CARTESIAN_POINT ( 'NONE',  ( 26.26584183167803133, 2.580188100158157916, -138.3181169695228334 ) ) ;
#13188=CARTESIAN_POINT ( 'NONE',  ( -4.781971238311125916, 15.00000000000000000, -110.8602639898872155 ) ) ;
#13190=B_SPLINE_CURVE_WITH_KNOTS ( 'NONE', 3,
 ( #4136, #8913, #3904, #2895, #425, #3043, #7754, #12469, #498, #1888 ),
 .UNSPECIFIED., .F., .F.,
 ( 4, 2, 2, 2, 4 ),
 ( 0.000000000000000000, 0.0005552365111544495723, 0.001110473022308899145, 0.001665709533463348609, 0.002220946044617798289 ),
 .UNSPECIFIED. ) ;
#13192=AXIS2_PLACEMENT_3D ( 'NONE', #5495, #1941, #11068 ) ;
#13198=CARTESIAN_POINT ( 'NONE',  ( 11.74818764249840797, 15.00000000000000000, -127.4816575577899584 ) ) ;
#13201=AXIS2_PLACEMENT_3D ( 'NONE', #2527, #14204, #4763 ) ;
#13202=LINE ( 'NONE', #1369, #3779 ) ;
#13210=CARTESIAN_POINT ( 'NONE',  ( 10.23916242951791844, 1.886766667146307919, -106.0869873573526263 ) ) ;
#13212=CIRCLE ( 'NONE', #9755, 1.250000000000005107 ) ;
#13213=CARTESIAN_POINT ( 'NONE',  ( -3.674418796289115718, 14.44898052987122128, -125.2714716606675722 ) ) ;
#13215=VERTEX_POINT ( 'NONE', #2485 ) ;
#13216=CARTESIAN_POINT ( 'NONE',  ( 7.530864077104208576, 1.500743522379207606, 1.949903166259959297 ) ) ;
#13223=CARTESIAN_POINT ( 'NONE',  ( 9.412918133875843196, 14.94619758066195914, -106.0880953390660579 ) ) ;
#13233=CARTESIAN_POINT ( 'NONE',  ( 12.37900876701962360, 2.133003846422337535, -165.9182586569806404 ) ) ;
#13236=CARTESIAN_POINT ( 'NONE',  ( -9.335177092165887203, 3.999999999999993783, -147.7150205453479543 ) ) ;
#13238=CARTESIAN_POINT ( 'NONE',  ( -22.81000397151760239, 8.673617379884034486E-16, -177.4076321631416704 ) ) ;
#13240=VERTEX_POINT ( 'NONE', #91 ) ;
#13256=CARTESIAN_POINT ( 'NONE',  ( -1.445049719264795529, 1.188659952750201131E-12, -134.5128495246223110 ) ) ;
#13257=CARTESIAN_POINT ( 'NONE',  ( 8.769209038339429441, 5.000000000000000888, -110.8932515380079025 ) ) ;
#13261=ORIENTED_EDGE ( 'NONE', *, *, #13113, .T. ) ;
#13263=CARTESIAN_POINT ( 'NONE',  ( 26.36813061592906138, 2.735303735283647786, -138.3050569091936097 ) ) ;
#13267=EDGE_LOOP ( 'NONE', ( #14587, #405, #2385, #2037 ) ) ;
#13268=CARTESIAN_POINT ( 'NONE',  ( 5.000000000000001776, 15.00000000000000000, -1.663700395152567513 ) ) ;
#13275=CARTESIAN_POINT ( 'NONE',  ( -25.33202823091587774, 0.2517120273413803733, -202.7304169256179307 ) ) ;
#13282=DIRECTION ( 'NONE',  ( 0.000000000000000000, -1.000000000000000000, 0.000000000000000000 ) ) ;
#13287=CARTESIAN_POINT ( 'NONE',  ( 10.45437233589498760, 14.39522854901148996, -106.2185126042158743 ) ) ;
#13292=CARTESIAN_POINT ( 'NONE',  ( 4.625401223603891943, 0.004023134192272380567, -0.5198385758609599394 ) ) ;
#13303=B_SPLINE_CURVE_WITH_KNOTS ( 'NONE', 3,
 ( #7892, #9208, #15256, #5578, #2030, #2258, #8044, #5801, #12924, #4726, #4647, #8117, #8194, #9356, #6963, #12693, #12844, #2179, #14082, #6883 ),
 .UNSPECIFIED., .F., .F.,
 ( 4, 2, 2, 2, 2, 2, 2, 2, 2, 4 ),
 ( -1.419801435424954991E-05, 0.001093604629081186205, 0.002201407272516621959, 0.003309209915952058146, 0.004417012559387493466, 0.005524815202822929219, 0.006078716524540635387, 0.006632617846258340687, 0.007740420489693738276, 0.008848223133129131529 ),
 .UNSPECIFIED. ) ;
#13308=CARTESIAN_POINT ( 'NONE',  ( 11.04730217088350663, 12.49999999999999822, -107.1178495010082941 ) ) ;
#13310=CARTESIAN_POINT ( 'NONE',  ( 1.592538968424295431, 8.673617379884034486E-16, -140.1913613025302254 ) ) ;
#13313=CARTESIAN_POINT ( 'NONE',  ( -10.59012558253652792, 8.673617379884035472E-16, -156.2763189018182857 ) ) ;
#13314=ORIENTED_EDGE ( 'NONE', *, *, #12014, .T. ) ;
#13318=CARTESIAN_POINT ( 'NONE',  ( -24.74264876967802351, 4.000000000000000888, -209.2209370252883787 ) ) ;
#13325=B_SPLINE_CURVE_WITH_KNOTS ( 'NONE', 3,
 ( #5646, #10364, #10143, #2028, #4498, #9131, #13711, #8043, #4575, #5424 ),
 .UNSPECIFIED., .F., .F.,
 ( 4, 2, 2, 2, 4 ),
 ( 0.000000000000000000, 0.0009395823385051277950, 0.001879164677010255590, 0.002818747015515383168, 0.003758329354020511180 ),
 .UNSPECIFIED. ) ;
#13326=B_SPLINE_CURVE_WITH_KNOTS ( 'NONE', 3,
 ( #1300, #13129, #10726, #7240, #11954, #13213, #1379, #6081, #212, #4926, #3774, #8479 ),
 .UNSPECIFIED., .F., .F.,
 ( 4, 2, 2, 2, 2, 4 ),
 ( 0.000000000000000000, 0.001181812431113227766, 0.001772718646669842841, 0.002363624862226459001, 0.003545437293339693055, 0.004727249724452926675 ),
 .UNSPECIFIED. ) ;
#13331=CARTESIAN_POINT ( 'NONE',  ( -5.418138540701908923, 15.00000000000000711, -127.8817495432483469 ) ) ;
#13333=CARTESIAN_POINT ( 'NONE',  ( -2.629469332551699789, -8.673617379884035472E-16, -121.9913505756445886 ) ) ;
#13335=ORIENTED_EDGE ( 'NONE', *, *, #11420, .F. ) ;
#13340=CARTESIAN_POINT ( 'NONE',  ( 22.68437819464854854, 0.2142782701973315329, -138.7614552119420352 ) ) ;
#13345=DIRECTION ( 'NONE',  ( 8.764770998266003672E-18, -0.000000000000000000, 1.000000000000000000 ) ) ;
#13348=AXIS2_PLACEMENT_3D ( 'NONE', #11606, #4428, #14964 ) ;
#13354=EDGE_LOOP ( 'NONE', ( #13010, #3833, #8542, #11080, #14436, #22, #6473, #5755, #3573, #4750, #10153, #8221, #9792 ) ) ;
#13361=EDGE_CURVE ( 'NONE', #5152, #933, #5904, .T. ) ;
#13370=CARTESIAN_POINT ( 'NONE',  ( 7.000000000000000888, 9.999999999999998224, -1.663700395152567513 ) ) ;
#13372=CARTESIAN_POINT ( 'NONE',  ( 4.029045719581688445, 0.1039572972702087761, -1.052128926548778542 ) ) ;
#13376=CIRCLE ( 'NONE', #9161, 0.5000000000000004441 ) ;
#13378=CARTESIAN_POINT ( 'NONE',  ( 0.000000000000000000, 9.999999999999998224, -100.6237003951525679 ) ) ;
#13379=CARTESIAN_POINT ( 'NONE',  ( 7.000000000000000888, 5.000000000000000888, -1.663700395152567513 ) ) ;
#13380=CARTESIAN_POINT ( 'NONE',  ( 1.165583190371173750, 4.454698458770116609, -139.4098078394992228 ) ) ;
#13384=EDGE_CURVE ( 'NONE', #1192, #5201, #12294, .T. ) ;
#13388=AXIS2_PLACEMENT_3D ( 'NONE', #8083, #12807, #6921 ) ;
#13390=( BOUNDED_CURVE ( )  B_SPLINE_CURVE ( 3, ( #4861, #14227, #77, #2626 ),
 .UNSPECIFIED., .F., .T. ) 
 B_SPLINE_CURVE_WITH_KNOTS ( ( 4, 4 ),
 ( 3.820990438000858802, 4.241828308846971041 ),
 .UNSPECIFIED. ) 
 CURVE ( )  GEOMETRIC_REPRESENTATION_ITEM ( )  RATIONAL_B_SPLINE_CURVE ( ( 1.000000000000000000, 0.9852956651098603302, 0.9852956651098603302, 1.000000000000000000 ) ) 
 REPRESENTATION_ITEM ( '' )  );
#13392=CARTESIAN_POINT ( 'NONE',  ( -4.808605925792019065, 8.673617379884035472E-16, -150.1721608607652456 ) ) ;
#13393=PLANE ( 'NONE',  #9639 ) ;
#13399=CARTESIAN_POINT ( 'NONE',  ( -13.61615722309449872, 4.488109077202681521E-13, -189.4575979531706480 ) ) ;
#13402=DIRECTION ( 'NONE',  ( 0.9997619372588932851, -0.000000000000000000, 0.02181900108494707474 ) ) ;
#13403=VERTEX_POINT ( 'NONE', #13156 ) ;
#13405=CARTESIAN_POINT ( 'NONE',  ( -9.079473912027703264, 3.253592935839261013, -115.4940425210697441 ) ) ;
#13407=EDGE_CURVE ( 'NONE', #10375, #2594, #11449, .T. ) ;
#13412=DIRECTION ( 'NONE',  ( 0.000000000000000000, 0.000000000000000000, 1.000000000000000000 ) ) ;
#13415=CARTESIAN_POINT ( 'NONE',  ( -4.406415408179883642, 15.00000000000000355, -116.9422405828140654 ) ) ;
#13416=CARTESIAN_POINT ( 'NONE',  ( -9.518035002864159821, -1.966966232440479402E-12, -117.2217326882803832 ) ) ;
#13417=CARTESIAN_POINT ( 'NONE',  ( 3.327290866796126068, 1.734723475976807094E-15, -114.7643839154946761 ) ) ;
#13422=ORIENTED_EDGE ( 'NONE', *, *, #13384, .T. ) ;
#13424=DIRECTION ( 'NONE',  ( 0.000000000000000000, 1.000000000000000000, 0.000000000000000000 ) ) ;
#13426=AXIS2_PLACEMENT_3D ( 'NONE', #10194, #4469, #7794 ) ;
#13430=CARTESIAN_POINT ( 'NONE',  ( -0.9685250182442692868, 15.00000000000000000, -114.0968640496209190 ) ) ;
#13439=EDGE_LOOP ( 'NONE', ( #187, #5760, #5509, #9521, #6949 ) ) ;
#13442=EDGE_LOOP ( 'NONE', ( #8101, #345, #1523, #8704 ) ) ;
#13443=CARTESIAN_POINT ( 'NONE',  ( 10.97171279554003043, 8.773889247172311556, -44.61149169061435060 ) ) ;
#13447=DIRECTION ( 'NONE',  ( 0.000000000000000000, -1.000000000000000000, 0.000000000000000000 ) ) ;
#13448=CARTESIAN_POINT ( 'NONE',  ( 13.87268740824488411, 13.20263832612636179, -126.2495228518582593 ) ) ;
#13451=VECTOR ( 'NONE', #7541, 999.9999999999998863 ) ;
#13458=CARTESIAN_POINT ( 'NONE',  ( -0.8684534520279955094, 10.00000000000000355, -104.6281219612548625 ) ) ;
#13465=DIRECTION ( 'NONE',  ( 0.02032500363963561651, 0.3636704086172907746, -0.9313059261720509907 ) ) ;
#13468=DIRECTION ( 'NONE',  ( -0.02181900108494707127, -0.000000000000000000, 0.9997619372588931741 ) ) ;
#13469=CARTESIAN_POINT ( 'NONE',  ( 9.962419064811388836, 0.09217387118650985367, -163.9266138299434772 ) ) ;
#13471=CARTESIAN_POINT ( 'NONE',  ( -30.34667403426979604, 4.000000000000237144, -197.7357094718530846 ) ) ;
#13474=CARTESIAN_POINT ( 'NONE',  ( 4.999884908348398049, 0.09438068890155060231, -1.653151978968578462 ) ) ;
#13477=VERTEX_POINT ( 'NONE', #12348 ) ;
#13482=CARTESIAN_POINT ( 'NONE',  ( 27.03835354040200301, 6.000000000000000000, -138.2189567750508843 ) ) ;
#13484=CARTESIAN_POINT ( 'NONE',  ( -8.786545012119724163, 2.617545850260423190, -115.6253344005663166 ) ) ;
#13487=( BOUNDED_SURFACE ( )  B_SPLINE_SURFACE ( 3, 2, ( 
 ( #9691, #11997, #2583 ),
 ( #5058, #8763, #8522 ),
 ( #12240, #8444, #14656 ),
 ( #2741, #13256, #2661 ),
 ( #3821, #1346, #7444 ),
 ( #7362, #262, #9923 ),
 ( #9770, #8598, #12076 ),
 ( #1500, #4895, #3978 ),
 ( #3738, #14576, #6211 ),
 ( #13175, #7284, #10926 ),
 ( #3900, #14336, #4973 ),
 ( #13333, #14422, #9607 ),
 ( #12161, #1423, #9843 ),
 ( #343, #14501, #2819 ),
 ( #8682, #7521, #1576 ),
 ( #6291, #11007, #421 ),
 ( #5131, #13416, #2892 ),
 ( #184, #4059, #1651 ) ),
 .UNSPECIFIED., .F., .F., .T. ) 
 B_SPLINE_SURFACE_WITH_KNOTS ( ( 4, 2, 2, 2, 2, 2, 2, 2, 4 ),
 ( 3, 3 ),
 ( 0.000000000000000000, 0.002730992342634833061, 0.005461984685269666122, 0.008192977027904498749, 0.01092396937053933224, 0.01365496171317416574, 0.01638595405580899750, 0.01911694639844382926, 0.02184793874107866449 ),
 ( 0.000000000000000000, 1.000000000000000000 ),
 .UNSPECIFIED. ) 
 GEOMETRIC_REPRESENTATION_ITEM ( )  RATIONAL_B_SPLINE_SURFACE ( (
 ( 1.000000000000000000, 0.7071067811865475727, 1.000000000000000000),
 ( 1.000000000000000000, 0.7071067811865475727, 1.000000000000000000),
 ( 1.000000000000000000, 0.7071067811865475727, 1.000000000000000000),
 ( 1.000000000000000000, 0.7071067811865475727, 1.000000000000000000),
 ( 1.000000000000000000, 0.7071067811865476838, 1.000000000000000000),
 ( 1.000000000000000000, 0.7071067811865476838, 1.000000000000000000),
 ( 1.000000000000000000, 0.7071067811865473507, 1.000000000000000000),
 ( 1.000000000000000000, 0.7071067811865473507, 1.000000000000000000),
 ( 1.000000000000000000, 0.7071067811865476838, 1.000000000000000000),
 ( 1.000000000000000000, 0.7071067811865476838, 1.000000000000000000),
 ( 1.000000000000000000, 0.7071067811865471286, 1.000000000000000000),
 ( 1.000000000000000000, 0.7071067811865471286, 1.000000000000000000),
 ( 1.000000000000000000, 0.7071067811865477948, 1.000000000000000000),
 ( 1.000000000000000000, 0.7071067811865477948, 1.000000000000000000),
 ( 1.000000000000000000, 0.7071067811865477948, 1.000000000000000000),
 ( 1.000000000000000000, 0.7071067811865477948, 1.000000000000000000),
 ( 1.000000000000000000, 0.7071067811865476838, 1.000000000000000000),
 ( 1.000000000000000000, 0.7071067811865476838, 1.000000000000000000) ) ) 
 REPRESENTATION_ITEM ( '' )  SURFACE ( )  );
#13494=CARTESIAN_POINT ( 'NONE',  ( 10.27157762096145710, 5.000000000000000888, -107.9972514638527912 ) ) ;
#13495=CARTESIAN_POINT ( 'NONE',  ( 0.000000000000000000, 15.00000000000000000, -100.6237003951525679 ) ) ;
#13500=CARTESIAN_POINT ( 'NONE',  ( 8.987149773678774878, 12.49999999999999645, 0.4909659112279870508 ) ) ;
#13501=CARTESIAN_POINT ( 'NONE',  ( 25.28120514378732864, 1.499740039320041296, -138.4427521360613866 ) ) ;
#13510=CARTESIAN_POINT ( 'NONE',  ( -24.82368063746440612, 4.000000000000000000, -209.1616663288132827 ) ) ;
#13512=SHAPE_DEFINITION_REPRESENTATION ( #4478, #7636 ) ;
#13513=CARTESIAN_POINT ( 'NONE',  ( 12.44913988807079086, 15.00000000000000000, -128.2750425511075036 ) ) ;
#13518=ORIENTED_EDGE ( 'NONE', *, *, #1168, .F. ) ;
#13520=B_SPLINE_CURVE_WITH_KNOTS ( 'NONE', 3,
 ( #6230, #10944, #362, #3917, #1743, #739, #2980, #13728, #10166, #667, #592, #3055, #6453, #7609, #3128, #14900, #8926, #6379, #12402, #9938, #8781, #6685 ),
 .UNSPECIFIED., .F., .F.,
 ( 4, 2, 2, 2, 2, 2, 2, 2, 2, 2, 4 ),
 ( 0.000000000000000000, 0.001234958623131101165, 0.002469917246262202330, 0.003704875869393304145, 0.004322355180958854619, 0.004939834492524404659, 0.005557313804089955567, 0.006174793115655505607, 0.007409751738786608290, 0.008644710361917709238, 0.009879668985048807583 ),
 .UNSPECIFIED. ) ;
#13522=DIRECTION ( 'NONE',  ( -0.000000000000000000, 1.000000000000000000, -0.000000000000000000 ) ) ;
#13539=CARTESIAN_POINT ( 'NONE',  ( -9.410661088365667837, 3.301239252470002050, -116.4362230898866528 ) ) ;
#13542=CARTESIAN_POINT ( 'NONE',  ( 12.73470083568815170, 2.902482184389665765, -166.2121014961018375 ) ) ;
#13543=CARTESIAN_POINT ( 'NONE',  ( 10.89041330322193701, 3.672903760508912097, -107.0396867723672329 ) ) ;
#13544=CARTESIAN_POINT ( 'NONE',  ( -15.97579411175272313, 3.999999999999753975, -155.0504951762476082 ) ) ;
#13549=CARTESIAN_POINT ( 'NONE',  ( 10.99340860758277927, 5.943472311793079221, -45.60560901953395785 ) ) ;
#13550=CARTESIAN_POINT ( 'NONE',  ( 16.61630038475162863, 8.673617379884034486E-16, -146.8898935758374478 ) ) ;
#13562=CARTESIAN_POINT ( 'NONE',  ( 9.112041370335649759, -1.070315399344735426E-12, -109.9899024349114853 ) ) ;
#13565=ORIENTED_EDGE ( 'NONE', *, *, #8460, .T. ) ;
#13571=VERTEX_POINT ( 'NONE', #11193 ) ;
#13575=CARTESIAN_POINT ( 'NONE',  ( 9.940211158120405344, 12.49999999999999822, -43.17897536272747772 ) ) ;
#13578=CARTESIAN_POINT ( 'NONE',  ( -9.076832803613291034, 12.38245414981636650, -116.5147594324881339 ) ) ;
#13581=CARTESIAN_POINT ( 'NONE',  ( 11.05697737868720232, 15.00000000000186162, -122.2826711086158014 ) ) ;
#13582=ORIENTED_EDGE ( 'NONE', *, *, #3849, .T. ) ;
#13588=CARTESIAN_POINT ( 'NONE',  ( 6.422699671861707316, 6.000000000000000000, -139.1645012375703061 ) ) ;
#13595=CARTESIAN_POINT ( 'NONE',  ( 11.04730217088330413, 5.000000000000001776, -107.1178495010084504 ) ) ;
#13598=EDGE_CURVE ( 'NONE', #5201, #2826, #9401, .T. ) ;
#13601=FACE_OUTER_BOUND ( 'NONE', #5546, .T. ) ;
#13607=CARTESIAN_POINT ( 'NONE',  ( -4.116580123655899648E-16, 10.00000000000000000, -101.3854116612075700 ) ) ;
#13609=CARTESIAN_POINT ( 'NONE',  ( 1.203323408085149371, 4.317064434386042038, -139.4038898281761760 ) ) ;
#13618=CARTESIAN_POINT ( 'NONE',  ( 4.999884908348399826, 0.09438068890153285262, -1.653151978968515845 ) ) ;
#13619=CARTESIAN_POINT ( 'NONE',  ( 8.935548306746154523, 5.000000000000000888, 2.855381328098136162 ) ) ;
#13620=CARTESIAN_POINT ( 'NONE',  ( 6.914202122640618953, 1.078315293502086643E-12, -105.2584297683565211 ) ) ;
#13622=CARTESIAN_POINT ( 'NONE',  ( -29.87892995173857003, 3.999999999999993783, -184.6141453219341599 ) ) ;
#13627=ORIENTED_EDGE ( 'NONE', *, *, #7824, .F. ) ;
#13629=CARTESIAN_POINT ( 'NONE',  ( 11.05182978094480895, 3.355895706359027564, -106.3279719483364829 ) ) ;
#13643=VERTEX_POINT ( 'NONE', #13751 ) ;
#13644=CARTESIAN_POINT ( 'NONE',  ( 8.935548306746158076, 10.33196145731881721, 2.855381328098129057 ) ) ;
#13645=CARTESIAN_POINT ( 'NONE',  ( -14.95313816010867392, 3.999999999999999112, -192.4638183655883097 ) ) ;
#13651=CARTESIAN_POINT ( 'NONE',  ( 10.04032073682954618, 11.75496761609937657, -45.01598776155166348 ) ) ;
#13654=CARTESIAN_POINT ( 'NONE',  ( 9.955014136429161553, 12.67960752135156888, -44.14371989070262003 ) ) ;
#13656=CARTESIAN_POINT ( 'NONE',  ( -8.207841483268280669, 13.21761715706680462, -115.8806436028953186 ) ) ;
#13658=CARTESIAN_POINT ( 'NONE',  ( 11.32055997300887462, 12.49999999999999822, -122.6997364777432438 ) ) ;
#13659=CIRCLE ( 'NONE', #2532, 1.000000000000028644 ) ;
#13660=CARTESIAN_POINT ( 'NONE',  ( 27.03835354040196037, 5.000000000000001776, -138.2189567750509696 ) ) ;
#13676=VERTEX_POINT ( 'NONE', #8949 ) ;
#13687=CARTESIAN_POINT ( 'NONE',  ( 10.98638689276455871, 5.830414921909241599, -45.28386912034150669 ) ) ;
#13690=CIRCLE ( 'NONE', #5771, 7.000000000000000000 ) ;
#13691=CARTESIAN_POINT ( 'NONE',  ( 1.004809442601927394, 6.000000000000000000, -139.4752805618705622 ) ) ;
#13692=CARTESIAN_POINT ( 'NONE',  ( 6.095360508540255573, 15.00000000000000000, -116.7523417411930211 ) ) ;
#13695=CARTESIAN_POINT ( 'NONE',  ( -30.68313436375902370, 4.000000000000354383, -191.4730121854663878 ) ) ;
#13700=DIRECTION ( 'NONE',  ( 0.000000000000000000, 0.000000000000000000, 1.000000000000000000 ) ) ;
#13705=CARTESIAN_POINT ( 'NONE',  ( -16.87511749404491823, 8.673617379884032514E-16, -186.9742884131397318 ) ) ;
#13706=CARTESIAN_POINT ( 'NONE',  ( -5.318033920936450443, 8.673617379884035472E-16, -111.4753907371134574 ) ) ;
#13711=CARTESIAN_POINT ( 'NONE',  ( -6.113022954200721060, 12.39308942777827127, -125.0150693682166292 ) ) ;
#13718=VERTEX_POINT ( 'NONE', #8615 ) ;
#13720=CARTESIAN_POINT ( 'NONE',  ( -1.885039096047290252, 15.00000000000000178, -115.1740262261674985 ) ) ;
#13728=CARTESIAN_POINT ( 'NONE',  ( 4.543692464186339208, 0.6724431706707657552, 2.119679957923213731 ) ) ;
#13729=CARTESIAN_POINT ( 'NONE',  ( -5.492028030077825917, 14.89159520566441408, -117.0085585369580770 ) ) ;
#13731=CARTESIAN_POINT ( 'NONE',  ( 6.454204466557374786, 15.00000000000000000, -118.3005150008459196 ) ) ;
#13732=CARTESIAN_POINT ( 'NONE',  ( -4.234402844927150689, 15.00000000000000000, -117.4888040839639558 ) ) ;
#13733=CARTESIAN_POINT ( 'NONE',  ( 22.20883717620709774, 0.09828479603275584731, -138.5096390345515545 ) ) ;
#13736=CARTESIAN_POINT ( 'NONE',  ( -21.96202414993823382, 4.000000000000001776, -164.0357374456417006 ) ) ;
#13739=FACE_OUTER_BOUND ( 'NONE', #12783, .T. ) ;
#13742=DIRECTION ( 'NONE',  ( 0.000000000000000000, 0.000000000000000000, 1.000000000000000000 ) ) ;
#13750=ORIENTED_EDGE ( 'NONE', *, *, #8014, .F. ) ;
#13751=CARTESIAN_POINT ( 'NONE',  ( 26.15341798802279527, 6.000000000000000000, -138.2600702976168350 ) ) ;
#13753=DIRECTION ( 'NONE',  ( -8.764770998266003672E-18, 0.000000000000000000, -1.000000000000000000 ) ) ;
#13759=CARTESIAN_POINT ( 'NONE',  ( -9.108720832937448719, 2.673239310146674708, -116.5073105006876375 ) ) ;
#13761=CARTESIAN_POINT ( 'NONE',  ( 4.675654263134669364, 1.363187254327671670E-15, -31.10957739081536033 ) ) ;
#13763=EDGE_CURVE ( 'NONE', #4341, #2589, #13376, .T. ) ;
#13764=DIRECTION ( 'NONE',  ( -0.000000000000000000, 1.000000000000000000, -0.000000000000000000 ) ) ;
#13766=CARTESIAN_POINT ( 'NONE',  ( -27.92420520952412488, -2.185846814899320366E-12, -179.9270560460287811 ) ) ;
#13767=CARTESIAN_POINT ( 'NONE',  ( 9.922656535062992944, 0.1207761337397980084, -163.9774224701945968 ) ) ;
#13772=DIRECTION ( 'NONE',  ( 0.000000000000000000, 1.000000000000000000, 0.000000000000000000 ) ) ;
#13773=CARTESIAN_POINT ( 'NONE',  ( -25.68027788593440874, 1.265875433067397582, -206.1712788784230099 ) ) ;
#13775=CARTESIAN_POINT ( 'NONE',  ( 8.963175985653281330, 12.17508258105334917, 1.589461697835446774 ) ) ;
#13776=CARTESIAN_POINT ( 'NONE',  ( 4.999999996894303855, 8.673617379884035472E-16, -101.5775160893583546 ) ) ;
#13788=ORIENTED_EDGE ( 'NONE', *, *, #10729, .T. ) ;
#13790=CARTESIAN_POINT ( 'NONE',  ( 8.414431238570866611, 12.50000000000000000, -115.4905761430241142 ) ) ;
#13799=CARTESIAN_POINT ( 'NONE',  ( -9.868623143903928252, 9.999999999999996447, -115.7530035192428528 ) ) ;
#13801=CARTESIAN_POINT ( 'NONE',  ( 8.317394296398017417, 15.00000000000000000, -114.4625571486813556 ) ) ;
#13804=CARTESIAN_POINT ( 'NONE',  ( 21.56441208847391167, 7.880035444290784328E-10, -138.8172008007609008 ) ) ;
#13814=CARTESIAN_POINT ( 'NONE',  ( -25.29848011718828005, 1.467800717594119675, -207.1124310616453954 ) ) ;
#13817=CARTESIAN_POINT ( 'NONE',  ( 8.362033940405666499, 5.000000000000000888, -112.8158568780617941 ) ) ;
#13818=DIRECTION ( 'NONE',  ( 0.9997619372588931741, 0.000000000000000000, 0.02181900108494707474 ) ) ;
#13820=ORIENTED_EDGE ( 'NONE', *, *, #8631, .T. ) ;
#13832=CARTESIAN_POINT ( 'NONE',  ( 11.30303403385899941, 12.83532670273191556, -106.4054638337314458 ) ) ;
#13834=ADVANCED_FACE ( 'NONE', ( #14519 ), #1322, .T. ) ;
#13838=CARTESIAN_POINT ( 'NONE',  ( -23.34801257951161091, 8.673617379884035472E-16, -203.6232164356695762 ) ) ;
#13841=VECTOR ( 'NONE', #402, 1000.000000000000000 ) ;
#13851=EDGE_CURVE ( 'NONE', #11832, #2518, #14622, .T. ) ;
#13852=CARTESIAN_POINT ( 'NONE',  ( 3.559460973860744559, 8.673617379884035472E-16, -107.0011611385543233 ) ) ;
#13867=CARTESIAN_POINT ( 'NONE',  ( 13.05859050630842333, 12.50000000000000000, -125.1312933577355437 ) ) ;
#13876=EDGE_CURVE ( 'NONE', #4807, #2207, #2911, .T. ) ;
#13884=CARTESIAN_POINT ( 'NONE',  ( 11.05697737879504494, 12.49999999999999822, -122.2826711085474756 ) ) ;
#13885=CARTESIAN_POINT ( 'NONE',  ( -4.580007248818704468, 15.00000000000000533, -117.4298695725142920 ) ) ;
#13886=ORIENTED_EDGE ( 'NONE', *, *, #12150, .T. ) ;
#13887=CARTESIAN_POINT ( 'NONE',  ( 21.54700699050549773, -3.203769437592921893E-16, -138.7416251624139818 ) ) ;
#13892=CARTESIAN_POINT ( 'NONE',  ( -9.629162051845682413, 4.000000000000000888, -147.9061454275191636 ) ) ;
#13902=CARTESIAN_POINT ( 'NONE',  ( -25.28590446626877863, 0.04176024460088630791, -200.8353957342116587 ) ) ;
#13906=CARTESIAN_POINT ( 'NONE',  ( 8.644432307942668814, 5.000000000000001776, -116.7877792220761961 ) ) ;
#13907=CARTESIAN_POINT ( 'NONE',  ( 8.895558325401111688, 6.000000000000000000, -125.4560052468458906 ) ) ;
#13908=ORIENTED_EDGE ( 'NONE', *, *, #10366, .F. ) ;
#13910=CARTESIAN_POINT ( 'NONE',  ( 9.103295372165979060, 15.00000000000043165, -106.0245955897191124 ) ) ;
#13915=ORIENTED_EDGE ( 'NONE', *, *, #517, .T. ) ;
#13916=DIRECTION ( 'NONE',  ( -0.9997619372588931741, -0.000000000000000000, -0.02181900108494707821 ) ) ;
#13923=CARTESIAN_POINT ( 'NONE',  ( 11.11125876792575085, 0.7539515673351797620, -165.0738428850340540 ) ) ;
#13927=DIRECTION ( 'NONE',  ( -0.000000000000000000, -1.000000000000000000, 0.000000000000000000 ) ) ;
#13929=CARTESIAN_POINT ( 'NONE',  ( 8.935548306746156300, 9.999999999999880984, 2.855381328098128613 ) ) ;
#13941=AXIS2_PLACEMENT_3D ( 'NONE', #1186, #2423, #5889 ) ;
#13945=VERTEX_POINT ( 'NONE', #796 ) ;
#13946=CARTESIAN_POINT ( 'NONE',  ( 8.701636889681944709, 12.50000000000000355, -110.9796434783077359 ) ) ;
#13959=CARTESIAN_POINT ( 'NONE',  ( 9.781725384838754422, 12.49999999999999822, -108.7377634488177165 ) ) ;
#13962=ADVANCED_FACE ( 'NONE', ( #14877 ), #12871, .T. ) ;
#13966=ORIENTED_EDGE ( 'NONE', *, *, #11673, .T. ) ;
#13971=ORIENTED_EDGE ( 'NONE', *, *, #9151, .F. ) ;
#13972=CARTESIAN_POINT ( 'NONE',  ( -5.836146573691745942, 14.76824404323223128, -116.8702851668251839 ) ) ;
#13975=CARTESIAN_POINT ( 'NONE',  ( -25.42189670022433035, 0.8929212780356239332, -205.7249994877904840 ) ) ;
#13979=CARTESIAN_POINT ( 'NONE',  ( 8.379952990905023213, 5.000000000000001776, -115.2049983755456282 ) ) ;
#13987=CARTESIAN_POINT ( 'NONE',  ( 0.000000000000000000, 9.999999999999998224, -100.6237003951525679 ) ) ;
#13992=CARTESIAN_POINT ( 'NONE',  ( 11.32016196459912649, 5.000000000000000888, -106.4092894470390291 ) ) ;
#13994=CARTESIAN_POINT ( 'NONE',  ( 5.845480107720362639, 3.062150895296549269, 4.850269518005670299 ) ) ;
#13999=DIRECTION ( 'NONE',  ( 0.000000000000000000, 0.000000000000000000, 1.000000000000000000 ) ) ;
#14000=CARTESIAN_POINT ( 'NONE',  ( 29.21736815051483660, 8.773889247172311556, -44.21329492081407153 ) ) ;
#14001=CIRCLE ( 'NONE', #5356, 1.101020514433642683 ) ;
#14002=FACE_OUTER_BOUND ( 'NONE', #5874, .T. ) ;
#14003=CARTESIAN_POINT ( 'NONE',  ( 0.7716514365823460286, 1.734723475976807094E-15, -111.8714012163897280 ) ) ;
#14005=CARTESIAN_POINT ( 'NONE',  ( 6.491365067585770809, 12.49999999999999822, 0.2705411889128697123 ) ) ;
#14015=VERTEX_POINT ( 'NONE', #2025 ) ;
#14021=ORIENTED_EDGE ( 'NONE', *, *, #733, .F. ) ;
#14024=CARTESIAN_POINT ( 'NONE',  ( -8.749806588114527273, 15.00000000000000000, -116.1271478199639944 ) ) ;
#14031=ORIENTED_EDGE ( 'NONE', *, *, #5368, .T. ) ;
#14032=DIRECTION ( 'NONE',  ( -0.02181900108494707127, 0.000000000000000000, 0.9997619372588931741 ) ) ;
#14041=CARTESIAN_POINT ( 'NONE',  ( 6.276419674667793380, 14.49781573971641890, 2.481921665638175956 ) ) ;
#14046=CARTESIAN_POINT ( 'NONE',  ( -25.02010205735157555, 1.581731481081007251, -206.7284262751177550 ) ) ;
#14060=CARTESIAN_POINT ( 'NONE',  ( -9.721966606378851239, 5.000000000000000888, -116.3614657639809309 ) ) ;
#14065=VERTEX_POINT ( 'NONE', #14801 ) ;
#14070=ORIENTED_EDGE ( 'NONE', *, *, #7047, .T. ) ;
#14074=CARTESIAN_POINT ( 'NONE',  ( 6.183275261587990457, 13.32019864978253310, 4.031137569194784831 ) ) ;
#14078=CARTESIAN_POINT ( 'NONE',  ( 1.299830696487494386, 4.000000000000000000, -139.3994634862947635 ) ) ;
#14082=CARTESIAN_POINT ( 'NONE',  ( 26.71007981443200308, 4.628737540243305304, -136.8791680534709769 ) ) ;
#14092=ORIENTED_EDGE ( 'NONE', *, *, #5981, .T. ) ;
#14103=CARTESIAN_POINT ( 'NONE',  ( 3.289302641759264567, 8.673617379884035472E-16, -113.8917107963726494 ) ) ;
#14108=CARTESIAN_POINT ( 'NONE',  ( 9.410602039359995175, 5.000000000000000888, -119.1126025277838920 ) ) ;
#14112=VECTOR ( 'NONE', #4256, 1000.000000000000114 ) ;
#14113=ORIENTED_EDGE ( 'NONE', *, *, #7824, .T. ) ;
#14115=CARTESIAN_POINT ( 'NONE',  ( 26.17093350124943640, 15.00000000000000000, -137.7213801722282085 ) ) ;
#14119=CARTESIAN_POINT ( 'NONE',  ( -0.3214635615754074527, 14.99999999999918998, -103.0394908280536299 ) ) ;
#14124=CARTESIAN_POINT ( 'NONE',  ( -25.24442296148506770, 1.715658728670576227, -207.5621366369104237 ) ) ;
#14125=CARTESIAN_POINT ( 'NONE',  ( 4.386720528383036388, -4.561518438557346199E-46, -133.8326913415544368 ) ) ;
#14126=CARTESIAN_POINT ( 'NONE',  ( 7.722366886286562426, 14.99999999999999645, -107.3067671354286574 ) ) ;
#14135=CARTESIAN_POINT ( 'NONE',  ( 4.999999999999998224, 0.000000000000000000, -45.97309604003007877 ) ) ;
#14142=CARTESIAN_POINT ( 'NONE',  ( 6.422699671861707316, -4.000000000000000000, -139.1645012375703061 ) ) ;
#14144=ADVANCED_FACE ( 'NONE', ( #5421 ), #2829, .T. ) ;
#14145=CARTESIAN_POINT ( 'NONE',  ( -23.15133049553021749, 8.673617379884035472E-16, -203.9554707965373268 ) ) ;
#14148=ADVANCED_FACE ( 'NONE', ( #11815, #13061 ), #15252, .F. ) ;
#14155=CARTESIAN_POINT ( 'NONE',  ( 8.807773658240529713, 15.00000000000000000, -105.8689255569511261 ) ) ;
#14171=EDGE_LOOP ( 'NONE', ( #128, #9425, #4749, #14241 ) ) ;
#14173=CARTESIAN_POINT ( 'NONE',  ( 10.36432819098247826, 8.673617379884035472E-16, -162.3272978866452831 ) ) ;
#14180=CARTESIAN_POINT ( 'NONE',  ( -0.7311112071359822107, 5.000000000000000888, -104.2753208119123798 ) ) ;
#14185=DIRECTION ( 'NONE',  ( 0.000000000000000000, 0.000000000000000000, -1.000000000000000000 ) ) ;
#14186=CARTESIAN_POINT ( 'NONE',  ( 8.694046762582464893, 5.000000000000000888, -116.9683691483771071 ) ) ;
#14187=VERTEX_POINT ( 'NONE', #10517 ) ;
#14192=EDGE_LOOP ( 'NONE', ( #12412, #1655, #12078, #13750 ) ) ;
#14193=CARTESIAN_POINT ( 'NONE',  ( -28.96136453847324788, 4.000000000000000000, -203.1938628845618666 ) ) ;
#14197=CARTESIAN_POINT ( 'NONE',  ( -0.06526978517727491380, 15.00000000000080824, -101.7940732946851341 ) ) ;
#14198=CIRCLE ( 'NONE', #8013, 3.000000000000005329 ) ;
#14204=DIRECTION ( 'NONE',  ( -0.9997619372588931741, -0.000000000000000000, -0.02181900108494707821 ) ) ;
#14213=CARTESIAN_POINT ( 'NONE',  ( 9.840588386097030238, 1.638247714399438948, -106.5338866644818125 ) ) ;
#14216=DIRECTION ( 'NONE',  ( 0.000000000000000000, 0.000000000000000000, 1.000000000000000000 ) ) ;
#14217=B_SPLINE_CURVE_WITH_KNOTS ( 'NONE', 3,
 ( #2968, #10299, #13720, #1890, #7680, #10155, #8840, #7833, #4211, #10234, #7900, #2039, #12547, #11161, #6750, #10007, #658, #4431 ),
 .UNSPECIFIED., .F., .F.,
 ( 4, 2, 2, 2, 2, 2, 2, 2, 4 ),
 ( 0.000000000000000000, 0.004943569348125147721, 0.007415354022187737627, 0.009887138696250326667, 0.01235892337031291484, 0.01359481570734420892, 0.01483070804437550301, 0.01730249271843805128, 0.01977427739250060129 ),
 .UNSPECIFIED. ) ;
#14220=CARTESIAN_POINT ( 'NONE',  ( 7.149317070426778997, 1.131903150115492362, 1.667266480437773257 ) ) ;
#14224=VERTEX_POINT ( 'NONE', #14078 ) ;
#14227=CARTESIAN_POINT ( 'NONE',  ( 17.37339609381778871, 6.000000000000000000, -130.0984517650821886 ) ) ;
#14235=EDGE_CURVE ( 'NONE', #13676, #9933, #5225, .T. ) ;
#14241=ORIENTED_EDGE ( 'NONE', *, *, #2836, .F. ) ;
#14242=ORIENTED_EDGE ( 'NONE', *, *, #1166, .F. ) ;
#14251=B_SPLINE_CURVE_WITH_KNOTS ( 'NONE', 3,
 ( #1494, #180, #11764, #4664, #10764, #29, #14330, #13170, #2501, #4892, #2351, #8287, #14257, #15270, #2580, #9531, #7280, #3586, #11994, #14103, #7196, #9602, #1418, #6123, #4970, #7049, #3504, #4818, #9685, #14417 ),
 .UNSPECIFIED., .F., .F.,
 ( 4, 2, 2, 2, 2, 2, 2, 2, 2, 2, 2, 2, 2, 2, 4 ),
 ( 6.938893903907228378E-18, 0.005155083077057498811, 0.007732624615586275105, 0.01031016615411505313, 0.01546524923117260572, 0.02062033230823015831, 0.02319787384675891725, 0.02577541538528767620, 0.02835295692381643515, 0.03093049846234519409, 0.03350804000087395651, 0.03479681077013833251, 0.03608558153940271546, 0.03866312307793146746, 0.04124066461646022641 ),
 .UNSPECIFIED. ) ;
#14254=CARTESIAN_POINT ( 'NONE',  ( -0.3803025174127598884, 5.000000000000000888, -103.2080563861792655 ) ) ;
#14256=EDGE_CURVE ( 'NONE', #12868, #8964, #10136, .T. ) ;
#14257=CARTESIAN_POINT ( 'NONE',  ( 5.703550681602465922, 8.673617379884033500E-16, -122.9904140605998890 ) ) ;
#14261=DIRECTION ( 'NONE',  ( -0.000000000000000000, -1.000000000000000000, -0.000000000000000000 ) ) ;
#14262=CARTESIAN_POINT ( 'NONE',  ( 10.27130088872558211, 5.000000000000000888, -120.9123952259834027 ) ) ;
#14268=CARTESIAN_POINT ( 'NONE',  ( -30.30611677948249039, 4.000000000000000888, -198.2470835936195783 ) ) ;
#14272=CARTESIAN_POINT ( 'NONE',  ( -2.424117392948417216, 9.999999999999998224, -107.6599666633534866 ) ) ;
#14275=CARTESIAN_POINT ( 'NONE',  ( 13.01561562359685276, 3.439206092960765293, -166.0850505222445008 ) ) ;
#14277=CARTESIAN_POINT ( 'NONE',  ( 11.00225911879145002, 8.749999999999998224, -91.84275802117696230 ) ) ;
#14278=VERTEX_POINT ( 'NONE', #157 ) ;
#14283=CARTESIAN_POINT ( 'NONE',  ( 17.43525470771941599, 8.749999999999998224, -88.70164870234812327 ) ) ;
#14285=CARTESIAN_POINT ( 'NONE',  ( 10.54544248586296717, 2.723356639041063953, -106.8702387211511819 ) ) ;
#14291=CARTESIAN_POINT ( 'NONE',  ( 8.026035668590276728, 2.099780044019236236, 2.291639928401612014 ) ) ;
#14308=CARTESIAN_POINT ( 'NONE',  ( 9.520855056337145683, 1.077704823981404338E-10, -163.5635978942416102 ) ) ;
#14309=CARTESIAN_POINT ( 'NONE',  ( 1.167531179896771798, 4.000000000000000000, -139.4941991647475845 ) ) ;
#14310=CARTESIAN_POINT ( 'NONE',  ( -3.868309323113294340, -5.416683946349036576E-13, -143.9840091578641363 ) ) ;
#14312=CARTESIAN_POINT ( 'NONE',  ( 6.766120961959584790, 0.8459668203398081898, 1.356709294556286860 ) ) ;
#14314=EDGE_LOOP ( 'NONE', ( #6894, #15008, #3076, #13886, #12568, #10728 ) ) ;
#14318=ORIENTED_EDGE ( 'NONE', *, *, #4680, .T. ) ;
#14320=CARTESIAN_POINT ( 'NONE',  ( -24.55211425566311689, 2.243498015498064377E-12, -206.7125218406129079 ) ) ;
#14325=ORIENTED_EDGE ( 'NONE', *, *, #15123, .T. ) ;
#14326=CARTESIAN_POINT ( 'NONE',  ( -7.230043083586494390, 0.9058721943649702402, -116.2995594653100682 ) ) ;
#14330=CARTESIAN_POINT ( 'NONE',  ( 13.55522405627131910, 8.673617379884037444E-16, -133.0209701713156392 ) ) ;
#14335=DIRECTION ( 'NONE',  ( 0.000000000000000000, 0.9434476287765544145, 0.3315216007380165641 ) ) ;
#14336=CARTESIAN_POINT ( 'NONE',  ( -6.451063615512949490, -8.037239669988805559E-13, -125.7472547710006694 ) ) ;
#14337=CARTESIAN_POINT ( 'NONE',  ( 9.374169689979092723, 8.673617379884035472E-16, -128.5794221292618431 ) ) ;
#14341=VERTEX_POINT ( 'NONE', #11205 ) ;
#14344=DIRECTION ( 'NONE',  ( 1.000000000000000000, 0.000000000000000000, 0.000000000000000000 ) ) ;
#14346=EDGE_CURVE ( 'NONE', #13403, #8964, #14593, .T. ) ;
#14351=CARTESIAN_POINT ( 'NONE',  ( -3.768042520815404917, 9.999999999999998224, -109.5986228335790145 ) ) ;
#14355=CIRCLE ( 'NONE', #10388, 7.000000000000000000 ) ;
#14357=CARTESIAN_POINT ( 'NONE',  ( 12.73427191684880277, 2.644333132995618119, -165.8787509141178020 ) ) ;
#14361=PLANE ( 'NONE',  #1099 ) ;
#14365=EDGE_CURVE ( 'NONE', #14224, #14065, #7946, .T. ) ;
#14367=CARTESIAN_POINT ( 'NONE',  ( -3.812461735095854287, 15.00000000000000178, -118.8814295322933390 ) ) ;
#14371=CARTESIAN_POINT ( 'NONE',  ( 14.17108320694883972, 12.64090008863623460, -126.4473401621325763 ) ) ;
#14373=CARTESIAN_POINT ( 'NONE',  ( 10.78057029805192180, 2.723356638990212186, -106.2467252071195389 ) ) ;
#14375=DIRECTION ( 'NONE',  ( 0.000000000000000000, 0.000000000000000000, 1.000000000000000000 ) ) ;
#14376=CARTESIAN_POINT ( 'NONE',  ( 1.243260443319662123, 6.000000000000000000, -139.4020581015306846 ) ) ;
#14379=CARTESIAN_POINT ( 'NONE',  ( 5.742112159410722505, 2.751696591659712698, 4.680416356127273581 ) ) ;
#14386=DIRECTION ( 'NONE',  ( 0.5205261093005589812, 0.000000000000000000, -0.8538457527776445177 ) ) ;
#14394=CARTESIAN_POINT ( 'NONE',  ( 9.500324903962138023, 2.296263824619149852E-15, -163.5886270269263889 ) ) ;
#14397=CARTESIAN_POINT ( 'NONE',  ( 1.078231930479242484, 6.000000000000000000, -139.4303258909232852 ) ) ;
#14399=B_SPLINE_CURVE_WITH_KNOTS ( 'NONE', 3,
 ( #10078, #13500, #5434, #7757, #14813, #12546, #10154, #4210, #8991, #11387, #4139, #8839, #5217, #4067, #13644, #9928 ),
 .UNSPECIFIED., .F., .F.,
 ( 4, 2, 2, 2, 2, 2, 2, 4 ),
 ( 0.000000000000000000, 0.0004968996385939453836, 0.0009937992771878907672, 0.001490698915781836151, 0.001987598554375781534, 0.002484498192969726918, 0.002981397831563672302, 0.003975197108751563069 ),
 .UNSPECIFIED. ) ;
#14400=CARTESIAN_POINT ( 'NONE',  ( -1.870253773668272945, 8.673617379884035472E-16, -147.6241727244333504 ) ) ;
#14411=CARTESIAN_POINT ( 'NONE',  ( -6.777586278698636946, 0.5200622811955745162, -116.7594943224618191 ) ) ;
#14417=CARTESIAN_POINT ( 'NONE',  ( 6.288457687488933523, 0.000000000000000000, -105.0111312234435985 ) ) ;
#14422=CARTESIAN_POINT ( 'NONE',  ( -7.251835631666873283, 7.915809026670424014E-13, -123.8995801872388824 ) ) ;
#14423=CARTESIAN_POINT ( 'NONE',  ( 19.51808381319401065, 4.284816698714185730E-13, -131.6416685808667069 ) ) ;
#14429=ORIENTED_EDGE ( 'NONE', *, *, #5368, .F. ) ;
#14431=CARTESIAN_POINT ( 'NONE',  ( 23.38516724735982777, 0.4291895315141152634, -138.6768690072186700 ) ) ;
#14436=ORIENTED_EDGE ( 'NONE', *, *, #1668, .T. ) ;
#14437=CARTESIAN_POINT ( 'NONE',  ( -3.768042520875636292, 15.00000000000000000, -109.5986228335309391 ) ) ;
#14440=VECTOR ( 'NONE', #10130, 1000.000000000000000 ) ;
#14452=DIRECTION ( 'NONE',  ( 0.000000000000000000, 1.000000000000000000, 0.000000000000000000 ) ) ;
#14457=CARTESIAN_POINT ( 'NONE',  ( 8.711870733155482327, 0.6047360044100810184, -105.8325059764879370 ) ) ;
#14463=CARTESIAN_POINT ( 'NONE',  ( 6.082631124755410568, 0.4612449235174558293, 0.6929822686081172911 ) ) ;
#14470=CARTESIAN_POINT ( 'NONE',  ( 8.807773658237110226, 15.00000000000000000, -105.8689255569501171 ) ) ;
#14477=CARTESIAN_POINT ( 'NONE',  ( 13.14021484082229030, 4.050274393866083678, -166.1764203671933444 ) ) ;
#14480=CARTESIAN_POINT ( 'NONE',  ( -4.375735311315418485, 3.999999999999874767, -143.3439008670868020 ) ) ;
#14482=CARTESIAN_POINT ( 'NONE',  ( -25.78682146806830033, 8.673617379884035472E-16, -192.1400676150700804 ) ) ;
#14493=CARTESIAN_POINT ( 'NONE',  ( -8.923457816048948388, 2.191178284877700833, -116.0747321664481717 ) ) ;
#14501=CARTESIAN_POINT ( 'NONE',  ( -8.326762664983050399, -7.864679486792610604E-13, -121.0857513972968604 ) ) ;
#14502=CARTESIAN_POINT ( 'NONE',  ( 8.300023318284271312, -4.283195660063827066E-13, -113.4762057881885795 ) ) ;
#14505=DIRECTION ( 'NONE',  ( 0.000000000000000000, 0.000000000000000000, 1.000000000000000000 ) ) ;
#14506=ORIENTED_EDGE ( 'NONE', *, *, #14544, .T. ) ;
#14515=CARTESIAN_POINT ( 'NONE',  ( -9.476787056091271921, 9.999999999999998224, -115.4301398046334981 ) ) ;
#14517=CARTESIAN_POINT ( 'NONE',  ( -25.43320932775275978, 3.897330828535134017, -209.0242640618165808 ) ) ;
#14518=CARTESIAN_POINT ( 'NONE',  ( 10.23189628017364505, 0.1924065811658746683, -164.0445219108954973 ) ) ;
#14519=FACE_OUTER_BOUND ( 'NONE', #15206, .T. ) ;
#14526=EDGE_CURVE ( 'NONE', #11140, #5472, #12820, .T. ) ;
#14527=DIRECTION ( 'NONE',  ( 0.000000000000000000, 0.000000000000000000, -1.000000000000000000 ) ) ;
#14531=CARTESIAN_POINT ( 'NONE',  ( 9.114992375658264478, 0.8572809181108925758, -105.9776340796685332 ) ) ;
#14537=CARTESIAN_POINT ( 'NONE',  ( 8.409813745801482554, 2.751696592305300282, 2.538033216846526940 ) ) ;
#14544=EDGE_CURVE ( 'NONE', #3281, #8227, #12122, .T. ) ;
#14556=CARTESIAN_POINT ( 'NONE',  ( -2.515578278476028107, 8.673617379884035472E-16, -148.1512477234490177 ) ) ;
#14561=VERTEX_POINT ( 'NONE', #992 ) ;
#14563=CARTESIAN_POINT ( 'NONE',  ( 12.67805275830794898, 8.673617379884037444E-16, -154.9658299924666665 ) ) ;
#14567=ORIENTED_EDGE ( 'NONE', *, *, #14635, .T. ) ;
#14576=CARTESIAN_POINT ( 'NONE',  ( -5.134731047560421757, 1.592765399726224076E-12, -128.4544621779126885 ) ) ;
#14579=AXIS2_PLACEMENT_3D ( 'NONE', #11259, #6391, #756 ) ;
#14580=DIRECTION ( 'NONE',  ( -8.764770998266003672E-18, 0.000000000000000000, -1.000000000000000000 ) ) ;
#14583=CARTESIAN_POINT ( 'NONE',  ( 27.03835354040201011, 4.628448260288817728, -138.2189567750509127 ) ) ;
#14587=ORIENTED_EDGE ( 'NONE', *, *, #4956, .F. ) ;
#14591=FACE_OUTER_BOUND ( 'NONE', #905, .T. ) ;
#14593=B_SPLINE_CURVE_WITH_KNOTS ( 'NONE', 3,
 ( #9034, #4398, #5258, #11428, #13539, #13759, #5554, #3154, #9107, #3017, #627, #6487, #15002, #8957, #12665, #1859, #4331, #850 ),
 .UNSPECIFIED., .F., .F.,
 ( 4, 2, 2, 2, 2, 2, 2, 2, 4 ),
 ( 0.000000000000000000, 0.001051779247122254166, 0.002103558494244507030, 0.003155337741366759895, 0.004207116988489012326, 0.005258896235611266491, 0.006310675482733521524, 0.007362454729855774822, 0.008414233976978029855 ),
 .UNSPECIFIED. ) ;
#14594=CARTESIAN_POINT ( 'NONE',  ( 11.57097051246173969, 14.81307274914749961, -125.6777153510405185 ) ) ;
#14600=VERTEX_POINT ( 'NONE', #4771 ) ;
#14608=AXIS2_PLACEMENT_3D ( 'NONE', #10002, #3824, #7287 ) ;
#14622=CIRCLE ( 'NONE', #7162, 2.000000000000007994 ) ;
#14626=CARTESIAN_POINT ( 'NONE',  ( 1.243260443319662123, 4.179859613694246079, -139.4020581015306846 ) ) ;
#14634=CARTESIAN_POINT ( 'NONE',  ( 12.67258870470521614, 3.477781664713254894, -166.5210692261007637 ) ) ;
#14635=EDGE_CURVE ( 'NONE', #4330, #13403, #5694, .T. ) ;
#14638=CARTESIAN_POINT ( 'NONE',  ( -30.65815467000176042, 3.999999999999813483, -194.1257268749498337 ) ) ;
#14639=CARTESIAN_POINT ( 'NONE',  ( 5.651020395687034181, 0.03103945442896835147, -140.5875639640649979 ) ) ;
#14640=CARTESIAN_POINT ( 'NONE',  ( 8.935548306746159852, 4.627360597499654560, 2.855381328098121507 ) ) ;
#14644=CARTESIAN_POINT ( 'NONE',  ( -22.23979083886640851, 4.000000000000000000, -203.8707431750928833 ) ) ;
#14654=ADVANCED_FACE ( 'NONE', ( #12974 ), #2378, .T. ) ;
#14656=CARTESIAN_POINT ( 'NONE',  ( -0.1621610436782315590, 4.999999999999206857, -136.1940307094523632 ) ) ;
#14657=CARTESIAN_POINT ( 'NONE',  ( 9.550372274932042771, 5.000000000000000888, -109.1178429856281156 ) ) ;
#14658=LINE ( 'NONE', #13495, #10632 ) ;
#14662=CARTESIAN_POINT ( 'NONE',  ( 8.895558325401111688, 6.000000000000000000, -141.4560052469132643 ) ) ;
#14671=CARTESIAN_POINT ( 'NONE',  ( -5.309262520577839872, 6.000000000000000000, -125.0911079416483176 ) ) ;
#14673=CARTESIAN_POINT ( 'NONE',  ( -25.14935590298316015, 3.999999999999999112, -209.2172623628708550 ) ) ;
#14678=FACE_OUTER_BOUND ( 'NONE', #6213, .T. ) ;
#14682=EDGE_LOOP ( 'NONE', ( #1506, #14318, #11912, #11770 ) ) ;
#14700=CARTESIAN_POINT ( 'NONE',  ( -1.313187589810638434, 10.00000000000000000, -105.6642581345501668 ) ) ;
#14701=CARTESIAN_POINT ( 'NONE',  ( 10.26465888295316020, 14.41280555647187889, -106.6644705394424619 ) ) ;
#14702=ADVANCED_FACE ( 'NONE', ( #12109 ), #10710, .F. ) ;
#14711=CARTESIAN_POINT ( 'NONE',  ( 12.62779646475434703, 2.635826865785323214, -166.1237625897486794 ) ) ;
#14712=CIRCLE ( 'NONE', #8018, 3.500000000000003109 ) ;
#14713=CARTESIAN_POINT ( 'NONE',  ( 8.665381006182327539, 0.6447310902546593558, -106.0007322442988738 ) ) ;
#14714=CARTESIAN_POINT ( 'NONE',  ( -30.17254888771753585, 3.999999999999511502, -186.2931491953524983 ) ) ;
#14719=ORIENTED_EDGE ( 'NONE', *, *, #12555, .T. ) ;
#14720=DIRECTION ( 'NONE',  ( 0.000000000000000000, 0.000000000000000000, 1.000000000000000000 ) ) ;
#14724=CARTESIAN_POINT ( 'NONE',  ( 10.97171279554003043, 8.773889247172311556, -44.61149169061435060 ) ) ;
#14725=ADVANCED_FACE ( 'NONE', ( #5161 ), #4847, .T. ) ;
#14729=CARTESIAN_POINT ( 'NONE',  ( 1.243260443319662123, 6.000000000000000000, -139.4020581015306846 ) ) ;
#14734=DIRECTION ( 'NONE',  ( 0.9997619372588932851, -0.000000000000000000, 0.02181900108494707474 ) ) ;
#14735=CARTESIAN_POINT ( 'NONE',  ( 9.112041370329526657, 5.000000000000000888, -109.9899024349129775 ) ) ;
#14741=CARTESIAN_POINT ( 'NONE',  ( 10.08988835584683308, 12.49999999999999822, -120.5979435464156211 ) ) ;
#14746=EDGE_CURVE ( 'NONE', #6908, #7480, #7237, .T. ) ;
#14753=CARTESIAN_POINT ( 'NONE',  ( -5.561182064723690921, 14.89159520570006379, -117.2542806587632214 ) ) ;
#14755=CARTESIAN_POINT ( 'NONE',  ( 13.03594997074850959, 15.00000000000000000, -125.1067209764227073 ) ) ;
#14766=AXIS2_PLACEMENT_3D ( 'NONE', #3819, #1574, #9687 ) ;
#14767=CARTESIAN_POINT ( 'NONE',  ( 11.28440626344662157, 4.315957715789585869, -106.3983886562123331 ) ) ;
#14781=EDGE_LOOP ( 'NONE', ( #3341, #13820, #3397, #4445 ) ) ;
#14785=CARTESIAN_POINT ( 'NONE',  ( 9.920343557553863434, 0.09491738922561235303, -163.9751099406502703 ) ) ;
#14790=CARTESIAN_POINT ( 'NONE',  ( -24.49765103532420341, 5.421660010089610387E-13, -170.6954199489630355 ) ) ;
#14795=CARTESIAN_POINT ( 'NONE',  ( 10.94278504614969982, 5.000000000000001776, -43.28600191872154568 ) ) ;
#14796=CARTESIAN_POINT ( 'NONE',  ( 9.573673229721526567, 1.209833687612193343, -105.8952646585356234 ) ) ;
#14799=CARTESIAN_POINT ( 'NONE',  ( -9.076832803613504197, 2.617545850183311540, -116.5147594324866134 ) ) ;
#14801=CARTESIAN_POINT ( 'NONE',  ( 6.422699671861705539, 4.000000000000000000, -139.1645012375703061 ) ) ;
#14807=EDGE_CURVE ( 'NONE', #14600, #7347, #12637, .T. ) ;
#14809=CARTESIAN_POINT ( 'NONE',  ( 3.473492316508982380, 8.673617379884035472E-16, -116.2542051831695602 ) ) ;
#14813=CARTESIAN_POINT ( 'NONE',  ( 8.973057892629592303, 12.37556808675488718, 1.136665787335843669 ) ) ;
#14814=CARTESIAN_POINT ( 'NONE',  ( 9.348010916527714542, 12.50000000000000000, -118.9691738015868339 ) ) ;
#14820=CARTESIAN_POINT ( 'NONE',  ( 10.98449899626661974, 11.68766481771978505, -45.34906724785665233 ) ) ;
#14822=CARTESIAN_POINT ( 'NONE',  ( -25.06471962037405277, 4.000000000000000000, -209.2255395231934472 ) ) ;
#14825=CARTESIAN_POINT ( 'NONE',  ( 9.136110106353408256, 12.49999999999999822, -109.8557328641390711 ) ) ;
#14827=CARTESIAN_POINT ( 'NONE',  ( 23.30137936743921756, 0.3998921152664920986, -138.6870304616822693 ) ) ;
#14828=EDGE_CURVE ( 'NONE', #8798, #1605, #11791, .T. ) ;
#14831=CARTESIAN_POINT ( 'NONE',  ( 1.167531179896771798, 4.000000000000000000, -139.4941991647475845 ) ) ;
#14835=DIRECTION ( 'NONE',  ( 0.9997619372588932851, 0.000000000000000000, 0.02181900108494707821 ) ) ;
#14843=CARTESIAN_POINT ( 'NONE',  ( 8.328184646254079837, 5.000000000000001776, -113.2132428591397542 ) ) ;
#14851=CARTESIAN_POINT ( 'NONE',  ( -8.226857985479757218, 10.00000000000000000, -114.4011953629546241 ) ) ;
#14853=CARTESIAN_POINT ( 'NONE',  ( 11.04730217088352617, 12.49999999999999822, -107.1178495010082088 ) ) ;
#14858=LINE ( 'NONE', #11128, #4232 ) ;
#14862=CARTESIAN_POINT ( 'NONE',  ( 4.999922786458842694, 0.03165940129594203845, -16.23938796091260528 ) ) ;
#14863=CARTESIAN_POINT ( 'NONE',  ( 5.904219792619186613, 15.00000000000000000, -112.3087459549632428 ) ) ;
#14864=CARTESIAN_POINT ( 'NONE',  ( 4.950900406836915124, 5.000000000000000888, -134.4284351762048573 ) ) ;
#14867=CARTESIAN_POINT ( 'NONE',  ( -23.99665711257156886, 8.673617379884035472E-16, -181.0464554320757884 ) ) ;
#14868=CARTESIAN_POINT ( 'NONE',  ( 12.66298273264138174, 3.439231053088831036, -166.5121423616285767 ) ) ;
#14872=LINE ( 'NONE', #5342, #14440 ) ;
#14875=CARTESIAN_POINT ( 'NONE',  ( -5.318033920858916908, 9.999999999999998224, -111.4753907371908923 ) ) ;
#14877=FACE_OUTER_BOUND ( 'NONE', #2317, .T. ) ;
#14880=CARTESIAN_POINT ( 'NONE',  ( 10.99551757066058322, 11.56847231179307478, -45.70224318734323532 ) ) ;
#14883=LINE ( 'NONE', #9135, #8998 ) ;
#14885=DIRECTION ( 'NONE',  ( -0.9997619372588931741, -0.000000000000000000, -0.02181900108494707474 ) ) ;
#14886=CARTESIAN_POINT ( 'NONE',  ( 1.320501113854931630, 5.000000000000000888, -137.8664870916819893 ) ) ;
#14890=CARTESIAN_POINT ( 'NONE',  ( 14.22910372453204353, 12.49999999999999822, -126.5134921567817941 ) ) ;
#14897=EDGE_CURVE ( 'NONE', #8964, #9805, #5931, .T. ) ;
#14898=CARTESIAN_POINT ( 'NONE',  ( 10.94790802041948652, 11.56847231179307478, -43.52074019388547299 ) ) ;
#14900=CARTESIAN_POINT ( 'NONE',  ( 5.456070725290617318, 2.049461655773607394, 4.191750790487847489 ) ) ;
#14901=CARTESIAN_POINT ( 'NONE',  ( -9.721966606378854792, 10.00000000000000000, -116.3614657639809451 ) ) ;
#14903=CARTESIAN_POINT ( 'NONE',  ( 12.15266112757328898, 12.49999999999999822, -123.9192486816531442 ) ) ;
#14904=CARTESIAN_POINT ( 'NONE',  ( -9.525540565743060739, 11.37243141597640061, -116.4087343257888705 ) ) ;
#14906=CARTESIAN_POINT ( 'NONE',  ( 26.30988878369277018, 2.644888176784162326, -138.3124949328119726 ) ) ;
#14912=CARTESIAN_POINT ( 'NONE',  ( 29.21736815051484015, 8.773889247172311556, -44.21329492081407153 ) ) ;
#14922=CARTESIAN_POINT ( 'NONE',  ( 17.88039419560352172, 5.000000000000000888, -130.2352974121733951 ) ) ;
#14926=AXIS2_PLACEMENT_3D ( 'NONE', #5065, #13424, #10934 ) ;
#14928=CARTESIAN_POINT ( 'NONE',  ( 11.03230074683944473, 12.83501270603766997, -107.1089630900316791 ) ) ;
#14939=CARTESIAN_POINT ( 'NONE',  ( 11.32016196459912649, 5.000000000000000888, -106.4092894470390291 ) ) ;
#14941=ORIENTED_EDGE ( 'NONE', *, *, #9219, .F. ) ;
#14942=CARTESIAN_POINT ( 'NONE',  ( -29.86630916335285946, 1.632654739009349985E-12, -191.5040656882066799 ) ) ;
#14943=CARTESIAN_POINT ( 'NONE',  ( 9.283947375375564803, 1.156835247712560688E-15, -163.3899434529763539 ) ) ;
#14946=ORIENTED_EDGE ( 'NONE', *, *, #2909, .T. ) ;
#14947=CARTESIAN_POINT ( 'NONE',  ( 10.32040002734025741, 5.000000000000000888, -106.4311084481271763 ) ) ;
#14950=CARTESIAN_POINT ( 'NONE',  ( -25.22418021123103671, 0.005679765489689153624, -199.5580873402903421 ) ) ;
#14951=CARTESIAN_POINT ( 'NONE',  ( 6.134629758992640625, 11.62037896290623884, 5.022017130777459926 ) ) ;
#14952=CARTESIAN_POINT ( 'NONE',  ( 3.167496085401364958, 8.673617379884035472E-16, -107.8568673623658754 ) ) ;
#14957=DIRECTION ( 'NONE',  ( 2.672056983927306511E-18, 1.000000000000000000, -1.224355256373460583E-16 ) ) ;
#14964=DIRECTION ( 'NONE',  ( 0.000000000000000000, 0.000000000000000000, 1.000000000000000000 ) ) ;
#14973=CARTESIAN_POINT ( 'NONE',  ( 10.96506322933161570, 11.77387500534620557, -44.79864310745833933 ) ) ;
#14975=CARTESIAN_POINT ( 'NONE',  ( -8.456080320763300406, 13.34348931139960293, -116.2291922150413654 ) ) ;
#14977=CARTESIAN_POINT ( 'NONE',  ( 5.990830680408624431, 15.00000000000000000, -116.1960808033739880 ) ) ;
#14979=CARTESIAN_POINT ( 'NONE',  ( 24.58533183484775719, 0.8477912208884822443, -138.1065029955142620 ) ) ;
#14982=CARTESIAN_POINT ( 'NONE',  ( -26.52423092236888635, 4.000000000000000888, -173.1808044485809717 ) ) ;
#14988=CARTESIAN_POINT ( 'NONE',  ( -25.23790167279625862, 0.7328807590307473419, -204.7435413102125210 ) ) ;
#14991=DIRECTION ( 'NONE',  ( -0.9997619372588932851, 0.000000000000000000, -0.02181900108494707474 ) ) ;
#15002=CARTESIAN_POINT ( 'NONE',  ( -6.572203743845886237, 0.4630310843464179871, -117.0568686706825048 ) ) ;
#15004=CARTESIAN_POINT ( 'NONE',  ( 11.32016196459912649, 12.49999999999999822, -106.4092894470390291 ) ) ;
#15006=CARTESIAN_POINT ( 'NONE',  ( 5.228075279701640099, 4.000000000000000000, -167.7939279834373849 ) ) ;
#15008=ORIENTED_EDGE ( 'NONE', *, *, #1771, .T. ) ;
#15010=CARTESIAN_POINT ( 'NONE',  ( 8.552111707065320090, 3.043081950488160103, 5.304473962697122680 ) ) ;
#15018=CARTESIAN_POINT ( 'NONE',  ( 10.63021595323582069, 2.452426006596266195, -106.2019669008089409 ) ) ;
#15019=DIRECTION ( 'NONE',  ( -0.000000000000000000, -1.000000000000000000, -0.000000000000000000 ) ) ;
#15021=CARTESIAN_POINT ( 'NONE',  ( 8.976503672017095425, 12.42208448007280275, 0.9787777583466945597 ) ) ;
#15046=CARTESIAN_POINT ( 'NONE',  ( -8.923457816049095825, 12.80882171512263312, -116.0747321664441074 ) ) ;
#15048=CARTESIAN_POINT ( 'NONE',  ( 10.31224696326443535, 14.99999999999627320, -121.0233796642843913 ) ) ;
#15052=CARTESIAN_POINT ( 'NONE',  ( 26.60417991234133339, 3.130032034377395522, -138.2748749807007016 ) ) ;
#15057=CARTESIAN_POINT ( 'NONE',  ( 29.24464190187102375, 8.773889247172311556, -45.46299734238769474 ) ) ;
#15064=CARTESIAN_POINT ( 'NONE',  ( -25.70158769154330258, 0.8049789667686304551, -204.9870591480219844 ) ) ;
#15073=CARTESIAN_POINT ( 'NONE',  ( -5.309262520577839872, 6.000000000000000000, -125.0911079416483176 ) ) ;
#15077=ADVANCED_FACE ( 'NONE', ( #1201 ), #3501, .T. ) ;
#15079=CARTESIAN_POINT ( 'NONE',  ( 1.320501113854931408, 5.000000000000000888, -137.8664870916819893 ) ) ;
#15086=ORIENTED_EDGE ( 'NONE', *, *, #9004, .F. ) ;
#15093=ORIENTED_EDGE ( 'NONE', *, *, #15271, .T. ) ;
#15096=VECTOR ( 'NONE', #10190, 1000.000000000000000 ) ;
#15097=CARTESIAN_POINT ( 'NONE',  ( 8.881162068611669014, 11.71160396371214496, 5.347396915146337193 ) ) ;
#15098=CARTESIAN_POINT ( 'NONE',  ( -2.424117392950516869, 5.000000000000000888, -107.6599666633565988 ) ) ;
#15100=ADVANCED_FACE ( 'NONE', ( #10557 ), #3252, .T. ) ;
#15101=CARTESIAN_POINT ( 'NONE',  ( 27.13166404935670073, 8.673617379884035472E-16, -138.0564292571840213 ) ) ;
#15107=CARTESIAN_POINT ( 'NONE',  ( 1.004809442601927394, 5.000000000000000888, -139.4752805618705622 ) ) ;
#15120=EDGE_LOOP ( 'NONE', ( #13788, #10212, #7456, #12953 ) ) ;
#15122=CARTESIAN_POINT ( 'NONE',  ( -0.8684534520279959535, 5.000000000000001776, -104.6281219612548341 ) ) ;
#15123=EDGE_CURVE ( 'NONE', #7276, #13215, #964, .T. ) ;
#15128=CARTESIAN_POINT ( 'NONE',  ( 10.88443679120024399, 8.773889247172311556, -40.61244394157877480 ) ) ;
#15129=DIRECTION ( 'NONE',  ( 0.000000000000000000, 0.000000000000000000, 1.000000000000000000 ) ) ;
#15130=VERTEX_POINT ( 'NONE', #3675 ) ;
#15131=CARTESIAN_POINT ( 'NONE',  ( 1.260825460258694797, 4.119514498333133545, -139.4012524756404332 ) ) ;
#15134=ORIENTED_EDGE ( 'NONE', *, *, #6925, .T. ) ;
#15136=CARTESIAN_POINT ( 'NONE',  ( -26.52470037256358992, 4.000000000000000000, -207.7145413388536781 ) ) ;
#15145=CARTESIAN_POINT ( 'NONE',  ( -25.55455346258773375, 2.452721150094688607, -207.9965800587423814 ) ) ;
#15149=CARTESIAN_POINT ( 'NONE',  ( 25.37775455676784730, 5.000000000000000888, -136.0262733555301224 ) ) ;
#15152=CARTESIAN_POINT ( 'NONE',  ( -4.122964195042671420, 10.00000000000000355, -110.0534507760547314 ) ) ;
#15153=AXIS2_PLACEMENT_3D ( 'NONE', #14912, #14835, #5682 ) ;
#15162=( BOUNDED_SURFACE ( )  B_SPLINE_SURFACE ( 3, 1, ( 
 ( #3932, #2856 ),
 ( #530, #6471 ),
 ( #1613, #6396 ),
 ( #2925, #5319 ) ),
 .UNSPECIFIED., .F., .F., .F. ) 
 B_SPLINE_SURFACE_WITH_KNOTS ( ( 4, 4 ),
 ( 2, 2 ),
 ( 0.000000000000000000, 1.000000000000000000 ),
 ( 0.000000000000000000, 1.000000000000000000 ),
 .UNSPECIFIED. ) 
 GEOMETRIC_REPRESENTATION_ITEM ( )  RATIONAL_B_SPLINE_SURFACE ( (
 ( 1.000000000000000000, 1.000000000000000000),
 ( 0.8656789684289789566, 0.8656789684289789566),
 ( 0.8656789684289789566, 0.8656789684289789566),
 ( 1.000000000000000000, 1.000000000000000000) ) ) 
 REPRESENTATION_ITEM ( '' )  SURFACE ( )  );
#15164=DIRECTION ( 'NONE',  ( 0.000000000000000000, 1.000000000000000000, 0.000000000000000000 ) ) ;
#15166=CARTESIAN_POINT ( 'NONE',  ( 8.669753383557360138, 3.405435594033015878, 5.423001458801155472 ) ) ;
#15172=ORIENTED_EDGE ( 'NONE', *, *, #9715, .T. ) ;
#15175=CARTESIAN_POINT ( 'NONE',  ( 8.875022499991096936, 9.999999999999747757, 5.628716256677545715 ) ) ;
#15179=DIRECTION ( 'NONE',  ( -0.9997619372588931741, 0.000000000000000000, -0.02181900108494707127 ) ) ;
#15181=DIRECTION ( 'NONE',  ( 0.000000000000000000, 1.000000000000000000, 0.000000000000000000 ) ) ;
#15183=B_SPLINE_CURVE_WITH_KNOTS ( 'NONE', 3,
 ( #15107, #7032, #10588, #5727 ),
 .UNSPECIFIED., .F., .F.,
 ( 4, 4 ),
 ( 0.000000000000000000, 1.000000000000000000 ),
 .UNSPECIFIED. ) ;
#15184=DIRECTION ( 'NONE',  ( -1.225982338248072509E-13, 0.000000000000000000, -1.000000000000000000 ) ) ;
#15190=EDGE_CURVE ( 'NONE', #7952, #5770, #13520, .T. ) ;
#15192=LINE ( 'NONE', #4585, #4513 ) ;
#15195=VECTOR ( 'NONE', #10206, 1000.000000000000000 ) ;
#15204=CARTESIAN_POINT ( 'NONE',  ( 10.82638304870340029, 12.49999999999999822, -107.3456397791438235 ) ) ;
#15205=CARTESIAN_POINT ( 'NONE',  ( 5.228075279701640099, 1.000000000000000000, -165.7939279834373849 ) ) ;
#15206=EDGE_LOOP ( 'NONE', ( #12329, #11098, #3827 ) ) ;
#15213=CARTESIAN_POINT ( 'NONE',  ( 9.044950117654433797, -4.000000000000000000, -137.9826476090360643 ) ) ;
#15215=ADVANCED_FACE ( 'NONE', ( #7689 ), #1970, .T. ) ;
#15217=ORIENTED_EDGE ( 'NONE', *, *, #8627, .T. ) ;
#15219=CARTESIAN_POINT ( 'NONE',  ( 1.814459646441706209, 14.99999999999999822, -110.3167319592368329 ) ) ;
#15222=CARTESIAN_POINT ( 'NONE',  ( -25.17932510765911047, 0.9650723256931513783, -205.4209994318837857 ) ) ;
#15223=DIRECTION ( 'NONE',  ( 0.9997619372588932851, 0.000000000000000000, 0.02181900108494707821 ) ) ;
#15229=CARTESIAN_POINT ( 'NONE',  ( 4.248871783098665311, 6.000000000000000000, -126.1456066832003842 ) ) ;
#15239=CARTESIAN_POINT ( 'NONE',  ( 9.991434137473303778, 4.873277969712327184, -45.52604821315951966 ) ) ;
#15240=ORIENTED_EDGE ( 'NONE', *, *, #7718, .F. ) ;
#15241=CARTESIAN_POINT ( 'NONE',  ( -27.33151177440234392, 4.000000000000656364, -206.5142783688401948 ) ) ;
#15248=CARTESIAN_POINT ( 'NONE',  ( -25.62889119307865116, 0.2563525944202221796, -202.7491877320029801 ) ) ;
#15250=CARTESIAN_POINT ( 'NONE',  ( 6.348887620881822791, 14.84416895885140875, 1.551339895120714685 ) ) ;
#15252=PLANE ( 'NONE',  #2012 ) ;
#15256=CARTESIAN_POINT ( 'NONE',  ( 21.56941276937137530, 0.02712874445307413007, -138.7330449865694391 ) ) ;
#15263=FACE_OUTER_BOUND ( 'NONE', #5660, .T. ) ;
#15267=ORIENTED_EDGE ( 'NONE', *, *, #1256, .T. ) ;
#15269=CARTESIAN_POINT ( 'NONE',  ( -1.313187589810638212, 5.000000000000000000, -105.6642581345501526 ) ) ;
#15270=CARTESIAN_POINT ( 'NONE',  ( 4.962552820103347528, 8.673617379884034486E-16, -121.4286218404057678 ) ) ;
#15271=EDGE_CURVE ( 'NONE', #40, #6618, #9068, .T. ) ;
#15272=CARTESIAN_POINT ( 'NONE',  ( 0.000000000000000000, 0.000000000000000000, 0.000000000000000000 ) ) ;
#15276=CARTESIAN_POINT ( 'NONE',  ( 19.51808381314846841, 5.000000000000000888, -131.6416685809227545 ) ) ;
#15282=LINE ( 'NONE', #1050, #348 ) ;
#15286=CARTESIAN_POINT ( 'NONE',  ( 6.124339417936002228, 10.65787600314544470, 5.248591459689508021 ) ) ;
#15289=CARTESIAN_POINT ( 'NONE',  ( -25.38784507181503614, 1.060216903838750113, -206.1915231985982757 ) ) ;
#15290=CARTESIAN_POINT ( 'NONE',  ( -2.276491945804053785, -4.336808689942018525E-15, -122.8215887834235787 ) ) ;
#15296=DIRECTION ( 'NONE',  ( 0.8538457527776451839, 0.000000000000000000, 0.5205261093005582040 ) ) ;
#15301=CARTESIAN_POINT ( 'NONE',  ( 1.049898006922821869, 4.588323854676484181, -139.4675471490223515 ) ) ;
#15303=CARTESIAN_POINT ( 'NONE',  ( -1.286431735982999758, 5.000000000000007105, -134.7299422376718496 ) ) ;
#15313=CARTESIAN_POINT ( 'NONE',  ( -25.80176686614077042, -6.001942919173320219E-12, -207.3616737857323642 ) ) ;
#15316=VECTOR ( 'NONE', #8711, 1000.000000000000000 ) ;
#15325=COLOUR_RGB('Deep Blue', 0.66274510, 0.83137255, 0.94901961);
#15326=FILL_AREA_STYLE_COLOUR('',#15325);
#15327=FILL_AREA_STYLE('',(#15326));
#15328=SURFACE_STYLE_FILL_AREA(#15327);
#15329=SURFACE_SIDE_STYLE('',(#15328));
#15330=SURFACE_STYLE_USAGE(.BOTH.,#15329);
#15331=PRESENTATION_STYLE_ASSIGNMENT((#15330));
#15377=STYLED_ITEM('',(#15331),#2140);
#15378=MECHANICAL_DESIGN_GEOMETRIC_PRESENTATION_REPRESENTATION('',(#15377),#3238);
ENDSEC;
END-ISO-10303-21;
